ISO-10303-21;
HEADER;
FILE_DESCRIPTION (('STEP AP214'),
    '1' );
FILE_NAME ('Spider.step',
    '2026-10-24T18:16:00',
    ( '' ),
    ( '' ),
    'SwSTEP 2.0',
    'SolidWorks 2025',
    '' );
FILE_SCHEMA (( 'AUTOMOTIVE_DESIGN' ));
ENDSEC;

DATA;
#2=ORIENTED_EDGE ( 'NONE', *, *, #580, .T. ) ;
#4=EDGE_CURVE ( 'NONE', #13144, #1499, #258, .T. ) ;
#5=CARTESIAN_POINT ( 'NONE',  ( 0.5595825771504284729, -0.1023622047244094474, 0.2048774586467246028 ) ) ;
#6=DIRECTION ( 'NONE',  ( 0.000000000000000000, 0.000000000000000000, 1.000000000000000000 ) ) ;
#8=VERTEX_POINT ( 'NONE', #4783 ) ;
#9=EDGE_LOOP ( 'NONE', ( #10778, #398, #8347, #5779 ) ) ;
#15=CARTESIAN_POINT ( 'NONE',  ( -0.2742631158500640209, -0.2952755905511811885, 0.2765435766697811881 ) ) ;
#19=CARTESIAN_POINT ( 'NONE',  ( 0.4625984251968510708, -0.1023622047244094474, 0.3807329531073309070 ) ) ;
#22=ORIENTED_EDGE ( 'NONE', *, *, #7341, .F. ) ;
#23=ADVANCED_FACE ( 'NONE', ( #187 ), #12882, .T. ) ;
#26=DIRECTION ( 'NONE',  ( 1.000000000000000000, 0.000000000000000000, 0.000000000000000000 ) ) ;
#27=LINE ( 'NONE', #5793, #612 ) ;
#32=ORIENTED_EDGE ( 'NONE', *, *, #5752, .F. ) ;
#33=CARTESIAN_POINT ( 'NONE',  ( -0.5905511811023629321, -0.09448818897637796532, 0.1591122789105256785 ) ) ;
#34=PLANE ( 'NONE',  #8140 ) ;
#38=EDGE_LOOP ( 'NONE', ( #10279, #15210, #1798, #2256 ) ) ;
#39=EDGE_CURVE ( 'NONE', #10242, #2574, #9139, .T. ) ;
#40=ORIENTED_EDGE ( 'NONE', *, *, #8775, .T. ) ;
#41=ORIENTED_EDGE ( 'NONE', *, *, #6196, .F. ) ;
#42=ORIENTED_EDGE ( 'NONE', *, *, #10757, .F. ) ;
#44=DIRECTION ( 'NONE',  ( 0.000000000000000000, 1.000000000000000000, 0.000000000000000000 ) ) ;
#47=DIRECTION ( 'NONE',  ( 0.000000000000000000, -1.000000000000000000, 0.000000000000000000 ) ) ;
#49=EDGE_CURVE ( 'NONE', #14974, #2230, #10873, .T. ) ;
#51=DIRECTION ( 'NONE',  ( 0.8660254037844385966, 0.000000000000000000, 0.5000000000000000000 ) ) ;
#54=FACE_OUTER_BOUND ( 'NONE', #13817, .T. ) ;
#55=( LENGTH_UNIT ( ) NAMED_UNIT ( * ) SI_UNIT ( $, .METRE. ) );
#56=ORIENTED_EDGE ( 'NONE', *, *, #1265, .F. ) ;
#58=ORIENTED_EDGE ( 'NONE', *, *, #10893, .T. ) ;
#59=EDGE_CURVE ( 'NONE', #1289, #10200, #14345, .T. ) ;
#61=ORIENTED_EDGE ( 'NONE', *, *, #7248, .T. ) ;
#62=DIRECTION ( 'NONE',  ( 0.000000000000000000, -1.000000000000000000, 0.000000000000000000 ) ) ;
#63=DIRECTION ( 'NONE',  ( 0.000000000000000000, 0.000000000000000000, 1.000000000000000000 ) ) ;
#64=DIRECTION ( 'NONE',  ( 0.000000000000000000, 0.000000000000000000, -1.000000000000000000 ) ) ;
#72=DIMENSIONAL_EXPONENTS ( 1.000000000000000000, 0.000000000000000000, 0.000000000000000000, 0.000000000000000000, 0.000000000000000000, 0.000000000000000000, 0.000000000000000000 ) ;
#73=EDGE_LOOP ( 'NONE', ( #10022, #9333, #9772, #13573 ) ) ;
#74=ORIENTED_EDGE ( 'NONE', *, *, #4819, .F. ) ;
#75=ADVANCED_FACE ( 'NONE', ( #9803 ), #2445, .T. ) ;
#77=EDGE_CURVE ( 'NONE', #14789, #11669, #7447, .T. ) ;
#79=EDGE_CURVE ( 'NONE', #10775, #13144, #8127, .T. ) ;
#83=DIRECTION ( 'NONE',  ( 0.000000000000000000, 0.000000000000000000, -1.000000000000000000 ) ) ;
#86=ORIENTED_EDGE ( 'NONE', *, *, #142, .F. ) ;
#93=CIRCLE ( 'NONE', #8836, 0.007874015748031499423 ) ;
#99=DIRECTION ( 'NONE',  ( 0.000000000000000000, 0.000000000000000000, -1.000000000000000000 ) ) ;
#102=DIRECTION ( 'NONE',  ( -0.000000000000000000, 1.000000000000000000, -0.000000000000000000 ) ) ;
#104=DIRECTION ( 'NONE',  ( 1.000000000000000000, 0.000000000000000000, 0.000000000000000000 ) ) ;
#105=VERTEX_POINT ( 'NONE', #13088 ) ;
#106=FACE_OUTER_BOUND ( 'NONE', #1446, .T. ) ;
#107=AXIS2_PLACEMENT_3D ( 'NONE', #2683, #12082, #8785 ) ;
#110=ORIENTED_EDGE ( 'NONE', *, *, #11508, .F. ) ;
#111=ORIENTED_EDGE ( 'NONE', *, *, #454, .T. ) ;
#114=AXIS2_PLACEMENT_3D ( 'NONE', #1059, #5812, #13822 ) ;
#117=AXIS2_PLACEMENT_3D ( 'NONE', #2165, #3498, #5743 ) ;
#118=LINE ( 'NONE', #11058, #11152 ) ;
#119=AXIS2_PLACEMENT_3D ( 'NONE', #8885, #662, #8010 ) ;
#120=ADVANCED_FACE ( 'NONE', ( #12541 ), #3452, .F. ) ;
#126=CARTESIAN_POINT ( 'NONE',  ( -0.5871416322685659717, -0.09448818897637796532, 0.1571437749735178357 ) ) ;
#130=DIRECTION ( 'NONE',  ( 0.000000000000000000, 1.000000000000000000, -0.000000000000000000 ) ) ;
#131=AXIS2_PLACEMENT_3D ( 'NONE', #4870, #14445, #104 ) ;
#132=CIRCLE ( 'NONE', #8366, 0.003937007874015749712 ) ;
#133=CIRCLE ( 'NONE', #9633, 0.003937007874015754916 ) ;
#136=FACE_OUTER_BOUND ( 'NONE', #9209, .T. ) ;
#137=AXIS2_PLACEMENT_3D ( 'NONE', #722, #10110, #6416 ) ;
#138=ORIENTED_EDGE ( 'NONE', *, *, #12039, .T. ) ;
#140=ORIENTED_EDGE ( 'NONE', *, *, #3284, .F. ) ;
#141=EDGE_LOOP ( 'NONE', ( #2502, #1091, #11460, #13655 ) ) ;
#142=EDGE_CURVE ( 'NONE', #9415, #10116, #8053, .T. ) ;
#143=CIRCLE ( 'NONE', #6372, 0.03937007874015753528 ) ;
#145=EDGE_CURVE ( 'NONE', #9212, #10209, #5623, .T. ) ;
#148=DIRECTION ( 'NONE',  ( -0.8660254037844398178, 0.000000000000000000, 0.4999999999999979461 ) ) ;
#149=CIRCLE ( 'NONE', #5881, 0.003937007874015758385 ) ;
#150=FACE_OUTER_BOUND ( 'NONE', #4683, .T. ) ;
#152=PLANE ( 'NONE',  #3906 ) ;
#153=DIRECTION ( 'NONE',  ( -0.5000000000000004441, 2.369676336725577685E-14, -0.8660254037844384856 ) ) ;
#154=DIRECTION ( 'NONE',  ( -1.000000000000000000, 0.000000000000000000, -3.614007241618347785E-16 ) ) ;
#155=DIRECTION ( 'NONE',  ( 0.4999999999999922284, -0.000000000000000000, -0.8660254037844430375 ) ) ;
#156=CARTESIAN_POINT ( 'NONE',  ( -0.2652685895081163259, -0.4881889763779528324, 0.03495519865516327068 ) ) ;
#159=AXIS2_PLACEMENT_3D ( 'NONE', #14084, #3448, #5697 ) ;
#162=ORIENTED_EDGE ( 'NONE', *, *, #7094, .T. ) ;
#164=ORIENTED_EDGE ( 'NONE', *, *, #13819, .T. ) ;
#168=VECTOR ( 'NONE', #5103, 39.37007874015748854 ) ;
#169=CIRCLE ( 'NONE', #8876, 0.003937007874015758385 ) ;
#172=DIRECTION ( 'NONE',  ( 0.000000000000000000, -1.000000000000000000, -0.000000000000000000 ) ) ;
#182=EDGE_CURVE ( 'NONE', #9678, #2117, #12141, .T. ) ;
#187=FACE_OUTER_BOUND ( 'NONE', #7423, .T. ) ;
#188=CARTESIAN_POINT ( 'NONE',  ( 0.5452755905511544876, -0.4881889763779528324, 0.2375319020879054499 ) ) ;
#193=CARTESIAN_POINT ( 'NONE',  ( 0.03346456692913318126, -0.4881889763779528324, 0.05796233017454787556 ) ) ;
#194=ORIENTED_EDGE ( 'NONE', *, *, #797, .T. ) ;
#197=DIRECTION ( 'NONE',  ( 0.000000000000000000, -1.000000000000000000, 0.000000000000000000 ) ) ;
#198=VECTOR ( 'NONE', #7263, 39.37007874015748143 ) ;
#200=ADVANCED_FACE ( 'NONE', ( #4464 ), #1966, .T. ) ;
#202=VECTOR ( 'NONE', #642, 39.37007874015748143 ) ;
#206=AXIS2_PLACEMENT_3D ( 'NONE', #1865, #6710, #10088 ) ;
#215=DIRECTION ( 'NONE',  ( 0.000000000000000000, -1.000000000000000000, 0.000000000000000000 ) ) ;
#216=LINE ( 'NONE', #1526, #9372 ) ;
#222=ORIENTED_EDGE ( 'NONE', *, *, #8343, .F. ) ;
#223=ORIENTED_EDGE ( 'NONE', *, *, #11523, .F. ) ;
#224=EDGE_CURVE ( 'NONE', #6983, #315, #12637, .T. ) ;
#229=CARTESIAN_POINT ( 'NONE',  ( -0.2359202325321149429, -0.4881889763779528324, 0.06286251073437545966 ) ) ;
#234=CARTESIAN_POINT ( 'NONE',  ( 0.3944453183761336135, -0.2952755905511811330, 0.1549960689574419737 ) ) ;
#235=EDGE_CURVE ( 'NONE', #15025, #13855, #13405, .T. ) ;
#241=VERTEX_POINT ( 'NONE', #12928 ) ;
#242=DIRECTION ( 'NONE',  ( 0.5000000000000000000, 0.000000000000000000, 0.8660254037844388186 ) ) ;
#243=CARTESIAN_POINT ( 'NONE',  ( -0.1618514667033796040, -0.4881889763779528324, 0.2161887458866224576 ) ) ;
#246=CARTESIAN_POINT ( 'NONE',  ( -0.1552072824047652788, -0.09448818897637796532, -0.5870514566507987197 ) ) ;
#248=ORIENTED_EDGE ( 'NONE', *, *, #12383, .F. ) ;
#251=CARTESIAN_POINT ( 'NONE',  ( -0.1552072824047652788, -0.09448818897637796532, -0.5909884645248143498 ) ) ;
#253=VERTEX_POINT ( 'NONE', #4379 ) ;
#256=EDGE_CURVE ( 'NONE', #14594, #6947, #2197, .T. ) ;
#258=LINE ( 'NONE', #1429, #5603 ) ;
#262=DIRECTION ( 'NONE',  ( 2.168404344971007142E-16, 0.000000000000000000, -1.000000000000000000 ) ) ;
#266=CARTESIAN_POINT ( 'NONE',  ( -0.6241293575972478580, -0.2952755905511811330, -0.3215685141414794113 ) ) ;
#270=ORIENTED_EDGE ( 'NONE', *, *, #3011, .T. ) ;
#272=ORIENTED_EDGE ( 'NONE', *, *, #5675, .F. ) ;
#273=EDGE_LOOP ( 'NONE', ( #11844, #14325 ) ) ;
#274=CARTESIAN_POINT ( 'NONE',  ( -0.4803149606299220720, -0.1023622047244094474, 0.3500470136031578194 ) ) ;
#275=CARTESIAN_POINT ( 'NONE',  ( 0.5905511811023622659, -0.2952755905511811330, -0.3797276218561363992 ) ) ;
#277=EDGE_CURVE ( 'NONE', #7744, #713, #1617, .T. ) ;
#278=FACE_OUTER_BOUND ( 'NONE', #9293, .T. ) ;
#279=DIRECTION ( 'NONE',  ( -0.000000000000000000, 1.000000000000000000, 0.000000000000000000 ) ) ;
#281=DIRECTION ( 'NONE',  ( 0.4999999999999966693, 0.000000000000000000, 0.8660254037844405950 ) ) ;
#282=CARTESIAN_POINT ( 'NONE',  ( -0.1552072824047652788, -0.003937007874015747977, -0.5870514566507987197 ) ) ;
#284=DIRECTION ( 'NONE',  ( -0.4999999999999873990, 0.000000000000000000, 0.8660254037844459241 ) ) ;
#285=CARTESIAN_POINT ( 'NONE',  ( 0.1552072824047652233, -0.09448818897637796532, -0.5870514566507987197 ) ) ;
#293=DIRECTION ( 'NONE',  ( 0.5000000000000035527, 0.000000000000000000, -0.8660254037844365982 ) ) ;
#297=CARTESIAN_POINT ( 'NONE',  ( -0.4296613173079366632, 0.000000000000000000, 0.4299076816772784415 ) ) ;
#298=DIRECTION ( 'NONE',  ( 0.000000000000000000, 0.000000000000000000, 1.000000000000000000 ) ) ;
#299=EDGE_LOOP ( 'NONE', ( #6916, #11845, #7301, #272 ) ) ;
#301=ORIENTED_EDGE ( 'NONE', *, *, #11469, .F. ) ;
#302=ORIENTED_EDGE ( 'NONE', *, *, #9316, .F. ) ;
#305=DIRECTION ( 'NONE',  ( -3.942553354492736135E-16, 0.000000000000000000, 1.000000000000000000 ) ) ;
#307=FACE_OUTER_BOUND ( 'NONE', #9651, .T. ) ;
#308=EDGE_CURVE ( 'NONE', #556, #11529, #4863, .T. ) ;
#311=CARTESIAN_POINT ( 'NONE',  ( -0.5871416322685660827, 0.000000000000000000, 0.1610807828475335768 ) ) ;
#313=DIRECTION ( 'NONE',  ( 0.000000000000000000, 0.000000000000000000, 1.000000000000000000 ) ) ;
#315=VERTEX_POINT ( 'NONE', #4702 ) ;
#320=ORIENTED_EDGE ( 'NONE', *, *, #11535, .F. ) ;
#321=EDGE_LOOP ( 'NONE', ( #11036, #7032, #11996, #10788 ) ) ;
#322=ORIENTED_EDGE ( 'NONE', *, *, #8280, .F. ) ;
#324=ADVANCED_FACE ( 'NONE', ( #5851 ), #15138, .T. ) ;
#329=DIRECTION ( 'NONE',  ( 0.5000000000000035527, 0.000000000000000000, -0.8660254037844365982 ) ) ;
#332=DIRECTION ( 'NONE',  ( 1.971276677246368068E-16, 0.000000000000000000, -1.000000000000000000 ) ) ;
#334=DIRECTION ( 'NONE',  ( 0.4999999999999995004, 0.000000000000000000, 0.8660254037844390407 ) ) ;
#335=CARTESIAN_POINT ( 'NONE',  ( -0.3635801767928720230, -0.2952755905511811330, 0.2871962198427739366 ) ) ;
#336=AXIS2_PLACEMENT_3D ( 'NONE', #14534, #4099, #14697 ) ;
#339=ORIENTED_EDGE ( 'NONE', *, *, #9830, .T. ) ;
#340=DIRECTION ( 'NONE',  ( -0.8660254037844387076, 0.000000000000000000, 0.4999999999999998890 ) ) ;
#341=CARTESIAN_POINT ( 'NONE',  ( 0.5649606299213149052, -0.1023622047244094474, 0.2034364137499825587 ) ) ;
#342=VECTOR ( 'NONE', #8477, 39.37007874015748143 ) ;
#347=AXIS2_PLACEMENT_3D ( 'NONE', #14818, #13324, #2592 ) ;
#351=DIRECTION ( 'NONE',  ( -0.8660254037844383745, 0.000000000000000000, -0.5000000000000003331 ) ) ;
#353=DIRECTION ( 'NONE',  ( 0.8660254037844383745, 0.000000000000000000, 0.5000000000000005551 ) ) ;
#356=VECTOR ( 'NONE', #8199, 39.37007874015748143 ) ;
#358=AXIS2_PLACEMENT_3D ( 'NONE', #8652, #13430, #2699 ) ;
#359=EDGE_CURVE ( 'NONE', #6020, #2868, #2424, .T. ) ;
#367=CIRCLE ( 'NONE', #3357, 0.04330708661417329020 ) ;
#370=LINE ( 'NONE', #13761, #2577 ) ;
#371=CARTESIAN_POINT ( 'NONE',  ( 0.5084014747882494856, -0.09842519685039370636, 0.2935257283254013583 ) ) ;
#372=CIRCLE ( 'NONE', #8882, 0.003937007874015724558 ) ;
#379=ORIENTED_EDGE ( 'NONE', *, *, #10742, .T. ) ;
#382=AXIS2_PLACEMENT_3D ( 'NONE', #11155, #12498, #4323 ) ;
#386=AXIS2_PLACEMENT_3D ( 'NONE', #5527, #841, #9620 ) ;
#391=DIRECTION ( 'NONE',  ( 0.000000000000000000, 0.000000000000000000, -1.000000000000000000 ) ) ;
#392=DIRECTION ( 'NONE',  ( 0.000000000000000000, -1.000000000000000000, 0.000000000000000000 ) ) ;
#397=AXIS2_PLACEMENT_3D ( 'NONE', #14731, #8601, #305 ) ;
#398=ORIENTED_EDGE ( 'NONE', *, *, #9450, .T. ) ;
#400=AXIS2_PLACEMENT_3D ( 'NONE', #2168, #7172, #1065 ) ;
#402=ORIENTED_EDGE ( 'NONE', *, *, #6447, .F. ) ;
#403=ORIENTED_EDGE ( 'NONE', *, *, #13234, .T. ) ;
#406=ORIENTED_EDGE ( 'NONE', *, *, #14437, .T. ) ;
#409=EDGE_CURVE ( 'NONE', #5520, #2117, #13395, .T. ) ;
#410=AXIS2_PLACEMENT_3D ( 'NONE', #3499, #8109, #15408 ) ;
#412=FACE_OUTER_BOUND ( 'NONE', #5822, .T. ) ;
#413=SPHERICAL_SURFACE ( 'NONE', #9205, 0.003937007874015747977 ) ;
#414=DIRECTION ( 'NONE',  ( -0.8660254037844309360, 0.000000000000000000, 0.5000000000000134337 ) ) ;
#418=DIRECTION ( 'NONE',  ( -3.614007241618347785E-16, 0.000000000000000000, 1.000000000000000000 ) ) ;
#420=DIRECTION ( 'NONE',  ( 0.4999999999999922284, -0.000000000000000000, -0.8660254037844430375 ) ) ;
#423=AXIS2_PLACEMENT_3D ( 'NONE', #12417, #10053, #6511 ) ;
#425=ORIENTED_EDGE ( 'NONE', *, *, #13589, .F. ) ;
#427=ORIENTED_EDGE ( 'NONE', *, *, #11037, .F. ) ;
#431=CIRCLE ( 'NONE', #7921, 0.003937007874015721089 ) ;
#435=CARTESIAN_POINT ( 'NONE',  ( -0.4803149606299220720, -0.4881889763779528324, 0.3500470136031578194 ) ) ;
#436=AXIS2_PLACEMENT_3D ( 'NONE', #8469, #13242, #2503 ) ;
#437=DIRECTION ( 'NONE',  ( 0.000000000000000000, 0.000000000000000000, -1.000000000000000000 ) ) ;
#438=CARTESIAN_POINT ( 'NONE',  ( -0.1574803149606299191, -0.09448818897637796532, -0.5909884645248143498 ) ) ;
#439=CARTESIAN_POINT ( 'NONE',  ( -0.1023622047242991467, -0.4921259842519685179, -0.5909884645248154600 ) ) ;
#441=CARTESIAN_POINT ( 'NONE',  ( 0.3780663654712341781, -0.2952755905511811330, 0.1046250900831900282 ) ) ;
#442=ADVANCED_FACE ( 'NONE', ( #5054 ), #14795, .T. ) ;
#445=CIRCLE ( 'NONE', #8476, 0.003937007874015749712 ) ;
#446=AXIS2_PLACEMENT_3D ( 'NONE', #1079, #4450, #2315 ) ;
#448=ORIENTED_EDGE ( 'NONE', *, *, #6594, .T. ) ;
#451=AXIS2_PLACEMENT_3D ( 'NONE', #1495, #12462, #1728 ) ;
#454=EDGE_CURVE ( 'NONE', #4728, #13507, #2390, .T. ) ;
#455=VECTOR ( 'NONE', #1209, 39.37007874015748143 ) ;
#459=CARTESIAN_POINT ( 'NONE',  ( 0.1062992125984796032, -0.4921259842519685179, -0.2482618547481154347 ) ) ;
#460=ADVANCED_FACE ( 'NONE', ( #13701 ), #4132, .T. ) ;
#464=CARTESIAN_POINT ( 'NONE',  ( 0.09842519685044814892, -0.2952755905511811330, -0.4190977005962941426 ) ) ;
#469=EDGE_LOOP ( 'NONE', ( #58, #3143, #2480, #4682 ) ) ;
#471=ORIENTED_EDGE ( 'NONE', *, *, #7915, .F. ) ;
#474=CIRCLE ( 'NONE', #9220, 0.003937007874015724558 ) ;
#484=EDGE_LOOP ( 'NONE', ( #14389, #4298, #8359 ) ) ;
#487=ORIENTED_EDGE ( 'NONE', *, *, #10319, .T. ) ;
#488=ORIENTED_EDGE ( 'NONE', *, *, #9455, .T. ) ;
#489=ORIENTED_EDGE ( 'NONE', *, *, #9553, .T. ) ;
#494=FACE_OUTER_BOUND ( 'NONE', #12042, .T. ) ;
#498=FACE_OUTER_BOUND ( 'NONE', #1145, .T. ) ;
#504=DIRECTION ( 'NONE',  ( -1.000000000000000000, 0.000000000000000000, 0.000000000000000000 ) ) ;
#506=DIRECTION ( 'NONE',  ( -0.8660254037844385966, 0.000000000000000000, -0.5000000000000001110 ) ) ;
#509=CARTESIAN_POINT ( 'NONE',  ( -0.06692913385815735250, -0.4881889763779528324, -0.5870514566507987197 ) ) ;
#510=DIRECTION ( 'NONE',  ( 0.4999999999999995004, 0.000000000000000000, 0.8660254037844390407 ) ) ;
#511=DIRECTION ( 'NONE',  ( 0.000000000000000000, 0.000000000000000000, -1.000000000000000000 ) ) ;
#512=LINE ( 'NONE', #11478, #1386 ) ;
#514=DIRECTION ( 'NONE',  ( 1.000000000000000000, 0.000000000000000000, 3.075191616504340279E-15 ) ) ;
#515=ORIENTED_EDGE ( 'NONE', *, *, #13205, .T. ) ;
#517=VERTEX_POINT ( 'NONE', #10766 ) ;
#518=ORIENTED_EDGE ( 'NONE', *, *, #11825, .T. ) ;
#527=CYLINDRICAL_SURFACE ( 'NONE', #3584, 0.003937007874015750579 ) ;
#530=EDGE_LOOP ( 'NONE', ( #9699, #86, #11976, #15040 ) ) ;
#531=ORIENTED_EDGE ( 'NONE', *, *, #11516, .F. ) ;
#534=ORIENTED_EDGE ( 'NONE', *, *, #10419, .T. ) ;
#537=CARTESIAN_POINT ( 'NONE',  ( -0.5871416322685659717, -0.09448818897637796532, 0.1571437749735178357 ) ) ;
#540=CYLINDRICAL_SURFACE ( 'NONE', #4641, 0.003937007874015724558 ) ;
#548=ORIENTED_EDGE ( 'NONE', *, *, #7094, .F. ) ;
#549=ORIENTED_EDGE ( 'NONE', *, *, #1610, .T. ) ;
#550=EDGE_CURVE ( 'NONE', #7731, #9204, #1632, .T. ) ;
#553=FACE_OUTER_BOUND ( 'NONE', #4160, .T. ) ;
#554=CARTESIAN_POINT ( 'NONE',  ( 0.2364476915724980366, -0.4921259842519685179, 0.06377609659104091500 ) ) ;
#556=VERTEX_POINT ( 'NONE', #12972 ) ;
#559=DIRECTION ( 'NONE',  ( 0.000000000000000000, 0.000000000000000000, 1.000000000000000000 ) ) ;
#572=DIRECTION ( 'NONE',  ( -0.000000000000000000, 1.000000000000000000, -0.000000000000000000 ) ) ;
#573=DIRECTION ( 'NONE',  ( 0.000000000000000000, 1.000000000000000000, -2.602085213965215375E-14 ) ) ;
#576=CARTESIAN_POINT ( 'NONE',  ( -0.1629063847838169987, -0.4881889763779528324, 0.2122517380126066888 ) ) ;
#577=DIRECTION ( 'NONE',  ( 0.8660254037844388186, -0.000000000000000000, -0.4999999999999995559 ) ) ;
#580=EDGE_CURVE ( 'NONE', #7744, #8756, #1058, .T. ) ;
#581=CARTESIAN_POINT ( 'NONE',  ( -0.1023622047242991467, -0.4881889763779528324, -0.5909884645248154600 ) ) ;
#583=ORIENTED_EDGE ( 'NONE', *, *, #550, .F. ) ;
#585=ADVANCED_FACE ( 'NONE', ( #5738 ), #15401, .T. ) ;
#587=CIRCLE ( 'NONE', #2578, 0.003937007874015724558 ) ;
#588=AXIS2_PLACEMENT_3D ( 'NONE', #13779, #10019, #3044 ) ;
#589=ADVANCED_FACE ( 'NONE', ( #15242 ), #990, .T. ) ;
#590=CARTESIAN_POINT ( 'NONE',  ( 0.1724006475077544120, -0.4921259842519685179, 0.1768186671464649640 ) ) ;
#599=CARTESIAN_POINT ( 'NONE',  ( -0.3117681530218310848, -0.2952755905511811330, 0.2981971199768678193 ) ) ;
#605=ORIENTED_EDGE ( 'NONE', *, *, #7108, .T. ) ;
#606=ADVANCED_FACE ( 'NONE', ( #11874 ), #11962, .T. ) ;
#609=EDGE_LOOP ( 'NONE', ( #11562, #301, #9130, #13793 ) ) ;
#610=ORIENTED_EDGE ( 'NONE', *, *, #10612, .T. ) ;
#612=VECTOR ( 'NONE', #5962, 39.37007874015748143 ) ;
#614=EDGE_CURVE ( 'NONE', #4318, #2230, #12153, .T. ) ;
#616=AXIS2_PLACEMENT_3D ( 'NONE', #15267, #1085, #10414 ) ;
#618=CIRCLE ( 'NONE', #13114, 0.003937007874015724558 ) ;
#621=DIRECTION ( 'NONE',  ( -4.336808689942015843E-14, 0.000000000000000000, 1.000000000000000000 ) ) ;
#625=FACE_OUTER_BOUND ( 'NONE', #8536, .T. ) ;
#626=DIRECTION ( 'NONE',  ( 0.5000000000000035527, 0.000000000000000000, -0.8660254037844365982 ) ) ;
#627=AXIS2_PLACEMENT_3D ( 'NONE', #193, #13095, #1435 ) ;
#629=CIRCLE ( 'NONE', #15392, 0.04330708661417331101 ) ;
#632=ORIENTED_EDGE ( 'NONE', *, *, #4758, .T. ) ;
#633=VECTOR ( 'NONE', #6325, 39.37007874015748143 ) ;
#635=ORIENTED_EDGE ( 'NONE', *, *, #5996, .T. ) ;
#637=AXIS2_PLACEMENT_3D ( 'NONE', #3207, #12688, #7976 ) ;
#640=DIRECTION ( 'NONE',  ( -0.8660254037844383745, 0.000000000000000000, -0.5000000000000004441 ) ) ;
#642=DIRECTION ( 'NONE',  ( -0.4999999999999979461, 0.000000000000000000, -0.8660254037844398178 ) ) ;
#645=DIRECTION ( 'NONE',  ( -0.5000000000000145439, -0.000000000000000000, -0.8660254037844303809 ) ) ;
#647=CARTESIAN_POINT ( 'NONE',  ( -0.1057717535580962598, -0.1023622047244094474, -0.2491754406047808068 ) ) ;
#648=ADVANCED_FACE ( 'NONE', ( #12030, #4884 ), #9908, .F. ) ;
#650=DIRECTION ( 'NONE',  ( -1.000000000000000000, -0.000000000000000000, -3.476578583725179813E-16 ) ) ;
#652=CARTESIAN_POINT ( 'NONE',  ( 0.000000000000000000, -0.4921259842519685179, 0.000000000000000000 ) ) ;
#658=AXIS2_PLACEMENT_3D ( 'NONE', #5672, #10617, #7081 ) ;
#659=CARTESIAN_POINT ( 'NONE',  ( -0.2681506793016945611, -0.09842519685039370636, 0.03207310886158502850 ) ) ;
#662=DIRECTION ( 'NONE',  ( -0.000000000000000000, 1.000000000000000000, -0.000000000000000000 ) ) ;
#668=ORIENTED_EDGE ( 'NONE', *, *, #8195, .F. ) ;
#669=DIRECTION ( 'NONE',  ( -1.000000000000000000, 0.000000000000000000, 0.000000000000000000 ) ) ;
#671=DIRECTION ( 'NONE',  ( -0.8660254037844405950, 0.000000000000000000, -0.4999999999999967248 ) ) ;
#674=CARTESIAN_POINT ( 'NONE',  ( -0.1724006475077544398, -0.4881889763779528324, 0.1728816592724491952 ) ) ;
#675=VERTEX_POINT ( 'NONE', #14596 ) ;
#678=AXIS2_PLACEMENT_3D ( 'NONE', #14612, #7540, #13279 ) ;
#679=ORIENTED_EDGE ( 'NONE', *, *, #14572, .F. ) ;
#683=DIRECTION ( 'NONE',  ( 0.000000000000000000, 0.000000000000000000, 1.000000000000000000 ) ) ;
#686=DIRECTION ( 'NONE',  ( 0.000000000000000000, 1.000000000000000000, -0.000000000000000000 ) ) ;
#687=CARTESIAN_POINT ( 'NONE',  ( -0.1872249459500325841, -0.09842519685039370636, -0.1080943729432645994 ) ) ;
#691=DIRECTION ( 'NONE',  ( 0.000000000000000000, 0.000000000000000000, -1.000000000000000000 ) ) ;
#701=CIRCLE ( 'NONE', #9210, 0.003937007874015758385 ) ;
#705=DIRECTION ( 'NONE',  ( 2.168404344971012655E-14, 0.000000000000000000, 1.000000000000000000 ) ) ;
#708=EDGE_CURVE ( 'NONE', #13984, #15156, #5125, .T. ) ;
#709=ORIENTED_EDGE ( 'NONE', *, *, #8054, .F. ) ;
#710=FACE_OUTER_BOUND ( 'NONE', #1482, .T. ) ;
#711=DIRECTION ( 'NONE',  ( 0.4999999999999991118, -0.000000000000000000, -0.8660254037844390407 ) ) ;
#712=AXIS2_PLACEMENT_3D ( 'NONE', #4868, #15319, #10812 ) ;
#713=VERTEX_POINT ( 'NONE', #14689 ) ;
#714=EDGE_CURVE ( 'NONE', #4318, #14414, #118, .T. ) ;
#718=DIRECTION ( 'NONE',  ( 0.000000000000000000, -1.000000000000000000, 0.000000000000000000 ) ) ;
#722=CARTESIAN_POINT ( 'NONE',  ( -0.09842519685028335019, -0.2952755905511811330, -0.4190977005962941981 ) ) ;
#725=ADVANCED_FACE ( 'NONE', ( #10826 ), #7386, .F. ) ;
#726=ORIENTED_EDGE ( 'NONE', *, *, #5696, .T. ) ;
#729=DIRECTION ( 'NONE',  ( 1.000000000000000000, 1.734723475976817507E-14, 0.000000000000000000 ) ) ;
#734=EDGE_LOOP ( 'NONE', ( #10955, #1406, #10244, #12393 ) ) ;
#737=DIRECTION ( 'NONE',  ( 0.5000000000000001110, 0.000000000000000000, -0.8660254037844385966 ) ) ;
#738=CYLINDRICAL_SURFACE ( 'NONE', #6887, 0.003937007874015758385 ) ;
#740=CARTESIAN_POINT ( 'NONE',  ( -0.4788739157331333707, -0.1023622047244094474, 0.3446689608323532661 ) ) ;
#743=ORIENTED_EDGE ( 'NONE', *, *, #7868, .F. ) ;
#746=CARTESIAN_POINT ( 'NONE',  ( 0.5860051159906326523, -0.09448818897637796532, 0.1591122789105293700 ) ) ;
#747=EDGE_CURVE ( 'NONE', #3536, #9448, #3643, .T. ) ;
#750=EDGE_CURVE ( 'NONE', #1302, #7482, #12094, .T. ) ;
#753=DIRECTION ( 'NONE',  ( 0.000000000000000000, 0.000000000000000000, -1.000000000000000000 ) ) ;
#756=CARTESIAN_POINT ( 'NONE',  ( 0.4591888763630541104, -0.4881889763779528324, 0.3787644491703230365 ) ) ;
#762=ORIENTED_EDGE ( 'NONE', *, *, #15301, .F. ) ;
#765=DIRECTION ( 'NONE',  ( -0.000000000000000000, 1.000000000000000000, -0.000000000000000000 ) ) ;
#767=CARTESIAN_POINT ( 'NONE',  ( 0.2353927734920605308, -0.1023622047244094474, 0.06771310446505662828 ) ) ;
#771=EDGE_LOOP ( 'NONE', ( #6516, #12506, #1056, #668 ) ) ;
#774=CARTESIAN_POINT ( 'NONE',  ( -0.06692913385815757454, -0.4881889763779528324, -2.418823744386252084E-17 ) ) ;
#777=VERTEX_POINT ( 'NONE', #9823 ) ;
#778=EDGE_CURVE ( 'NONE', #7384, #11994, #8647, .T. ) ;
#785=DIRECTION ( 'NONE',  ( -0.000000000000000000, 1.000000000000000000, -0.000000000000000000 ) ) ;
#786=CARTESIAN_POINT ( 'NONE',  ( 0.1586168312385622392, -0.09842519685039370636, -0.5890199605878065903 ) ) ;
#787=ORIENTED_EDGE ( 'NONE', *, *, #7677, .F. ) ;
#788=DIRECTION ( 'NONE',  ( -0.5000000000000004441, -0.000000000000000000, -0.8660254037844384856 ) ) ;
#790=FACE_OUTER_BOUND ( 'NONE', #8805, .T. ) ;
#791=LINE ( 'NONE', #6898, #14091 ) ;
#792=ORIENTED_EDGE ( 'NONE', *, *, #77, .F. ) ;
#793=CYLINDRICAL_SURFACE ( 'NONE', #11958, 0.003937007874015750579 ) ;
#794=ORIENTED_EDGE ( 'NONE', *, *, #9584, .F. ) ;
#797=EDGE_CURVE ( 'NONE', #9540, #1289, #4399, .T. ) ;
#799=DIRECTION ( 'NONE',  ( 0.000000000000000000, -1.000000000000000000, -0.000000000000000000 ) ) ;
#801=ADVANCED_FACE ( 'NONE', ( #8881 ), #738, .T. ) ;
#805=DIRECTION ( 'NONE',  ( -0.5000000000000028866, -0.000000000000000000, 0.8660254037844371533 ) ) ;
#806=DIRECTION ( 'NONE',  ( 0.4999999999999979461, 0.000000000000000000, 0.8660254037844398178 ) ) ;
#807=ORIENTED_EDGE ( 'NONE', *, *, #14959, .T. ) ;
#808=CYLINDRICAL_SURFACE ( 'NONE', #14177, 0.03937007874015754916 ) ;
#809=DIRECTION ( 'NONE',  ( 0.000000000000000000, -1.000000000000000000, -0.000000000000000000 ) ) ;
#810=DIRECTION ( 'NONE',  ( 0.8660254037844398178, -0.000000000000000000, -0.4999999999999979461 ) ) ;
#816=LINE ( 'NONE', #8025, #356 ) ;
#818=ADVANCED_FACE ( 'NONE', ( #1749 ), #895, .T. ) ;
#820=DIRECTION ( 'NONE',  ( -0.4999999999999996114, -0.000000000000000000, -0.8660254037844389297 ) ) ;
#824=PLANE ( 'NONE',  #13907 ) ;
#825=VECTOR ( 'NONE', #4213, 39.37007874015748143 ) ;
#826=AXIS2_PLACEMENT_3D ( 'NONE', #6958, #14170, #7030 ) ;
#829=ORIENTED_EDGE ( 'NONE', *, *, #9644, .F. ) ;
#833=CARTESIAN_POINT ( 'NONE',  ( -0.1062992125983150127, -0.1023622047244094474, -0.2482618547482104143 ) ) ;
#835=VECTOR ( 'NONE', #4975, 39.37007874015748143 ) ;
#837=AXIS2_PLACEMENT_3D ( 'NONE', #6207, #2532, #7307 ) ;
#840=DIRECTION ( 'NONE',  ( 0.000000000000000000, 0.000000000000000000, -1.000000000000000000 ) ) ;
#841=DIRECTION ( 'NONE',  ( 0.8660254037844397068, 0.000000000000000000, -0.4999999999999981681 ) ) ;
#842=CIRCLE ( 'NONE', #2095, 0.003937007874015758385 ) ;
#843=DIRECTION ( 'NONE',  ( 1.000000000000000000, 0.000000000000000000, 0.000000000000000000 ) ) ;
#844=DIRECTION ( 'NONE',  ( -0.000000000000000000, -0.000000000000000000, -1.000000000000000000 ) ) ;
#845=ORIENTED_EDGE ( 'NONE', *, *, #9115, .F. ) ;
#846=DIRECTION ( 'NONE',  ( -0.000000000000000000, 1.000000000000000000, 0.000000000000000000 ) ) ;
#848=DIRECTION ( 'NONE',  ( -0.8660254037844347108, 0.000000000000000000, -0.5000000000000069944 ) ) ;
#849=DIRECTION ( 'NONE',  ( -0.000000000000000000, -0.000000000000000000, 1.000000000000000000 ) ) ;
#850=ORIENTED_EDGE ( 'NONE', *, *, #11015, .F. ) ;
#852=AXIS2_PLACEMENT_3D ( 'NONE', #6869, #11661, #10090 ) ;
#853=AXIS2_PLACEMENT_3D ( 'NONE', #1926, #10536, #6764 ) ;
#857=CIRCLE ( 'NONE', #5594, 0.003937007874015754916 ) ;
#858=DIRECTION ( 'NONE',  ( 0.000000000000000000, 0.000000000000000000, -1.000000000000000000 ) ) ;
#860=CARTESIAN_POINT ( 'NONE',  ( 0.1062992125984796032, -0.4921259842519685179, -0.2482618547481154347 ) ) ;
#865=AXIS2_PLACEMENT_3D ( 'NONE', #7504, #5524, #3341 ) ;
#867=DIRECTION ( 'NONE',  ( 0.000000000000000000, -0.000000000000000000, -1.000000000000000000 ) ) ;
#868=ORIENTED_EDGE ( 'NONE', *, *, #1236, .F. ) ;
#870=AXIS2_PLACEMENT_3D ( 'NONE', #10796, #14421, #2198 ) ;
#873=ADVANCED_FACE ( 'NONE', ( #5181 ), #10899, .T. ) ;
#875=ORIENTED_EDGE ( 'NONE', *, *, #9352, .T. ) ;
#878=EDGE_CURVE ( 'NONE', #7659, #6985, #13741, .T. ) ;
#885=CARTESIAN_POINT ( 'NONE',  ( 0.05905511811029064834, -0.1023622047244094474, -0.5870514566507987197 ) ) ;
#887=CARTESIAN_POINT ( 'NONE',  ( 0.4296613173079339432, -0.09448818897637796532, 0.4299076816772811060 ) ) ;
#890=FACE_OUTER_BOUND ( 'NONE', #9539, .T. ) ;
#895=TOROIDAL_SURFACE ( 'NONE', #4145, 0.04330708661417328326, 0.003937007874015747977 ) ;
#897=VERTEX_POINT ( 'NONE', #11228 ) ;
#899=ORIENTED_EDGE ( 'NONE', *, *, #2261, .F. ) ;
#902=FACE_OUTER_BOUND ( 'NONE', #2102, .T. ) ;
#905=ORIENTED_EDGE ( 'NONE', *, *, #7727, .F. ) ;
#907=( GEOMETRIC_REPRESENTATION_CONTEXT ( 3 ) GLOBAL_UNCERTAINTY_ASSIGNED_CONTEXT ( ( #5158 ) ) GLOBAL_UNIT_ASSIGNED_CONTEXT ( ( #9292, #7018, #5913 ) ) REPRESENTATION_CONTEXT ( 'NONE', 'WORKASPACE' ) );
#908=AXIS2_PLACEMENT_3D ( 'NONE', #8038, #4517, #13842 ) ;
#910=FACE_OUTER_BOUND ( 'NONE', #11631, .T. ) ;
#913=CIRCLE ( 'NONE', #12421, 0.003937007874015746242 ) ;
#916=ADVANCED_FACE ( 'NONE', ( #13090 ), #10678, .T. ) ;
#920=DIRECTION ( 'NONE',  ( 0.000000000000000000, -0.000000000000000000, -1.000000000000000000 ) ) ;
#923=EDGE_CURVE ( 'NONE', #8145, #9678, #5626, .T. ) ;
#927=ORIENTED_EDGE ( 'NONE', *, *, #4510, .F. ) ;
#929=ADVANCED_FACE ( 'NONE', ( #3475 ), #12950, .T. ) ;
#934=DIRECTION ( 'NONE',  ( -1.000000000000000000, 0.000000000000000000, 0.000000000000000000 ) ) ;
#935=CARTESIAN_POINT ( 'NONE',  ( -0.1574803149606299191, -0.09842519685039370636, -0.5909884645248143498 ) ) ;
#943=ORIENTED_EDGE ( 'NONE', *, *, #10484, .T. ) ;
#944=EDGE_CURVE ( 'NONE', #7482, #14862, #6374, .T. ) ;
#948=EDGE_CURVE ( 'NONE', #7254, #2901, #10655, .T. ) ;
#949=DIRECTION ( 'NONE',  ( 0.000000000000000000, 0.000000000000000000, -1.000000000000000000 ) ) ;
#952=DIRECTION ( 'NONE',  ( 0.000000000000000000, -1.000000000000000000, 0.000000000000000000 ) ) ;
#954=CARTESIAN_POINT ( 'NONE',  ( -0.1763376553817701531, -0.09842519685039370636, 0.1699995694788710154 ) ) ;
#955=LINE ( 'NONE', #4538, #13612 ) ;
#958=ORIENTED_EDGE ( 'NONE', *, *, #7721, .T. ) ;
#960=FACE_OUTER_BOUND ( 'NONE', #1382, .T. ) ;
#961=AXIS2_PLACEMENT_3D ( 'NONE', #4474, #2274, #12778 ) ;
#963=CYLINDRICAL_SURFACE ( 'NONE', #11859, 0.003937007874015743640 ) ;
#964=ORIENTED_EDGE ( 'NONE', *, *, #4575, .F. ) ;
#965=DIRECTION ( 'NONE',  ( 1.734723475976807094E-14, -1.000000000000000000, 0.000000000000000000 ) ) ;
#967=ORIENTED_EDGE ( 'NONE', *, *, #948, .F. ) ;
#968=AXIS2_PLACEMENT_3D ( 'NONE', #11211, #6190, #9746 ) ;
#973=CARTESIAN_POINT ( 'NONE',  ( -0.1552072824047652788, -0.09842519685039370636, -0.5909884645248143498 ) ) ;
#974=DIRECTION ( 'NONE',  ( -1.000000000000000000, 0.000000000000000000, 0.000000000000000000 ) ) ;
#976=CARTESIAN_POINT ( 'NONE',  ( -0.5905511811023629321, -0.09842519685039370636, 0.1591122789105256785 ) ) ;
#977=ORIENTED_EDGE ( 'NONE', *, *, #15068, .F. ) ;
#981=DIRECTION ( 'NONE',  ( 0.000000000000000000, 0.000000000000000000, -1.000000000000000000 ) ) ;
#984=VERTEX_POINT ( 'NONE', #2046 ) ;
#985=DIRECTION ( 'NONE',  ( 0.000000000000000000, 0.000000000000000000, 1.000000000000000000 ) ) ;
#986=VERTEX_POINT ( 'NONE', #6991 ) ;
#987=ORIENTED_EDGE ( 'NONE', *, *, #4982, .T. ) ;
#988=EDGE_CURVE ( 'NONE', #8756, #6899, #3902, .T. ) ;
#989=ORIENTED_EDGE ( 'NONE', *, *, #10688, .F. ) ;
#990=SPHERICAL_SURFACE ( 'NONE', #13637, 0.003937007874015747977 ) ;
#991=EDGE_CURVE ( 'NONE', #6292, #13356, #14275, .T. ) ;
#992=DIRECTION ( 'NONE',  ( 0.000000000000000000, 0.000000000000000000, -1.000000000000000000 ) ) ;
#995=DIRECTION ( 'NONE',  ( 0.8660254037844385966, 0.000000000000000000, 0.5000000000000001110 ) ) ;
#997=CARTESIAN_POINT ( 'NONE',  ( -0.1062992125983148878, -0.1023622047244094474, -0.5909884645248154600 ) ) ;
#998=EDGE_CURVE ( 'NONE', #10209, #986, #14164, .T. ) ;
#1002=CARTESIAN_POINT ( 'NONE',  ( 1.880363195541211833E-17, -0.4881889763779528324, 0.1535433070866141780 ) ) ;
#1003=DIRECTION ( 'NONE',  ( -1.000000000000000000, 0.000000000000000000, 0.000000000000000000 ) ) ;
#1006=EDGE_LOOP ( 'NONE', ( #11275, #9630, #2726, #9101 ) ) ;
#1007=ORIENTED_EDGE ( 'NONE', *, *, #3290, .F. ) ;
#1008=EDGE_CURVE ( 'NONE', #9261, #6774, #14410, .T. ) ;
#1009=DIRECTION ( 'NONE',  ( 0.8660254037844365982, -0.000000000000000000, 0.5000000000000035527 ) ) ;
#1017=CARTESIAN_POINT ( 'NONE',  ( 0.4572203724260462399, -0.4921259842519685179, 0.3821739980041199969 ) ) ;
#1023=DIRECTION ( 'NONE',  ( 0.4999999999999981681, -0.000000000000000000, 0.8660254037844397068 ) ) ;
#1026=EDGE_CURVE ( 'NONE', #6685, #10277, #11654, .T. ) ;
#1028=DIRECTION ( 'NONE',  ( 0.5000000000000004441, 3.469446951953638170E-14, 0.8660254037844383745 ) ) ;
#1029=DIRECTION ( 'NONE',  ( 0.000000000000000000, -1.000000000000000000, 0.000000000000000000 ) ) ;
#1030=EDGE_LOOP ( 'NONE', ( #7422, #792, #11889, #9381 ) ) ;
#1037=EDGE_LOOP ( 'NONE', ( #270, #7446, #2193, #12989, #1239, #3316, #6250, #4471, #9799, #11494, #534, #1260, #10547, #8192, #10475, #4205 ) ) ;
#1038=ORIENTED_EDGE ( 'NONE', *, *, #11523, .T. ) ;
#1039=EDGE_LOOP ( 'NONE', ( #9659, #9479, #4658, #5021 ) ) ;
#1043=DIRECTION ( 'NONE',  ( -1.000000000000000000, -0.000000000000000000, -3.476578583725179813E-16 ) ) ;
#1048=DIRECTION ( 'NONE',  ( 1.000000000000000000, 0.000000000000000000, 3.075191616504340279E-15 ) ) ;
#1051=LINE ( 'NONE', #12875, #3373 ) ;
#1053=EDGE_CURVE ( 'NONE', #8246, #3171, #4640, .T. ) ;
#1054=ORIENTED_EDGE ( 'NONE', *, *, #4125, .T. ) ;
#1056=ORIENTED_EDGE ( 'NONE', *, *, #8407, .F. ) ;
#1058=LINE ( 'NONE', #7803, #11644 ) ;
#1059=CARTESIAN_POINT ( 'NONE',  ( -0.5379290338433416752, -0.1023622047244094474, 0.2423824958184911116 ) ) ;
#1064=AXIS2_PLACEMENT_3D ( 'NONE', #11866, #5662, #15159 ) ;
#1065=DIRECTION ( 'NONE',  ( 0.000000000000000000, 0.000000000000000000, 1.000000000000000000 ) ) ;
#1069=FACE_OUTER_BOUND ( 'NONE', #2234, .T. ) ;
#1075=ORIENTED_EDGE ( 'NONE', *, *, #14521, .F. ) ;
#1079=CARTESIAN_POINT ( 'NONE',  ( 0.000000000000000000, -0.4881889763779528324, 0.2083147301385909200 ) ) ;
#1080=FACE_OUTER_BOUND ( 'NONE', #2492, .T. ) ;
#1081=DIRECTION ( 'NONE',  ( -0.4999999999999982236, 0.000000000000000000, -0.8660254037844395958 ) ) ;
#1083=VERTEX_POINT ( 'NONE', #4992 ) ;
#1084=VECTOR ( 'NONE', #13829, 39.37007874015748143 ) ;
#1085=DIRECTION ( 'NONE',  ( 0.000000000000000000, -1.000000000000000000, 0.000000000000000000 ) ) ;
#1088=TOROIDAL_SURFACE ( 'NONE', #12839, 0.007874015748031495954, 0.003937007874015747977 ) ;
#1089=EDGE_CURVE ( 'NONE', #8213, #14839, #8903, .T. ) ;
#1090=ORIENTED_EDGE ( 'NONE', *, *, #11951, .F. ) ;
#1091=ORIENTED_EDGE ( 'NONE', *, *, #14062, .T. ) ;
#1093=VERTEX_POINT ( 'NONE', #6626 ) ;
#1094=AXIS2_PLACEMENT_3D ( 'NONE', #3540, #10900, #6990 ) ;
#1101=DIRECTION ( 'NONE',  ( -0.000000000000000000, 0.000000000000000000, 1.000000000000000000 ) ) ;
#1103=ORIENTED_EDGE ( 'NONE', *, *, #13036, .T. ) ;
#1105=CARTESIAN_POINT ( 'NONE',  ( -0.06692913385815728311, -0.2952755905511811330, -0.4190977005962941426 ) ) ;
#1106=DIRECTION ( 'NONE',  ( -0.8660254037844385966, 0.000000000000000000, 0.5000000000000001110 ) ) ;
#1107=AXIS2_PLACEMENT_3D ( 'NONE', #7484, #1611, #6375 ) ;
#1108=CIRCLE ( 'NONE', #13108, 0.003937007874015758385 ) ;
#1114=AXIS2_PLACEMENT_3D ( 'NONE', #9732, #3997, #11107 ) ;
#1116=ORIENTED_EDGE ( 'NONE', *, *, #5872, .T. ) ;
#1117=EDGE_CURVE ( 'NONE', #8847, #15055, #5351, .T. ) ;
#1118=EDGE_LOOP ( 'NONE', ( #3689, #4152, #977, #3450 ) ) ;
#1119=ORIENTED_EDGE ( 'NONE', *, *, #2493, .F. ) ;
#1122=AXIS2_PLACEMENT_3D ( 'NONE', #14650, #2657, #6303 ) ;
#1124=AXIS2_PLACEMENT_3D ( 'NONE', #9247, #5475, #10193 ) ;
#1125=EDGE_CURVE ( 'NONE', #5966, #5709, #132, .T. ) ;
#1127=CARTESIAN_POINT ( 'NONE',  ( -0.09842519685028340570, -0.4881889763779528324, -0.5870514566507987197 ) ) ;
#1131=CIRCLE ( 'NONE', #119, 0.003937007874015758385 ) ;
#1133=DIRECTION ( 'NONE',  ( -1.000000000000000000, 0.000000000000000000, 0.000000000000000000 ) ) ;
#1136=CARTESIAN_POINT ( 'NONE',  ( 0.4591888763630541104, -0.1023622047244094474, 0.3787644491703230365 ) ) ;
#1138=AXIS2_PLACEMENT_3D ( 'NONE', #9344, #11618, #1048 ) ;
#1141=ORIENTED_EDGE ( 'NONE', *, *, #10199, .F. ) ;
#1143=ORIENTED_EDGE ( 'NONE', *, *, #5974, .F. ) ;
#1145=EDGE_LOOP ( 'NONE', ( #3197, #1402, #14727 ) ) ;
#1148=EDGE_CURVE ( 'NONE', #11634, #8246, #13667, .T. ) ;
#1149=DIRECTION ( 'NONE',  ( 0.000000000000000000, 0.000000000000000000, 1.000000000000000000 ) ) ;
#1153=LINE ( 'NONE', #11731, #4595 ) ;
#1154=CIRCLE ( 'NONE', #1885, 0.007874015748031499423 ) ;
#1156=CARTESIAN_POINT ( 'NONE',  ( 0.2364476915724980366, -0.1023622047244094474, 0.06377609659104091500 ) ) ;
#1159=DIRECTION ( 'NONE',  ( -0.000000000000000000, 1.000000000000000000, -0.000000000000000000 ) ) ;
#1160=ORIENTED_EDGE ( 'NONE', *, *, #14997, .F. ) ;
#1163=VERTEX_POINT ( 'NONE', #1637 ) ;
#1167=AXIS2_PLACEMENT_3D ( 'NONE', #6938, #6845, #4745 ) ;
#1168=CARTESIAN_POINT ( 'NONE',  ( -0.5418660417173573052, -0.4881889763779528324, 0.2355633981508970798 ) ) ;
#1172=AXIS2_PLACEMENT_3D ( 'NONE', #8430, #6053, #10842 ) ;
#1173=DIRECTION ( 'NONE',  ( -3.614007241618347785E-16, 0.000000000000000000, 1.000000000000000000 ) ) ;
#1175=EDGE_CURVE ( 'NONE', #10209, #7182, #169, .T. ) ;
#1176=FACE_OUTER_BOUND ( 'NONE', #14953, .T. ) ;
#1177=CARTESIAN_POINT ( 'NONE',  ( -0.4591888763630546655, -0.1023622047244094474, 0.3787644491703233141 ) ) ;
#1178=CIRCLE ( 'NONE', #423, 0.003937007874015721089 ) ;
#1183=CARTESIAN_POINT ( 'NONE',  ( 0.4330708661417309036, -0.09448818897637796532, 0.4318761856142889766 ) ) ;
#1189=DIRECTION ( 'NONE',  ( -0.4999999999999979461, -0.000000000000000000, -0.8660254037844398178 ) ) ;
#1191=DIRECTION ( 'NONE',  ( -0.8660254037844385966, 0.000000000000000000, 0.5000000000000001110 ) ) ;
#1194=EDGE_LOOP ( 'NONE', ( #138, #12948, #905, #1357 ) ) ;
#1198=FACE_BOUND ( 'NONE', #8594, .T. ) ;
#1199=CARTESIAN_POINT ( 'NONE',  ( -0.5860051159906336515, -0.003937007874015747977, 0.1591122789105256785 ) ) ;
#1200=ORIENTED_EDGE ( 'NONE', *, *, #4816, .T. ) ;
#1202=VERTEX_POINT ( 'NONE', #10085 ) ;
#1204=ADVANCED_FACE ( 'NONE', ( #307 ), #13467, .T. ) ;
#1209=DIRECTION ( 'NONE',  ( 0.5000000000000036637, -0.000000000000000000, 0.8660254037844364872 ) ) ;
#1217=LINE ( 'NONE', #5970, #5418 ) ;
#1218=AXIS2_PLACEMENT_3D ( 'NONE', #2988, #6561, #6799 ) ;
#1221=ORIENTED_EDGE ( 'NONE', *, *, #14388, .F. ) ;
#1223=VERTEX_POINT ( 'NONE', #14796 ) ;
#1224=DIRECTION ( 'NONE',  ( -0.8660254037844383745, 0.000000000000000000, -0.5000000000000004441 ) ) ;
#1226=FACE_OUTER_BOUND ( 'NONE', #2353, .T. ) ;
#1229=CIRCLE ( 'NONE', #15232, 0.003937007874015721089 ) ;
#1233=EDGE_CURVE ( 'NONE', #11698, #12320, #6903, .T. ) ;
#1235=AXIS2_PLACEMENT_3D ( 'NONE', #4705, #6890, #5944 ) ;
#1236=EDGE_CURVE ( 'NONE', #8739, #5216, #8622, .T. ) ;
#1238=EDGE_CURVE ( 'NONE', #3335, #15025, #11109, .T. ) ;
#1239=ORIENTED_EDGE ( 'NONE', *, *, #359, .T. ) ;
#1241=ORIENTED_EDGE ( 'NONE', *, *, #1117, .T. ) ;
#1244=CYLINDRICAL_SURFACE ( 'NONE', #10211, 0.003937007874015758385 ) ;
#1245=FACE_OUTER_BOUND ( 'NONE', #4224, .T. ) ;
#1248=EDGE_LOOP ( 'NONE', ( #7093, #11274, #11913, #12025 ) ) ;
#1253=EDGE_LOOP ( 'NONE', ( #3177, #2084, #3195, #11288 ) ) ;
#1255=CARTESIAN_POINT ( 'NONE',  ( -0.05905511811012585655, -0.1023622047244094474, -0.5870514566507987197 ) ) ;
#1256=CARTESIAN_POINT ( 'NONE',  ( -0.4749369078591176296, -0.4881889763779528324, 0.3514880584999472424 ) ) ;
#1260=ORIENTED_EDGE ( 'NONE', *, *, #2805, .T. ) ;
#1262=LINE ( 'NONE', #8158, #5344 ) ;
#1265=EDGE_CURVE ( 'NONE', #5839, #2421, #2621, .T. ) ;
#1268=EDGE_CURVE ( 'NONE', #14809, #9393, #13378, .T. ) ;
#1270=ORIENTED_EDGE ( 'NONE', *, *, #2028, .T. ) ;
#1271=DIRECTION ( 'NONE',  ( -3.614007241618347785E-16, 0.000000000000000000, 1.000000000000000000 ) ) ;
#1277=DIRECTION ( 'NONE',  ( -0.000000000000000000, -1.000000000000000000, -0.000000000000000000 ) ) ;
#1279=ORIENTED_EDGE ( 'NONE', *, *, #2460, .T. ) ;
#1280=CARTESIAN_POINT ( 'NONE',  ( 0.5894146648244296127, -0.09448818897637796532, 0.1571437749735214717 ) ) ;
#1281=DIRECTION ( 'NONE',  ( -0.4999999999999996114, -0.000000000000000000, -0.8660254037844389297 ) ) ;
#1284=DIRECTION ( 'NONE',  ( 1.000000000000000000, 0.000000000000000000, 0.000000000000000000 ) ) ;
#1287=ORIENTED_EDGE ( 'NONE', *, *, #1175, .T. ) ;
#1289=VERTEX_POINT ( 'NONE', #12821 ) ;
#1291=DIRECTION ( 'NONE',  ( -0.8660254037844405950, 0.000000000000000000, -0.4999999999999966693 ) ) ;
#1295=CARTESIAN_POINT ( 'NONE',  ( 0.3569402812043664941, -0.2952755905511811330, 0.1333425256503553147 ) ) ;
#1296=PLANE ( 'NONE',  #7157 ) ;
#1299=DIRECTION ( 'NONE',  ( 1.000000000000000000, 0.000000000000000000, 0.000000000000000000 ) ) ;
#1300=CARTESIAN_POINT ( 'NONE',  ( 0.04921259842516963884, -0.4881889763779528324, -0.08523872084487790768 ) ) ;
#1301=EDGE_CURVE ( 'NONE', #4570, #1083, #3621, .T. ) ;
#1302=VERTEX_POINT ( 'NONE', #10404 ) ;
#1303=EDGE_LOOP ( 'NONE', ( #7238, #14934, #10727, #5233 ) ) ;
#1304=ORIENTED_EDGE ( 'NONE', *, *, #12115, .T. ) ;
#1305=EDGE_CURVE ( 'NONE', #4499, #5085, #10411, .T. ) ;
#1306=EDGE_CURVE ( 'NONE', #13646, #13558, #2180, .T. ) ;
#1308=DIRECTION ( 'NONE',  ( 0.000000000000000000, 1.000000000000000000, 0.000000000000000000 ) ) ;
#1309=CYLINDRICAL_SURFACE ( 'NONE', #14469, 0.003937007874015737569 ) ;
#1311=CARTESIAN_POINT ( 'NONE',  ( -0.5905511811023629321, -0.09842519685039370636, 0.1591122789105256785 ) ) ;
#1312=CARTESIAN_POINT ( 'NONE',  ( -0.4591888763630546655, -0.4881889763779528324, 0.3787644491703233141 ) ) ;
#1317=ORIENTED_EDGE ( 'NONE', *, *, #8054, .T. ) ;
#1322=DIRECTION ( 'NONE',  ( -0.8660254037844385966, -0.000000000000000000, 0.4999999999999998890 ) ) ;
#1323=ADVANCED_FACE ( 'NONE', ( #12756 ), #15183, .T. ) ;
#1324=LINE ( 'NONE', #7431, #6350 ) ;
#1329=LINE ( 'NONE', #4937, #2425 ) ;
#1331=ORIENTED_EDGE ( 'NONE', *, *, #14763, .F. ) ;
#1334=AXIS2_PLACEMENT_3D ( 'NONE', #2347, #7133, #2089 ) ;
#1336=ORIENTED_EDGE ( 'NONE', *, *, #878, .F. ) ;
#1338=LINE ( 'NONE', #10588, #342 ) ;
#1340=CARTESIAN_POINT ( 'NONE',  ( 0.5452755905511544876, -0.1023622047244094474, 0.2375319020879054499 ) ) ;
#1342=CIRCLE ( 'NONE', #2831, 0.007874015748031475137 ) ;
#1346=ORIENTED_EDGE ( 'NONE', *, *, #10688, .T. ) ;
#1350=LINE ( 'NONE', #2370, #3127 ) ;
#1351=DIRECTION ( 'NONE',  ( 0.000000000000000000, -0.000000000000000000, 1.000000000000000000 ) ) ;
#1352=EDGE_CURVE ( 'NONE', #2681, #1223, #2011, .T. ) ;
#1353=CYLINDRICAL_SURFACE ( 'NONE', #4678, 0.03937007874015754916 ) ;
#1354=ORIENTED_EDGE ( 'NONE', *, *, #9263, .F. ) ;
#1356=AXIS2_PLACEMENT_3D ( 'NONE', #126, #9595, #13274 ) ;
#1357=ORIENTED_EDGE ( 'NONE', *, *, #4601, .F. ) ;
#1359=ORIENTED_EDGE ( 'NONE', *, *, #4172, .T. ) ;
#1361=AXIS2_PLACEMENT_3D ( 'NONE', #12006, #8303, #6896 ) ;
#1363=CIRCLE ( 'NONE', #5850, 0.003937007874015721089 ) ;
#1365=CYLINDRICAL_SURFACE ( 'NONE', #9860, 0.003937007874015758385 ) ;
#1366=FACE_OUTER_BOUND ( 'NONE', #3882, .T. ) ;
#1367=EDGE_CURVE ( 'NONE', #11240, #7731, #4621, .T. ) ;
#1369=DIRECTION ( 'NONE',  ( 0.000000000000000000, 1.000000000000000000, 0.000000000000000000 ) ) ;
#1372=CARTESIAN_POINT ( 'NONE',  ( -0.5860051159906336515, -0.003937007874015747977, 0.1591122789105256785 ) ) ;
#1375=AXIS2_PLACEMENT_3D ( 'NONE', #2969, #8829, #12452 ) ;
#1376=CIRCLE ( 'NONE', #9648, 0.1574803149606299191 ) ;
#1377=AXIS2_PLACEMENT_3D ( 'NONE', #6098, #12073, #14573 ) ;
#1379=DIRECTION ( 'NONE',  ( 0.000000000000000000, 0.000000000000000000, 1.000000000000000000 ) ) ;
#1380=LINE ( 'NONE', #6140, #6914 ) ;
#1381=CIRCLE ( 'NONE', #2120, 0.007874015748031482076 ) ;
#1382=EDGE_LOOP ( 'NONE', ( #1200, #6636, #5665, #4463 ) ) ;
#1383=ORIENTED_EDGE ( 'NONE', *, *, #10764, .F. ) ;
#1386=VECTOR ( 'NONE', #14931, 39.37007874015748143 ) ;
#1387=AXIS2_PLACEMENT_3D ( 'NONE', #2383, #14228, #11795 ) ;
#1392=ADVANCED_FACE ( 'NONE', ( #11483 ), #15012, .T. ) ;
#1394=CARTESIAN_POINT ( 'NONE',  ( 0.4330708661417309036, -0.09842519685039370636, 0.4318761856142889766 ) ) ;
#1397=EDGE_CURVE ( 'NONE', #10200, #13984, #12426, .T. ) ;
#1401=AXIS2_PLACEMENT_3D ( 'NONE', #3237, #8007, #11780 ) ;
#1402=ORIENTED_EDGE ( 'NONE', *, *, #8846, .T. ) ;
#1404=EDGE_LOOP ( 'NONE', ( #7999, #8474, #11179, #13109 ) ) ;
#1406=ORIENTED_EDGE ( 'NONE', *, *, #6368, .F. ) ;
#1416=DIRECTION ( 'NONE',  ( 0.000000000000000000, 0.000000000000000000, -1.000000000000000000 ) ) ;
#1417=AXIS2_PLACEMENT_3D ( 'NONE', #7709, #14768, #573 ) ;
#1419=ORIENTED_EDGE ( 'NONE', *, *, #14159, .F. ) ;
#1422=ADVANCED_FACE ( 'NONE', ( #5197 ), #5434, .T. ) ;
#1423=DIRECTION ( 'NONE',  ( -0.8660254037844383745, 0.000000000000000000, -0.5000000000000004441 ) ) ;
#1426=EDGE_CURVE ( 'NONE', #13559, #6292, #7633, .T. ) ;
#1427=EDGE_CURVE ( 'NONE', #3491, #5898, #12416, .T. ) ;
#1429=CARTESIAN_POINT ( 'NONE',  ( 0.3706061991976991044, -0.09842519685039370636, -0.2139695888701345916 ) ) ;
#1431=LINE ( 'NONE', #6185, #1604 ) ;
#1435=DIRECTION ( 'NONE',  ( -0.5000000000000000000, 0.000000000000000000, -0.8660254037844385966 ) ) ;
#1437=CARTESIAN_POINT ( 'NONE',  ( -0.4606299212598433113, -0.4921259842519685179, 0.3841425019411278674 ) ) ;
#1440=VECTOR ( 'NONE', #5295, 39.37007874015748143 ) ;
#1441=CARTESIAN_POINT ( 'NONE',  ( 0.2613315816342647868, -0.4881889763779528324, 0.03601011673569576993 ) ) ;
#1442=CARTESIAN_POINT ( 'NONE',  ( 0.06767366483286080259, -0.2952755905511811330, 0.7209811753676967916 ) ) ;
#1443=CIRCLE ( 'NONE', #5931, 0.003937007874015743640 ) ;
#1446=EDGE_LOOP ( 'NONE', ( #3472, #11159, #6773, #2326 ) ) ;
#1456=DIRECTION ( 'NONE',  ( -0.000000000000000000, -1.000000000000000000, -0.000000000000000000 ) ) ;
#1458=CARTESIAN_POINT ( 'NONE',  ( -0.1552072824047653066, -0.09448818897637796532, -0.5870514566507987197 ) ) ;
#1459=CIRCLE ( 'NONE', #4946, 0.003937007874015754916 ) ;
#1460=CARTESIAN_POINT ( 'NONE',  ( 0.5418660417173575272, -0.4921259842519685179, 0.2355633981508976627 ) ) ;
#1461=AXIS2_PLACEMENT_3D ( 'NONE', #5868, #15363, #9256 ) ;
#1468=EDGE_CURVE ( 'NONE', #15072, #12817, #3016, .T. ) ;
#1471=CARTESIAN_POINT ( 'NONE',  ( 0.1618514667033794374, -0.4881889763779528324, 0.2161887458866224576 ) ) ;
#1472=VECTOR ( 'NONE', #7323, 39.37007874015748143 ) ;
#1473=SPHERICAL_SURFACE ( 'NONE', #14206, 0.003937007874015747977 ) ;
#1474=CARTESIAN_POINT ( 'NONE',  ( 0.1028896637646825596, -0.1023622047244094474, -0.2462933508111075365 ) ) ;
#1482=EDGE_LOOP ( 'NONE', ( #13423, #9079, #1781, #850 ) ) ;
#1483=ORIENTED_EDGE ( 'NONE', *, *, #15195, .F. ) ;
#1488=ADVANCED_FACE ( 'NONE', ( #13033 ), #11633, .F. ) ;
#1489=LINE ( 'NONE', #2734, #10112 ) ;
#1492=CARTESIAN_POINT ( 'NONE',  ( 0.4319503555479007328, -0.2952755905511811330, 0.1766496122645286049 ) ) ;
#1494=ORIENTED_EDGE ( 'NONE', *, *, #9429, .T. ) ;
#1495=CARTESIAN_POINT ( 'NONE',  ( 0.5576140732134206024, -0.4881889763779528324, 0.2082870074805215910 ) ) ;
#1497=CARTESIAN_POINT ( 'NONE',  ( -0.2647411304678976007, -0.09842519685039372024, 0.03404161279859290595 ) ) ;
#1499=VERTEX_POINT ( 'NONE', #2062 ) ;
#1500=ORIENTED_EDGE ( 'NONE', *, *, #14226, .F. ) ;
#1501=EDGE_CURVE ( 'NONE', #8390, #15216, #4564, .T. ) ;
#1502=SPHERICAL_SURFACE ( 'NONE', #3612, 0.003937007874015747977 ) ;
#1512=CARTESIAN_POINT ( 'NONE',  ( -0.1734555655881918346, -0.1023622047244094474, 0.1728816592724491952 ) ) ;
#1518=CARTESIAN_POINT ( 'NONE',  ( -0.05905511811012585655, -0.1023622047244094474, -0.5909884645248154600 ) ) ;
#1519=CARTESIAN_POINT ( 'NONE',  ( -0.1724006475077544398, -0.4881889763779528324, 0.1768186671464649640 ) ) ;
#1523=CARTESIAN_POINT ( 'NONE',  ( 0.1618514667033794374, -0.4881889763779528324, 0.2122517380126066888 ) ) ;
#1524=ADVANCED_FACE ( 'NONE', ( #902 ), #8097, .T. ) ;
#1526=CARTESIAN_POINT ( 'NONE',  ( 0.4307978335858664853, -0.09842519685039370636, 0.4318761856142889766 ) ) ;
#1530=ORIENTED_EDGE ( 'NONE', *, *, #5773, .T. ) ;
#1531=FACE_OUTER_BOUND ( 'NONE', #2276, .T. ) ;
#1534=CARTESIAN_POINT ( 'NONE',  ( 0.5894146648244296127, -0.003937007874015747977, 0.1571437749735214717 ) ) ;
#1536=DIRECTION ( 'NONE',  ( 0.4999999999999966693, 0.000000000000000000, 0.8660254037844405950 ) ) ;
#1538=EDGE_CURVE ( 'NONE', #2979, #6007, #12884, .T. ) ;
#1540=FACE_OUTER_BOUND ( 'NONE', #11225, .T. ) ;
#1543=EDGE_CURVE ( 'NONE', #10323, #8667, #10374, .T. ) ;
#1548=DIRECTION ( 'NONE',  ( 0.8660254037844383745, 0.000000000000000000, 0.5000000000000004441 ) ) ;
#1552=EDGE_CURVE ( 'NONE', #8212, #8213, #2605, .T. ) ;
#1556=ADVANCED_FACE ( 'NONE', ( #5507 ), #3490, .F. ) ;
#1570=EDGE_CURVE ( 'NONE', #8667, #8301, #11791, .T. ) ;
#1571=ORIENTED_EDGE ( 'NONE', *, *, #5696, .F. ) ;
#1575=CIRCLE ( 'NONE', #10326, 0.003937007874015750579 ) ;
#1577=AXIS2_PLACEMENT_3D ( 'NONE', #8678, #2488, #13227 ) ;
#1585=EDGE_CURVE ( 'NONE', #984, #9393, #12803, .T. ) ;
#1586=DIRECTION ( 'NONE',  ( 0.000000000000000000, 0.000000000000000000, -1.000000000000000000 ) ) ;
#1592=CIRCLE ( 'NONE', #107, 0.007874015748031499423 ) ;
#1596=DIRECTION ( 'NONE',  ( 0.000000000000000000, -1.000000000000000000, 0.000000000000000000 ) ) ;
#1597=CARTESIAN_POINT ( 'NONE',  ( 0.03357817649489055339, -0.2952755905511811330, 0.7012961359976183084 ) ) ;
#1601=AXIS2_PLACEMENT_3D ( 'NONE', #2236, #5740, #992 ) ;
#1604=VECTOR ( 'NONE', #8856, 39.37007874015748143 ) ;
#1605=CARTESIAN_POINT ( 'NONE',  ( -0.4307978335858689833, -0.003937007874015747977, 0.4279391777402706265 ) ) ;
#1607=ORIENTED_EDGE ( 'NONE', *, *, #13477, .F. ) ;
#1608=TOROIDAL_SURFACE ( 'NONE', #8118, 0.04330708661417328326, 0.003937007874015747977 ) ;
#1610=EDGE_CURVE ( 'NONE', #4124, #6576, #13195, .T. ) ;
#1611=DIRECTION ( 'NONE',  ( 0.4999999999999996114, 0.000000000000000000, 0.8660254037844389297 ) ) ;
#1613=CIRCLE ( 'NONE', #11882, 0.003937007874015758385 ) ;
#1616=CARTESIAN_POINT ( 'NONE',  ( 0.000000000000000000, 0.000000000000000000, 0.000000000000000000 ) ) ;
#1617=CIRCLE ( 'NONE', #10371, 0.1574803149606299191 ) ;
#1618=TOROIDAL_SURFACE ( 'NONE', #11632, 0.04330708661417328326, 0.003937007874015747977 ) ;
#1621=CIRCLE ( 'NONE', #10876, 0.003937007874015758385 ) ;
#1626=DIRECTION ( 'NONE',  ( 0.5000000000000003331, 0.000000000000000000, -0.8660254037844387076 ) ) ;
#1627=VERTEX_POINT ( 'NONE', #10358 ) ;
#1628=ORIENTED_EDGE ( 'NONE', *, *, #5394, .F. ) ;
#1629=VECTOR ( 'NONE', #12264, 39.37007874015748143 ) ;
#1630=ORIENTED_EDGE ( 'NONE', *, *, #2426, .F. ) ;
#1631=AXIS2_PLACEMENT_3D ( 'NONE', #1993, #2225, #13029 ) ;
#1632=CIRCLE ( 'NONE', #1387, 0.04330708661417331101 ) ;
#1637=CARTESIAN_POINT ( 'NONE',  ( 0.1062992125984796865, -0.09448818897637796532, -0.5909884645248143498 ) ) ;
#1638=CARTESIAN_POINT ( 'NONE',  ( 0.5433070866142283295, -0.1023622047244094474, 0.2409414509217496780 ) ) ;
#1639=DIRECTION ( 'NONE',  ( 0.4999999999999966693, 0.000000000000000000, 0.8660254037844405950 ) ) ;
#1640=CARTESIAN_POINT ( 'NONE',  ( 1.904470415996868375E-17, -0.4921259842519685179, 0.1535433070866141780 ) ) ;
#1641=FACE_OUTER_BOUND ( 'NONE', #1039, .T. ) ;
#1653=ADVANCED_FACE ( 'NONE', ( #13746 ), #1989, .T. ) ;
#1655=VECTOR ( 'NONE', #7555, 39.37007874015748143 ) ;
#1656=ADVANCED_FACE ( 'NONE', ( #6750, #13975 ), #2050, .F. ) ;
#1663=DIRECTION ( 'NONE',  ( 0.5000000000000036637, -0.000000000000000000, 0.8660254037844364872 ) ) ;
#1665=DIRECTION ( 'NONE',  ( -0.5000000000000003331, -0.000000000000000000, 0.8660254037844387076 ) ) ;
#1670=DIRECTION ( 'NONE',  ( 0.000000000000000000, 0.000000000000000000, 1.000000000000000000 ) ) ;
#1677=CARTESIAN_POINT ( 'NONE',  ( -0.5860051159906336515, -0.003937007874015747977, 0.1591122789105256785 ) ) ;
#1682=DIRECTION ( 'NONE',  ( -0.8660254037844395958, 0.000000000000000000, 0.4999999999999982236 ) ) ;
#1685=FACE_OUTER_BOUND ( 'NONE', #8518, .T. ) ;
#1686=DIRECTION ( 'NONE',  ( 0.000000000000000000, 1.000000000000000000, 0.000000000000000000 ) ) ;
#1687=DIRECTION ( 'NONE',  ( 0.000000000000000000, -1.000000000000000000, -0.000000000000000000 ) ) ;
#1690=AXIS2_PLACEMENT_3D ( 'NONE', #2211, #5786, #4396 ) ;
#1691=ORIENTED_EDGE ( 'NONE', *, *, #15456, .T. ) ;
#1692=DIRECTION ( 'NONE',  ( 0.000000000000000000, 0.000000000000000000, 1.000000000000000000 ) ) ;
#1693=ORIENTED_EDGE ( 'NONE', *, *, #8707, .T. ) ;
#1694=AXIS2_PLACEMENT_3D ( 'NONE', #599, #5210, #1774 ) ;
#1700=DIRECTION ( 'NONE',  ( 0.5000000000000035527, 0.000000000000000000, -0.8660254037844365982 ) ) ;
#1704=TOROIDAL_SURFACE ( 'NONE', #14975, 0.04330708661417328326, 0.003937007874015747977 ) ;
#1710=EDGE_LOOP ( 'NONE', ( #7050, #11774, #11724, #13595 ) ) ;
#1711=ORIENTED_EDGE ( 'NONE', *, *, #12080, .T. ) ;
#1713=ORIENTED_EDGE ( 'NONE', *, *, #10319, .F. ) ;
#1714=ORIENTED_EDGE ( 'NONE', *, *, #8843, .F. ) ;
#1717=DIRECTION ( 'NONE',  ( 0.5000000000000000000, 0.000000000000000000, -0.8660254037844385966 ) ) ;
#1718=CARTESIAN_POINT ( 'NONE',  ( -0.5084014747882513729, -0.09842519685039370636, 0.2935257283253980831 ) ) ;
#1719=CARTESIAN_POINT ( 'NONE',  ( 0.06692913385832209572, -0.4881889763779528324, -0.2377126739437404879 ) ) ;
#1721=CARTESIAN_POINT ( 'NONE',  ( -0.5595825771504281398, -0.4881889763779528324, 0.2048774586467239645 ) ) ;
#1722=DIRECTION ( 'NONE',  ( 0.000000000000000000, -1.000000000000000000, 0.000000000000000000 ) ) ;
#1724=SPHERICAL_SURFACE ( 'NONE', #9947, 0.003937007874015747977 ) ;
#1728=DIRECTION ( 'NONE',  ( 0.000000000000000000, 0.000000000000000000, -1.000000000000000000 ) ) ;
#1733=DIRECTION ( 'NONE',  ( -1.504632769052539669E-28, -8.673617379884051249E-15, 1.000000000000000000 ) ) ;
#1738=ORIENTED_EDGE ( 'NONE', *, *, #5192, .F. ) ;
#1739=ADVANCED_FACE ( 'NONE', ( #9195 ), #2673, .F. ) ;
#1740=CYLINDRICAL_SURFACE ( 'NONE', #4919, 0.003937007874015735834 ) ;
#1743=EDGE_CURVE ( 'NONE', #4061, #4031, #13436, .T. ) ;
#1744=DIRECTION ( 'NONE',  ( 0.000000000000000000, 0.000000000000000000, 1.000000000000000000 ) ) ;
#1745=ORIENTED_EDGE ( 'NONE', *, *, #9638, .F. ) ;
#1748=DIRECTION ( 'NONE',  ( 0.8660254037844385966, 0.000000000000000000, -0.4999999999999998890 ) ) ;
#1749=FACE_OUTER_BOUND ( 'NONE', #3031, .T. ) ;
#1753=DIRECTION ( 'NONE',  ( 0.000000000000000000, -1.000000000000000000, 0.000000000000000000 ) ) ;
#1756=DIRECTION ( 'NONE',  ( 0.8660254037844459241, 0.000000000000000000, 0.4999999999999873990 ) ) ;
#1757=CARTESIAN_POINT ( 'NONE',  ( -0.4572203724260467950, -0.4921259842519685179, 0.3821739980041202744 ) ) ;
#1759=FACE_OUTER_BOUND ( 'NONE', #10317, .T. ) ;
#1761=DIRECTION ( 'NONE',  ( -1.445602896647339903E-16, -0.000000000000000000, 1.000000000000000000 ) ) ;
#1762=ORIENTED_EDGE ( 'NONE', *, *, #2654, .T. ) ;
#1767=CARTESIAN_POINT ( 'NONE',  ( 0.5398975377803496567, -0.09842519685039372024, 0.2389729469846946508 ) ) ;
#1771=CARTESIAN_POINT ( 'NONE',  ( 0.2647411304680618027, -0.1023622047244094474, 0.03404161279868787859 ) ) ;
#1773=EDGE_CURVE ( 'NONE', #8290, #3157, #14124, .T. ) ;
#1774=DIRECTION ( 'NONE',  ( -0.8660254037844390407, 0.000000000000000000, 0.4999999999999994449 ) ) ;
#1777=ORIENTED_EDGE ( 'NONE', *, *, #6701, .F. ) ;
#1778=EDGE_CURVE ( 'NONE', #7138, #7284, #14200, .T. ) ;
#1781=ORIENTED_EDGE ( 'NONE', *, *, #13152, .T. ) ;
#1782=ORIENTED_EDGE ( 'NONE', *, *, #991, .F. ) ;
#1783=ORIENTED_EDGE ( 'NONE', *, *, #12115, .F. ) ;
#1786=DIRECTION ( 'NONE',  ( 0.000000000000000000, 1.000000000000000000, 0.000000000000000000 ) ) ;
#1792=CARTESIAN_POINT ( 'NONE',  ( -0.5418660417173573052, -0.09842519685039370636, 0.2355633981508970798 ) ) ;
#1794=ORIENTED_EDGE ( 'NONE', *, *, #12680, .F. ) ;
#1795=DIRECTION ( 'NONE',  ( -0.4999999999999995004, -0.000000000000000000, -0.8660254037844390407 ) ) ;
#1798=ORIENTED_EDGE ( 'NONE', *, *, #2623, .F. ) ;
#1799=EDGE_LOOP ( 'NONE', ( #10229, #6759, #4858, #1287 ) ) ;
#1801=DIRECTION ( 'NONE',  ( -1.000000000000000000, 0.000000000000000000, -3.075191616504340279E-15 ) ) ;
#1802=DIRECTION ( 'NONE',  ( 0.8660254037844385966, 0.000000000000000000, -0.4999999999999998890 ) ) ;
#1809=FACE_OUTER_BOUND ( 'NONE', #6119, .T. ) ;
#1810=VERTEX_POINT ( 'NONE', #11784 ) ;
#1814=FACE_OUTER_BOUND ( 'NONE', #4208, .T. ) ;
#1819=CIRCLE ( 'NONE', #826, 0.04330708661417328326 ) ;
#1820=DIRECTION ( 'NONE',  ( -1.000000000000000000, -0.000000000000000000, -3.476578583725179813E-16 ) ) ;
#1822=LINE ( 'NONE', #438, #7406 ) ;
#1824=ADVANCED_FACE ( 'NONE', ( #13186 ), #2220, .T. ) ;
#1825=DIRECTION ( 'NONE',  ( -0.000000000000000000, 1.000000000000000000, 0.000000000000000000 ) ) ;
#1827=CARTESIAN_POINT ( 'NONE',  ( 0.5615510810874363434, -0.09842519685039370636, 0.2014679098129276424 ) ) ;
#1828=CARTESIAN_POINT ( 'NONE',  ( 0.06299212598430634080, -0.4881889763779528324, -0.2366577558633030653 ) ) ;
#1829=ORIENTED_EDGE ( 'NONE', *, *, #4344, .F. ) ;
#1831=CARTESIAN_POINT ( 'NONE',  ( 0.000000000000000000, -0.4921259842519685179, 0.000000000000000000 ) ) ;
#1835=AXIS2_PLACEMENT_3D ( 'NONE', #4970, #13213, #7250 ) ;
#1837=ADVANCED_FACE ( 'NONE', ( #13025 ), #12870, .T. ) ;
#1843=CARTESIAN_POINT ( 'NONE',  ( 0.2613315816342647868, -0.4921259842519685179, 0.03601011673569576993 ) ) ;
#1846=CIRCLE ( 'NONE', #10607, 0.003937007874015721089 ) ;
#1847=CARTESIAN_POINT ( 'NONE',  ( 0.000000000000000000, 2.165354330708661568, 0.000000000000000000 ) ) ;
#1852=ORIENTED_EDGE ( 'NONE', *, *, #11199, .T. ) ;
#1853=ORIENTED_EDGE ( 'NONE', *, *, #9622, .F. ) ;
#1854=ORIENTED_EDGE ( 'NONE', *, *, #11237, .T. ) ;
#1857=AXIS2_PLACEMENT_3D ( 'NONE', #7340, #3912, #3990 ) ;
#1858=EDGE_CURVE ( 'NONE', #6593, #2728, #4786, .T. ) ;
#1861=DIRECTION ( 'NONE',  ( -0.8660254037844395958, 0.000000000000000000, 0.4999999999999982236 ) ) ;
#1862=TOROIDAL_SURFACE ( 'NONE', #7355, 0.007874015748031495954, 0.003937007874015747977 ) ;
#1864=CIRCLE ( 'NONE', #12627, 0.003937007874015754916 ) ;
#1865=CARTESIAN_POINT ( 'NONE',  ( 0.2681506793018588186, -0.4881889763779528324, 0.03207310886168001501 ) ) ;
#1868=EDGE_CURVE ( 'NONE', #1163, #2262, #4696, .T. ) ;
#1869=CARTESIAN_POINT ( 'NONE',  ( 0.09842519685044820443, -0.4881889763779528324, -0.5870514566507987197 ) ) ;
#1874=LINE ( 'NONE', #2099, #14951 ) ;
#1876=AXIS2_PLACEMENT_3D ( 'NONE', #1136, #5888, #13894 ) ;
#1882=ORIENTED_EDGE ( 'NONE', *, *, #4444, .T. ) ;
#1885=AXIS2_PLACEMENT_3D ( 'NONE', #4955, #3711, #7457 ) ;
#1888=DIRECTION ( 'NONE',  ( 0.000000000000000000, 0.000000000000000000, -1.000000000000000000 ) ) ;
#1889=EDGE_CURVE ( 'NONE', #13559, #1223, #13696, .T. ) ;
#1891=CARTESIAN_POINT ( 'NONE',  ( 0.2642136714278430776, -0.4921259842519685179, 0.03889220652927401906 ) ) ;
#1893=DIRECTION ( 'NONE',  ( 0.000000000000000000, 0.000000000000000000, -1.000000000000000000 ) ) ;
#1896=CARTESIAN_POINT ( 'NONE',  ( 0.5905511811023622659, -0.2952755905511811330, -0.3797276218561363992 ) ) ;
#1899=ORIENTED_EDGE ( 'NONE', *, *, #12865, .T. ) ;
#1901=DIRECTION ( 'NONE',  ( 0.4999999999999995004, 0.000000000000000000, 0.8660254037844390407 ) ) ;
#1904=AXIS2_PLACEMENT_3D ( 'NONE', #11701, #15223, #3394 ) ;
#1905=VERTEX_POINT ( 'NONE', #3929 ) ;
#1906=ORIENTED_EDGE ( 'NONE', *, *, #13596, .F. ) ;
#1908=PRODUCT ( 'Spider', 'Spider', '', ( #9038 ) ) ;
#1910=DIRECTION ( 'NONE',  ( 1.000000000000000000, 0.000000000000000000, 0.000000000000000000 ) ) ;
#1912=DIRECTION ( 'NONE',  ( -0.5000000000000004441, -0.000000000000000000, -0.8660254037844384856 ) ) ;
#1914=DIRECTION ( 'NONE',  ( 0.5000000000000035527, 0.000000000000000000, -0.8660254037844365982 ) ) ;
#1919=CARTESIAN_POINT ( 'NONE',  ( -0.06692913385815757454, -0.4921259842519685179, -2.418823744386252084E-17 ) ) ;
#1921=LINE ( 'NONE', #12568, #14937 ) ;
#1926=CARTESIAN_POINT ( 'NONE',  ( -0.2681506793016945611, -0.1023622047244094474, 0.03207310886158502850 ) ) ;
#1930=FACE_OUTER_BOUND ( 'NONE', #9258, .T. ) ;
#1931=AXIS2_PLACEMENT_3D ( 'NONE', #3119, #14876, #8931 ) ;
#1933=EDGE_CURVE ( 'NONE', #2868, #2979, #13948, .T. ) ;
#1936=AXIS2_PLACEMENT_3D ( 'NONE', #13291, #4916, #13062 ) ;
#1938=ORIENTED_EDGE ( 'NONE', *, *, #1367, .F. ) ;
#1939=EDGE_LOOP ( 'NONE', ( #11995, #12572, #13977, #12235 ) ) ;
#1940=AXIS2_PLACEMENT_3D ( 'NONE', #2450, #5723, #4726 ) ;
#1941=ORIENTED_EDGE ( 'NONE', *, *, #13477, .T. ) ;
#1945=CARTESIAN_POINT ( 'NONE',  ( -0.06299212598414166697, -0.2952755905511811330, -0.4190977005962941426 ) ) ;
#1947=AXIS2_PLACEMENT_3D ( 'NONE', #11990, #9709, #14317 ) ;
#1954=DIRECTION ( 'NONE',  ( -0.5000000000000035527, -0.000000000000000000, 0.8660254037844365982 ) ) ;
#1959=EDGE_CURVE ( 'NONE', #12255, #14974, #6560, .T. ) ;
#1961=EDGE_LOOP ( 'NONE', ( #12312, #10307, #10096, #7268 ) ) ;
#1966=CYLINDRICAL_SURFACE ( 'NONE', #13124, 0.003937007874015724558 ) ;
#1967=CIRCLE ( 'NONE', #6417, 0.003937007874015724558 ) ;
#1968=DIRECTION ( 'NONE',  ( 0.000000000000000000, 0.000000000000000000, -1.000000000000000000 ) ) ;
#1971=DIRECTION ( 'NONE',  ( -1.060575238724907285E-16, 1.000000000000000000, 6.123233995736761105E-17 ) ) ;
#1972=LINE ( 'NONE', #8155, #5624 ) ;
#1973=ORIENTED_EDGE ( 'NONE', *, *, #14321, .T. ) ;
#1974=CARTESIAN_POINT ( 'NONE',  ( -0.5615510810874360104, -0.09448818897637796532, 0.2014679098129269208 ) ) ;
#1979=DIRECTION ( 'NONE',  ( -1.000000000000000000, -1.734723475976807094E-14, 0.000000000000000000 ) ) ;
#1984=DIRECTION ( 'NONE',  ( 1.000000000000000000, 1.734723475976802677E-14, 0.000000000000000000 ) ) ;
#1986=EDGE_CURVE ( 'NONE', #13529, #10725, #1443, .T. ) ;
#1989=CYLINDRICAL_SURFACE ( 'NONE', #6663, 0.003937007874015721089 ) ;
#1991=ORIENTED_EDGE ( 'NONE', *, *, #14391, .T. ) ;
#1993=CARTESIAN_POINT ( 'NONE',  ( -0.06692913385815728311, -0.2952755905511811330, -0.4190977005962941426 ) ) ;
#1999=EDGE_CURVE ( 'NONE', #2901, #3536, #12946, .T. ) ;
#2001=CYLINDRICAL_SURFACE ( 'NONE', #14089, 0.003937007874015724558 ) ;
#2002=DIRECTION ( 'NONE',  ( 4.336808689942025625E-15, 0.000000000000000000, 1.000000000000000000 ) ) ;
#2007=ORIENTED_EDGE ( 'NONE', *, *, #5272, .T. ) ;
#2009=ORIENTED_EDGE ( 'NONE', *, *, #10583, .T. ) ;
#2010=DIRECTION ( 'NONE',  ( 0.000000000000000000, 0.000000000000000000, -1.000000000000000000 ) ) ;
#2011=LINE ( 'NONE', #9233, #13122 ) ;
#2015=DIRECTION ( 'NONE',  ( 0.8660254037844383745, 0.000000000000000000, 0.5000000000000004441 ) ) ;
#2019=LINE ( 'NONE', #5531, #11444 ) ;
#2020=EDGE_CURVE ( 'NONE', #13529, #10010, #11280, .T. ) ;
#2021=DIRECTION ( 'NONE',  ( 0.000000000000000000, 0.000000000000000000, -1.000000000000000000 ) ) ;
#2025=ORIENTED_EDGE ( 'NONE', *, *, #5981, .T. ) ;
#2028=EDGE_CURVE ( 'NONE', #14862, #11768, #10451, .T. ) ;
#2034=CARTESIAN_POINT ( 'NONE',  ( 0.000000000000000000, -0.4921259842519685179, 0.2083147301385909200 ) ) ;
#2039=ORIENTED_EDGE ( 'NONE', *, *, #4192, .F. ) ;
#2041=ORIENTED_EDGE ( 'NONE', *, *, #2654, .F. ) ;
#2044=EDGE_CURVE ( 'NONE', #12219, #14791, #12931, .T. ) ;
#2046=CARTESIAN_POINT ( 'NONE',  ( -0.5379290338433415641, -0.09842519685039370636, 0.2423824958184910838 ) ) ;
#2048=DIRECTION ( 'NONE',  ( 0.000000000000000000, 1.000000000000000000, 0.000000000000000000 ) ) ;
#2050=PLANE ( 'NONE',  #4686 ) ;
#2051=CARTESIAN_POINT ( 'NONE',  ( 0.4141303577462121521, -0.2952755905511811330, 0.1209005806194717869 ) ) ;
#2054=ADVANCED_FACE ( 'NONE', ( #8298 ), #10569, .F. ) ;
#2060=ORIENTED_EDGE ( 'NONE', *, *, #3193, .F. ) ;
#2061=ADVANCED_FACE ( 'NONE', ( #13008 ), #7043, .F. ) ;
#2062=CARTESIAN_POINT ( 'NONE',  ( 0.5860051159906326523, -0.09842519685039370636, 0.1591122789105293700 ) ) ;
#2063=EDGE_LOOP ( 'NONE', ( #13034, #5955, #2082, #8899 ) ) ;
#2064=ORIENTED_EDGE ( 'NONE', *, *, #8846, .F. ) ;
#2066=AXIS2_PLACEMENT_3D ( 'NONE', #3098, #14852, #2862 ) ;
#2067=CARTESIAN_POINT ( 'NONE',  ( -0.06299212598414173636, -0.1023622047244094474, -0.2366577558633980449 ) ) ;
#2073=DIRECTION ( 'NONE',  ( -0.8660254037844390407, 0.000000000000000000, 0.4999999999999994449 ) ) ;
#2074=SPHERICAL_SURFACE ( 'NONE', #14586, 0.003937007874015747977 ) ;
#2075=CARTESIAN_POINT ( 'NONE',  ( -0.06692913385815735250, -0.4881889763779528324, -0.5870514566507987197 ) ) ;
#2079=VERTEX_POINT ( 'NONE', #954 ) ;
#2080=CIRCLE ( 'NONE', #10829, 0.003937007874015741038 ) ;
#2081=ADVANCED_FACE ( 'NONE', ( #8058 ), #5683, .T. ) ;
#2082=ORIENTED_EDGE ( 'NONE', *, *, #49, .F. ) ;
#2084=ORIENTED_EDGE ( 'NONE', *, *, #11237, .F. ) ;
#2088=AXIS2_PLACEMENT_3D ( 'NONE', #6059, #4909, #3739 ) ;
#2089=DIRECTION ( 'NONE',  ( -1.000000000000000000, 0.000000000000000000, 0.000000000000000000 ) ) ;
#2095=AXIS2_PLACEMENT_3D ( 'NONE', #3483, #14355, #7295 ) ;
#2098=VERTEX_POINT ( 'NONE', #4537 ) ;
#2099=CARTESIAN_POINT ( 'NONE',  ( 0.1574803149606299191, -0.09448818897637796532, -0.5909884645248143498 ) ) ;
#2101=EDGE_LOOP ( 'NONE', ( #8506, #13736, #6923, #11840 ) ) ;
#2102=EDGE_LOOP ( 'NONE', ( #4188, #14365, #1075, #8468 ) ) ;
#2105=CIRCLE ( 'NONE', #117, 0.003937007874015758385 ) ;
#2106=TOROIDAL_SURFACE ( 'NONE', #1114, 0.04330708661417328326, 0.003937007874015747977 ) ;
#2108=AXIS2_PLACEMENT_3D ( 'NONE', #1127, #11850, #10749 ) ;
#2110=EDGE_LOOP ( 'NONE', ( #4960, #15372, #7655, #222 ) ) ;
#2117=VERTEX_POINT ( 'NONE', #14562 ) ;
#2119=CYLINDRICAL_SURFACE ( 'NONE', #12126, 0.003937007874015724558 ) ;
#2120=AXIS2_PLACEMENT_3D ( 'NONE', #13185, #3705, #9809 ) ;
#2123=ORIENTED_EDGE ( 'NONE', *, *, #10480, .T. ) ;
#2126=EDGE_CURVE ( 'NONE', #10256, #4318, #9792, .T. ) ;
#2131=ORIENTED_EDGE ( 'NONE', *, *, #9016, .F. ) ;
#2135=CARTESIAN_POINT ( 'NONE',  ( -0.3294846884549019750, -0.2952755905511811330, 0.2675111804726950648 ) ) ;
#2136=VECTOR ( 'NONE', #12914, 39.37007874015748143 ) ;
#2137=PLANE ( 'NONE',  #13354 ) ;
#2140=DIRECTION ( 'NONE',  ( 0.000000000000000000, 0.000000000000000000, -1.000000000000000000 ) ) ;
#2142=ORIENTED_EDGE ( 'NONE', *, *, #12322, .T. ) ;
#2146=AXIS2_PLACEMENT_3D ( 'NONE', #774, #418, #9164 ) ;
#2148=AXIS2_PLACEMENT_3D ( 'NONE', #2561, #14558, #8604 ) ;
#2151=CIRCLE ( 'NONE', #10901, 0.003937007874015724558 ) ;
#2153=ORIENTED_EDGE ( 'NONE', *, *, #7341, .T. ) ;
#2155=ORIENTED_EDGE ( 'NONE', *, *, #2493, .T. ) ;
#2156=EDGE_LOOP ( 'NONE', ( #8278, #14220, #11687 ) ) ;
#2160=DIRECTION ( 'NONE',  ( 0.5000000000000008882, 0.000000000000000000, -0.8660254037844381525 ) ) ;
#2161=VECTOR ( 'NONE', #11412, 39.37007874015748143 ) ;
#2165=CARTESIAN_POINT ( 'NONE',  ( -0.1724006475077544398, -0.4881889763779528324, 0.1768186671464649917 ) ) ;
#2167=CARTESIAN_POINT ( 'NONE',  ( -0.06692913385815749128, -0.09842519685039370636, -0.2377126739438355507 ) ) ;
#2168=CARTESIAN_POINT ( 'NONE',  ( -0.1062992125983150127, -0.4881889763779528324, -0.2482618547482104143 ) ) ;
#2170=CARTESIAN_POINT ( 'NONE',  ( -0.5576140732134202693, -0.4881889763779528324, 0.2082870074805209248 ) ) ;
#2173=ORIENTED_EDGE ( 'NONE', *, *, #7896, .F. ) ;
#2174=ORIENTED_EDGE ( 'NONE', *, *, #11214, .F. ) ;
#2176=EDGE_LOOP ( 'NONE', ( #9345, #13334 ) ) ;
#2177=EDGE_CURVE ( 'NONE', #9678, #8145, #5568, .T. ) ;
#2180=LINE ( 'NONE', #5686, #4114 ) ;
#2182=EDGE_CURVE ( 'NONE', #13463, #14839, #9592, .T. ) ;
#2186=LINE ( 'NONE', #5761, #10407 ) ;
#2188=CARTESIAN_POINT ( 'NONE',  ( 0.06692913385832212347, -0.09842519685039370636, -0.5870514566507987197 ) ) ;
#2190=DIRECTION ( 'NONE',  ( -1.000000000000000000, 0.000000000000000000, 0.000000000000000000 ) ) ;
#2193=ORIENTED_EDGE ( 'NONE', *, *, #5100, .T. ) ;
#2196=AXIS2_PLACEMENT_3D ( 'NONE', #13193, #334, #11049 ) ;
#2197=LINE ( 'NONE', #10261, #11112 ) ;
#2198=DIRECTION ( 'NONE',  ( 0.000000000000000000, 0.000000000000000000, -1.000000000000000000 ) ) ;
#2199=EDGE_CURVE ( 'NONE', #6983, #12059, #6012, .T. ) ;
#2201=DIRECTION ( 'NONE',  ( 0.000000000000000000, 0.000000000000000000, 1.000000000000000000 ) ) ;
#2204=ORIENTED_EDGE ( 'NONE', *, *, #7281, .F. ) ;
#2205=FACE_OUTER_BOUND ( 'NONE', #5564, .T. ) ;
#2207=AXIS2_PLACEMENT_3D ( 'NONE', #6804, #13014, #3380 ) ;
#2211=CARTESIAN_POINT ( 'NONE',  ( 0.000000000000000000, 2.165354330708661568, 0.000000000000000000 ) ) ;
#2212=ORIENTED_EDGE ( 'NONE', *, *, #14769, .F. ) ;
#2214=CIRCLE ( 'NONE', #10964, 0.003937007874015749712 ) ;
#2215=SPHERICAL_SURFACE ( 'NONE', #1094, 0.003937007874015747977 ) ;
#2216=DIRECTION ( 'NONE',  ( -0.5000000000000000000, -0.000000000000000000, -0.8660254037844388186 ) ) ;
#2217=ADVANCED_FACE ( 'NONE', ( #12001 ), #1088, .T. ) ;
#2219=CARTESIAN_POINT ( 'NONE',  ( 0.06692913385832208184, -0.2952755905511811330, -0.4190977005962941426 ) ) ;
#2220=CYLINDRICAL_SURFACE ( 'NONE', #1940, 0.003937007874015724558 ) ;
#2225=DIRECTION ( 'NONE',  ( 1.000000000000000000, 0.000000000000000000, 3.614007241618347785E-16 ) ) ;
#2226=CARTESIAN_POINT ( 'NONE',  ( -0.4591888763630546655, -0.4881889763779528324, 0.3787644491703233141 ) ) ;
#2228=LINE ( 'NONE', #15155, #15436 ) ;
#2230=VERTEX_POINT ( 'NONE', #9072 ) ;
#2234=EDGE_LOOP ( 'NONE', ( #13282, #1241, #11772 ) ) ;
#2236=CARTESIAN_POINT ( 'NONE',  ( -0.06692913385815749128, -0.1023622047244094474, -0.2377126739438355507 ) ) ;
#2238=EDGE_CURVE ( 'NONE', #9448, #2526, #2885, .T. ) ;
#2241=EDGE_CURVE ( 'NONE', #13020, #13305, #5814, .T. ) ;
#2246=ORIENTED_EDGE ( 'NONE', *, *, #4659, .F. ) ;
#2248=ORIENTED_EDGE ( 'NONE', *, *, #10262, .F. ) ;
#2250=CARTESIAN_POINT ( 'NONE',  ( 0.000000000000000000, -0.1023622047244094474, 0.1574803149606299191 ) ) ;
#2256=ORIENTED_EDGE ( 'NONE', *, *, #8742, .F. ) ;
#2258=EDGE_CURVE ( 'NONE', #12255, #241, #10092, .T. ) ;
#2259=CARTESIAN_POINT ( 'NONE',  ( -0.1657884745773953172, -0.4881889763779528324, 0.2093696482190284536 ) ) ;
#2261=EDGE_CURVE ( 'NONE', #3506, #5709, #5462, .T. ) ;
#2262=VERTEX_POINT ( 'NONE', #6483 ) ;
#2267=DIRECTION ( 'NONE',  ( -3.973232667114494807E-16, 0.000000000000000000, 1.000000000000000000 ) ) ;
#2268=CARTESIAN_POINT ( 'NONE',  ( -0.5905511811023629321, -0.09448818897637796532, 0.1591122789105256785 ) ) ;
#2269=CARTESIAN_POINT ( 'NONE',  ( 1.904470415996868375E-17, 2.165354330708661568, -0.1535433070866141780 ) ) ;
#2273=FACE_OUTER_BOUND ( 'NONE', #2528, .T. ) ;
#2274=DIRECTION ( 'NONE',  ( 0.8660254037844405950, -3.174764303743830077E-15, -0.4999999999999967248 ) ) ;
#2276=EDGE_LOOP ( 'NONE', ( #15148, #7530, #11805, #12924 ) ) ;
#2284=DIRECTION ( 'NONE',  ( 0.4999999999999966693, 0.000000000000000000, -0.8660254037844405950 ) ) ;
#2286=CARTESIAN_POINT ( 'NONE',  ( -0.2647411304678976007, -0.4881889763779528324, 0.03404161279859290595 ) ) ;
#2290=ORIENTED_EDGE ( 'NONE', *, *, #11903, .T. ) ;
#2293=DIRECTION ( 'NONE',  ( 0.4999999999999949485, 0.000000000000000000, -0.8660254037844415942 ) ) ;
#2295=CARTESIAN_POINT ( 'NONE',  ( 0.09842519685044820443, -0.4881889763779528324, -0.5870514566507987197 ) ) ;
#2296=ORIENTED_EDGE ( 'NONE', *, *, #11860, .F. ) ;
#2300=EDGE_CURVE ( 'NONE', #8494, #8120, #93, .T. ) ;
#2301=LINE ( 'NONE', #4885, #6328 ) ;
#2303=DIRECTION ( 'NONE',  ( 0.4999999999999930056, 0.000000000000000000, 0.8660254037844428154 ) ) ;
#2305=FACE_OUTER_BOUND ( 'NONE', #13155, .T. ) ;
#2306=DIRECTION ( 'NONE',  ( -1.224646799147358384E-16, 0.000000000000000000, -1.000000000000000000 ) ) ;
#2307=FACE_OUTER_BOUND ( 'NONE', #13019, .T. ) ;
#2309=ORIENTED_EDGE ( 'NONE', *, *, #12865, .F. ) ;
#2310=ORIENTED_EDGE ( 'NONE', *, *, #15243, .F. ) ;
#2315=DIRECTION ( 'NONE',  ( 0.000000000000000000, 0.000000000000000000, 1.000000000000000000 ) ) ;
#2317=CARTESIAN_POINT ( 'NONE',  ( -0.2681506793016946166, -0.1023622047244094474, 0.03207310886158502850 ) ) ;
#2319=CARTESIAN_POINT ( 'NONE',  ( -0.3137366569588388998, -0.2952755905511811330, 0.2947875711430708590 ) ) ;
#2322=VECTOR ( 'NONE', #11017, 39.37007874015748143 ) ;
#2324=CARTESIAN_POINT ( 'NONE',  ( -0.5379290338433416752, -0.1023622047244094474, 0.2423824958184911116 ) ) ;
#2325=VECTOR ( 'NONE', #3957, 39.37007874015748143 ) ;
#2326=ORIENTED_EDGE ( 'NONE', *, *, #359, .F. ) ;
#2327=ADVANCED_FACE ( 'NONE', ( #6630 ), #7569, .F. ) ;
#2329=ADVANCED_FACE ( 'NONE', ( #1641 ), #6400, .F. ) ;
#2331=AXIS2_PLACEMENT_3D ( 'NONE', #3037, #12593, #1861 ) ;
#2332=AXIS2_PLACEMENT_3D ( 'NONE', #4036, #686, #11080 ) ;
#2335=EDGE_CURVE ( 'NONE', #3128, #6177, #4588, .T. ) ;
#2338=LINE ( 'NONE', #12061, #10622 ) ;
#2345=VECTOR ( 'NONE', #12663, 39.37007874015748143 ) ;
#2347=CARTESIAN_POINT ( 'NONE',  ( -0.05905511811012585655, -0.1023622047244094474, -0.5909884645248143498 ) ) ;
#2351=AXIS2_PLACEMENT_3D ( 'NONE', #740, #9111, #12492 ) ;
#2353=EDGE_LOOP ( 'NONE', ( #13730, #3537, #6665 ) ) ;
#2358=AXIS2_PLACEMENT_3D ( 'NONE', #12701, #11762, #10566 ) ;
#2359=VECTOR ( 'NONE', #9410, 39.37007874015748143 ) ;
#2362=CARTESIAN_POINT ( 'NONE',  ( -0.09842519685028340570, -0.1023622047244094474, -0.5870514566507987197 ) ) ;
#2363=AXIS2_PLACEMENT_3D ( 'NONE', #10903, #7520, #7289 ) ;
#2364=FACE_OUTER_BOUND ( 'NONE', #11745, .T. ) ;
#2367=VERTEX_POINT ( 'NONE', #6868 ) ;
#2370=CARTESIAN_POINT ( 'NONE',  ( 0.5629921259842255443, -0.4881889763779528324, 0.2068459625837324456 ) ) ;
#2372=FACE_OUTER_BOUND ( 'NONE', #13231, .T. ) ;
#2373=VECTOR ( 'NONE', #13666, 39.37007874015748143 ) ;
#2374=AXIS2_PLACEMENT_3D ( 'NONE', #4256, #8891, #13670 ) ;
#2375=AXIS2_PLACEMENT_3D ( 'NONE', #6022, #4944, #5958 ) ;
#2377=ORIENTED_EDGE ( 'NONE', *, *, #3447, .T. ) ;
#2379=AXIS2_PLACEMENT_3D ( 'NONE', #7897, #6304, #11101 ) ;
#2381=ORIENTED_EDGE ( 'NONE', *, *, #14521, .T. ) ;
#2383=CARTESIAN_POINT ( 'NONE',  ( 0.06299212598430636856, -0.2952755905511811330, -0.4190977005962941426 ) ) ;
#2384=DIRECTION ( 'NONE',  ( -0.5000000000000004441, 0.000000000000000000, 0.8660254037844384856 ) ) ;
#2385=CARTESIAN_POINT ( 'NONE',  ( 0.4121618538092042816, -0.2952755905511811330, 0.1243101294532687889 ) ) ;
#2387=AXIS2_PLACEMENT_3D ( 'NONE', #11988, #154, #1173 ) ;
#2388=DIRECTION ( 'NONE',  ( -0.8660254037844427044, 0.000000000000000000, 0.4999999999999929501 ) ) ;
#2390=CIRCLE ( 'NONE', #397, 0.04330708661417331101 ) ;
#2393=CARTESIAN_POINT ( 'NONE',  ( -0.5860051159906336515, -0.003937007874015747977, 0.1591122789105256785 ) ) ;
#2397=ORIENTED_EDGE ( 'NONE', *, *, #1089, .F. ) ;
#2401=VECTOR ( 'NONE', #12556, 39.37007874015748143 ) ;
#2409=FACE_OUTER_BOUND ( 'NONE', #1037, .T. ) ;
#2411=AXIS2_PLACEMENT_3D ( 'NONE', #285, #12041, #7314 ) ;
#2412=PLANE ( 'NONE',  #2387 ) ;
#2413=ADVANCED_FACE ( 'NONE', ( #12979 ), #3587, .T. ) ;
#2414=ORIENTED_EDGE ( 'NONE', *, *, #13531, .F. ) ;
#2415=DIRECTION ( 'NONE',  ( 0.5000000000000069944, 0.000000000000000000, -0.8660254037844347108 ) ) ;
#2416=CARTESIAN_POINT ( 'NONE',  ( 0.1062992125984796865, -0.1023622047244094474, -0.5870514566507987197 ) ) ;
#2418=AXIS2_PLACEMENT_3D ( 'NONE', #8799, #510, #7854 ) ;
#2419=ORIENTED_EDGE ( 'NONE', *, *, #454, .F. ) ;
#2421=VERTEX_POINT ( 'NONE', #11802 ) ;
#2423=AXIS2_PLACEMENT_3D ( 'NONE', #3713, #10758, #9676 ) ;
#2424=LINE ( 'NONE', #1183, #9399 ) ;
#2425=VECTOR ( 'NONE', #14502, 39.37007874015748143 ) ;
#2426=EDGE_CURVE ( 'NONE', #5050, #2901, #10925, .T. ) ;
#2433=ORIENTED_EDGE ( 'NONE', *, *, #9553, .F. ) ;
#2435=DIRECTION ( 'NONE',  ( -0.8660254037844385966, 0.000000000000000000, -0.5000000000000002220 ) ) ;
#2437=AXIS2_PLACEMENT_3D ( 'NONE', #14034, #1979, #965 ) ;
#2438=PLANE ( 'NONE',  #11723 ) ;
#2441=ADVANCED_FACE ( 'NONE', ( #10771 ), #5061, .T. ) ;
#2442=AXIS2_PLACEMENT_3D ( 'NONE', #2188, #4525, #9308 ) ;
#2445=CYLINDRICAL_SURFACE ( 'NONE', #11895, 0.003937007874015737569 ) ;
#2449=CARTESIAN_POINT ( 'NONE',  ( 0.5413385826772204590, -0.1023622047244094474, 0.2443509997555466662 ) ) ;
#2450=CARTESIAN_POINT ( 'NONE',  ( 0.09842519685044820443, -0.4921259842519685179, -0.5870514566507987197 ) ) ;
#2451=CIRCLE ( 'NONE', #4942, 0.003937007874015754916 ) ;
#2452=DIRECTION ( 'NONE',  ( 0.5000000000000035527, 0.000000000000000000, -0.8660254037844365982 ) ) ;
#2454=VERTEX_POINT ( 'NONE', #5113 ) ;
#2455=FACE_OUTER_BOUND ( 'NONE', #13676, .T. ) ;
#2456=FACE_OUTER_BOUND ( 'NONE', #8094, .T. ) ;
#2458=EDGE_CURVE ( 'NONE', #8212, #13463, #7079, .T. ) ;
#2460=EDGE_CURVE ( 'NONE', #7138, #13559, #8800, .T. ) ;
#2461=AXIS2_PLACEMENT_3D ( 'NONE', #6327, #12247, #11042 ) ;
#2463=ORIENTED_EDGE ( 'NONE', *, *, #10759, .T. ) ;
#2464=VERTEX_POINT ( 'NONE', #8890 ) ;
#2465=CIRCLE ( 'NONE', #11210, 0.003937007874015750579 ) ;
#2467=EDGE_CURVE ( 'NONE', #6881, #1627, #11074, .T. ) ;
#2468=DIRECTION ( 'NONE',  ( 0.4999999999999966693, 0.000000000000000000, -0.8660254037844405950 ) ) ;
#2469=PLANE ( 'NONE',  #8600 ) ;
#2472=AXIS2_PLACEMENT_3D ( 'NONE', #6545, #11340, #11429 ) ;
#2473=LINE ( 'NONE', #5983, #13602 ) ;
#2474=CARTESIAN_POINT ( 'NONE',  ( -0.1023622047242992716, -0.1023622047244094474, -0.2482618547482104143 ) ) ;
#2475=DIRECTION ( 'NONE',  ( 0.000000000000000000, 1.000000000000000000, 0.000000000000000000 ) ) ;
#2476=CARTESIAN_POINT ( 'NONE',  ( 0.2681506793018588186, -0.4921259842519685179, 0.03207310886168001501 ) ) ;
#2480=ORIENTED_EDGE ( 'NONE', *, *, #8707, .F. ) ;
#2481=ADVANCED_FACE ( 'NONE', ( #9829 ), #12855, .T. ) ;
#2483=DIRECTION ( 'NONE',  ( -0.000000000000000000, 1.000000000000000000, -0.000000000000000000 ) ) ;
#2485=CARTESIAN_POINT ( 'NONE',  ( 0.1552072824047652233, -0.09448818897637796532, -0.5870514566507987197 ) ) ;
#2487=CARTESIAN_POINT ( 'NONE',  ( -0.1586168312385622670, -0.09842519685039370636, -0.5890199605878064792 ) ) ;
#2488=DIRECTION ( 'NONE',  ( 0.000000000000000000, 0.000000000000000000, 1.000000000000000000 ) ) ;
#2490=ORIENTED_EDGE ( 'NONE', *, *, #2629, .F. ) ;
#2492=EDGE_LOOP ( 'NONE', ( #11115, #12466, #12355, #2600 ) ) ;
#2493=EDGE_CURVE ( 'NONE', #9186, #12161, #8734, .T. ) ;
#2494=DIRECTION ( 'NONE',  ( -0.000000000000000000, 1.000000000000000000, -0.000000000000000000 ) ) ;
#2502=ORIENTED_EDGE ( 'NONE', *, *, #15099, .T. ) ;
#2503=DIRECTION ( 'NONE',  ( 1.000000000000000000, 0.000000000000000000, 0.000000000000000000 ) ) ;
#2504=CARTESIAN_POINT ( 'NONE',  ( 0.000000000000000000, 0.000000000000000000, 0.000000000000000000 ) ) ;
#2509=ORIENTED_EDGE ( 'NONE', *, *, #13243, .T. ) ;
#2510=ADVANCED_FACE ( 'NONE', ( #11154, #7397 ), #3795, .F. ) ;
#2511=DIRECTION ( 'NONE',  ( 0.4999999999999981681, -0.000000000000000000, 0.8660254037844397068 ) ) ;
#2512=CARTESIAN_POINT ( 'NONE',  ( -0.4586614173228359959, -0.09448818897637796532, 0.3875520507749251053 ) ) ;
#2515=FACE_OUTER_BOUND ( 'NONE', #2899, .T. ) ;
#2519=ORIENTED_EDGE ( 'NONE', *, *, #8122, .F. ) ;
#2524=ORIENTED_EDGE ( 'NONE', *, *, #15389, .F. ) ;
#2526=VERTEX_POINT ( 'NONE', #7623 ) ;
#2528=EDGE_LOOP ( 'NONE', ( #8776, #9819, #15272, #2131 ) ) ;
#2529=DIRECTION ( 'NONE',  ( 0.8660254037844385966, 0.000000000000000000, 0.5000000000000001110 ) ) ;
#2530=EDGE_CURVE ( 'NONE', #11605, #13986, #11065, .T. ) ;
#2531=CARTESIAN_POINT ( 'NONE',  ( -0.09842519685028337795, -0.2952755905511811330, -0.3797276218561366767 ) ) ;
#2532=DIRECTION ( 'NONE',  ( -0.000000000000000000, 1.000000000000000000, 0.000000000000000000 ) ) ;
#2537=CYLINDRICAL_SURFACE ( 'NONE', #6861, 0.003937007874015757518 ) ;
#2538=EDGE_CURVE ( 'NONE', #4047, #9540, #13979, .T. ) ;
#2539=DIRECTION ( 'NONE',  ( -0.000000000000000000, -1.000000000000000000, -0.000000000000000000 ) ) ;
#2545=FACE_OUTER_BOUND ( 'NONE', #3111, .T. ) ;
#2549=LINE ( 'NONE', #371, #9330 ) ;
#2552=CARTESIAN_POINT ( 'NONE',  ( -0.1062992125983148878, -0.09842519685039370636, -0.5870514566507987197 ) ) ;
#2553=ADVANCED_FACE ( 'NONE', ( #14929 ), #11861, .T. ) ;
#2561=CARTESIAN_POINT ( 'NONE',  ( 0.4141303577462121521, -0.2952755905511811330, 0.1209005806194717869 ) ) ;
#2564=LINE ( 'NONE', #4993, #10853 ) ;
#2567=CARTESIAN_POINT ( 'NONE',  ( 0.03357817649489055339, -0.2952755905511811330, 0.7012961359976183084 ) ) ;
#2570=CYLINDRICAL_SURFACE ( 'NONE', #8198, 0.03937007874015759773 ) ;
#2572=DIRECTION ( 'NONE',  ( 0.000000000000000000, -1.000000000000000000, 0.000000000000000000 ) ) ;
#2573=DIRECTION ( 'NONE',  ( -1.000000000000000000, 0.000000000000000000, 0.000000000000000000 ) ) ;
#2574=VERTEX_POINT ( 'NONE', #6589 ) ;
#2576=AXIS2_PLACEMENT_3D ( 'NONE', #1945, #7970, #12820 ) ;
#2577=VECTOR ( 'NONE', #7488, 39.37007874015748854 ) ;
#2578=AXIS2_PLACEMENT_3D ( 'NONE', #6052, #6427, #1744 ) ;
#2580=ORIENTED_EDGE ( 'NONE', *, *, #10746, .F. ) ;
#2581=CARTESIAN_POINT ( 'NONE',  ( -0.1062992125983148878, -0.09448818897637796532, -0.5909884645248143498 ) ) ;
#2583=CARTESIAN_POINT ( 'NONE',  ( 0.09842519685044796851, -0.4921259842519685179, 3.910662073933746312E-17 ) ) ;
#2585=DIRECTION ( 'NONE',  ( -0.8660254037844347108, 0.000000000000000000, -0.5000000000000069944 ) ) ;
#2586=DIRECTION ( 'NONE',  ( 0.000000000000000000, 0.000000000000000000, -1.000000000000000000 ) ) ;
#2588=DIRECTION ( 'NONE',  ( 0.8660254037844249408, 0.000000000000000000, -0.5000000000000236478 ) ) ;
#2589=ORIENTED_EDGE ( 'NONE', *, *, #4787, .F. ) ;
#2590=FACE_BOUND ( 'NONE', #7749, .T. ) ;
#2592=DIRECTION ( 'NONE',  ( 0.8660254037844385966, 0.000000000000000000, 0.5000000000000000000 ) ) ;
#2593=VECTOR ( 'NONE', #14677, 39.37007874015748143 ) ;
#2594=DIRECTION ( 'NONE',  ( -0.8660254037844390407, 0.000000000000000000, 0.4999999999999994449 ) ) ;
#2596=EDGE_CURVE ( 'NONE', #8551, #8, #14356, .T. ) ;
#2598=ORIENTED_EDGE ( 'NONE', *, *, #9520, .F. ) ;
#2600=ORIENTED_EDGE ( 'NONE', *, *, #5754, .T. ) ;
#2601=VECTOR ( 'NONE', #10769, 39.37007874015748143 ) ;
#2603=AXIS2_PLACEMENT_3D ( 'NONE', #15323, #5911, #6768 ) ;
#2604=EDGE_LOOP ( 'NONE', ( #7424, #14538, #9077, #7840 ) ) ;
#2605=CIRCLE ( 'NONE', #12123, 0.003937007874015724558 ) ;
#2609=AXIS2_PLACEMENT_3D ( 'NONE', #14208, #5794, #3477 ) ;
#2616=EDGE_CURVE ( 'NONE', #3033, #9504, #7091, .T. ) ;
#2617=CARTESIAN_POINT ( 'NONE',  ( -0.4783464566929145900, -0.4921259842519685179, 0.3534565624369550574 ) ) ;
#2619=DIRECTION ( 'NONE',  ( -1.060575238724906792E-16, 1.000000000000000000, -6.123233995736767268E-17 ) ) ;
#2621=CIRCLE ( 'NONE', #4862, 0.003937007874015745375 ) ;
#2623=EDGE_CURVE ( 'NONE', #11872, #12443, #8603, .T. ) ;
#2624=AXIS2_PLACEMENT_3D ( 'NONE', #3618, #7285, #1271 ) ;
#2627=AXIS2_PLACEMENT_3D ( 'NONE', #10033, #12618, #5235 ) ;
#2629=EDGE_CURVE ( 'NONE', #6774, #6775, #842, .T. ) ;
#2632=AXIS2_PLACEMENT_3D ( 'NONE', #9090, #3142, #867 ) ;
#2635=CARTESIAN_POINT ( 'NONE',  ( 0.3669897256266698715, -0.2952755905511811330, 0.2891647237797818626 ) ) ;
#2638=DIRECTION ( 'NONE',  ( -0.8660254037844347108, 0.000000000000000000, -0.5000000000000069944 ) ) ;
#2641=DIRECTION ( 'NONE',  ( -0.4999999999999998335, 0.000000000000000000, -0.8660254037844388186 ) ) ;
#2648=EDGE_CURVE ( 'NONE', #9446, #5934, #3849, .T. ) ;
#2650=CIRCLE ( 'NONE', #4657, 0.04330708661417328326 ) ;
#2654=EDGE_CURVE ( 'NONE', #10930, #4497, #1592, .T. ) ;
#2655=AXIS2_PLACEMENT_3D ( 'NONE', #14688, #2762, #1984 ) ;
#2657=DIRECTION ( 'NONE',  ( -3.973232667114495301E-16, 0.000000000000000000, 1.000000000000000000 ) ) ;
#2659=DIRECTION ( 'NONE',  ( 0.000000000000000000, 1.000000000000000000, 0.000000000000000000 ) ) ;
#2660=LINE ( 'NONE', #2567, #12447 ) ;
#2666=DIRECTION ( 'NONE',  ( -0.000000000000000000, -0.000000000000000000, -1.000000000000000000 ) ) ;
#2669=ORIENTED_EDGE ( 'NONE', *, *, #15399, .F. ) ;
#2670=AXIS2_PLACEMENT_3D ( 'NONE', #3710, #329, #5967 ) ;
#2671=DIRECTION ( 'NONE',  ( 0.8660254037844347108, 0.000000000000000000, 0.5000000000000069944 ) ) ;
#2672=EDGE_CURVE ( 'NONE', #8847, #7384, #7339, .T. ) ;
#2673=TOROIDAL_SURFACE ( 'NONE', #11436, 0.1614173228346456879, 0.003937007874015747977 ) ;
#2679=AXIS2_PLACEMENT_3D ( 'NONE', #10602, #14287, #14054 ) ;
#2681=VERTEX_POINT ( 'NONE', #7456 ) ;
#2683=CARTESIAN_POINT ( 'NONE',  ( 0.2393297813660762718, -0.09842519685039370636, 0.06089400679746260342 ) ) ;
#2684=VECTOR ( 'NONE', #1954, 39.37007874015748143 ) ;
#2685=CARTESIAN_POINT ( 'NONE',  ( 0.000000000000000000, -0.4921259842519685179, 0.000000000000000000 ) ) ;
#2687=ORIENTED_EDGE ( 'NONE', *, *, #4030, .T. ) ;
#2688=ORIENTED_EDGE ( 'NONE', *, *, #11656, .F. ) ;
#2692=CARTESIAN_POINT ( 'NONE',  ( 0.09842519685044813504, -0.2952755905511811330, -0.3797276218561366212 ) ) ;
#2699=DIRECTION ( 'NONE',  ( 0.8660254037844385966, 0.000000000000000000, -0.4999999999999998890 ) ) ;
#2702=EDGE_CURVE ( 'NONE', #6685, #12009, #3781, .T. ) ;
#2703=CARTESIAN_POINT ( 'NONE',  ( 0.09842519685044814892, -0.2952755905511811330, -0.4190977005962941426 ) ) ;
#2705=AXIS2_PLACEMENT_3D ( 'NONE', #10539, #12018, #9667 ) ;
#2706=DIRECTION ( 'NONE',  ( 0.8660254037844385966, -0.000000000000000000, 0.5000000000000001110 ) ) ;
#2708=ORIENTED_EDGE ( 'NONE', *, *, #5284, .F. ) ;
#2712=CIRCLE ( 'NONE', #1218, 0.03937007874015751446 ) ;
#2714=CARTESIAN_POINT ( 'NONE',  ( -0.4496668909809726777, -0.2952755905511811330, 0.1459636727603558504 ) ) ;
#2719=ADVANCED_FACE ( 'NONE', ( #5240, #10039 ), #8547, .F. ) ;
#2726=ORIENTED_EDGE ( 'NONE', *, *, #14605, .F. ) ;
#2727=ORIENTED_EDGE ( 'NONE', *, *, #5996, .F. ) ;
#2728=VERTEX_POINT ( 'NONE', #13414 ) ;
#2732=CARTESIAN_POINT ( 'NONE',  ( -0.5084014747882513729, -0.4881889763779528324, 0.2935257283253980831 ) ) ;
#2734=CARTESIAN_POINT ( 'NONE',  ( 0.000000000000000000, -0.4921259842519685179, 0.1574803149606299191 ) ) ;
#2740=VERTEX_POINT ( 'NONE', #4162 ) ;
#2746=VERTEX_POINT ( 'NONE', #13795 ) ;
#2748=CARTESIAN_POINT ( 'NONE',  ( 0.1017691531708310448, -0.2952755905511811330, 0.7406662147377752747 ) ) ;
#2752=ORIENTED_EDGE ( 'NONE', *, *, #14129, .T. ) ;
#2753=CARTESIAN_POINT ( 'NONE',  ( 1.976792077363838002E-17, 5.629100846319917971E-17, 0.1614173228346456879 ) ) ;
#2762=DIRECTION ( 'NONE',  ( -0.000000000000000000, 0.000000000000000000, 1.000000000000000000 ) ) ;
#2775=DIRECTION ( 'NONE',  ( -0.8660254037844398178, 0.000000000000000000, 0.4999999999999979461 ) ) ;
#2777=( NAMED_UNIT ( * ) SI_UNIT ( $, .STERADIAN. ) SOLID_ANGLE_UNIT ( ) );
#2782=EDGE_CURVE ( 'NONE', #5753, #3506, #4392, .T. ) ;
#2783=DIRECTION ( 'NONE',  ( -1.000000000000000000, 0.000000000000000000, 0.000000000000000000 ) ) ;
#2784=LINE ( 'NONE', #10947, #1655 ) ;
#2802=EDGE_CURVE ( 'NONE', #11638, #14035, #5331, .T. ) ;
#2805=EDGE_CURVE ( 'NONE', #8036, #7766, #9255, .T. ) ;
#2807=ORIENTED_EDGE ( 'NONE', *, *, #11515, .T. ) ;
#2810=ORIENTED_EDGE ( 'NONE', *, *, #7321, .F. ) ;
#2812=FACE_OUTER_BOUND ( 'NONE', #6071, .T. ) ;
#2817=DIRECTION ( 'NONE',  ( 0.000000000000000000, 0.000000000000000000, -1.000000000000000000 ) ) ;
#2820=CIRCLE ( 'NONE', #11319, 0.003937007874015721089 ) ;
#2822=VECTOR ( 'NONE', #5047, 39.37007874015748143 ) ;
#2823=CARTESIAN_POINT ( 'NONE',  ( -0.2652685895081163259, -0.4921259842519685179, 0.03495519865516327068 ) ) ;
#2824=AXIS2_PLACEMENT_3D ( 'NONE', #5816, #10618, #51 ) ;
#2827=ORIENTED_EDGE ( 'NONE', *, *, #8540, .F. ) ;
#2831=AXIS2_PLACEMENT_3D ( 'NONE', #9774, #6219, #10938 ) ;
#2836=FACE_OUTER_BOUND ( 'NONE', #8922, .T. ) ;
#2840=LINE ( 'NONE', #435, #6092 ) ;
#2843=CARTESIAN_POINT ( 'NONE',  ( 0.1552072824047652233, -0.003937007874015747977, -0.5870514566507987197 ) ) ;
#2844=CIRCLE ( 'NONE', #1857, 0.003937007874015747977 ) ;
#2848=DIRECTION ( 'NONE',  ( 1.000000000000000000, 0.000000000000000000, 0.000000000000000000 ) ) ;
#2850=ORIENTED_EDGE ( 'NONE', *, *, #1570, .T. ) ;
#2851=TOROIDAL_SURFACE ( 'NONE', #2351, 0.007874015748031495954, 0.003937007874015747977 ) ;
#2856=AXIS2_PLACEMENT_3D ( 'NONE', #9512, #13321, #2588 ) ;
#2860=AXIS2_PLACEMENT_3D ( 'NONE', #13789, #12841, #8056 ) ;
#2862=DIRECTION ( 'NONE',  ( 0.000000000000000000, 0.000000000000000000, 1.000000000000000000 ) ) ;
#2863=CIRCLE ( 'NONE', #7616, 0.003937007874015741038 ) ;
#2868=VERTEX_POINT ( 'NONE', #7920 ) ;
#2870=CIRCLE ( 'NONE', #14148, 0.003937007874015758385 ) ;
#2872=CIRCLE ( 'NONE', #11642, 0.003937007874015724558 ) ;
#2875=ORIENTED_EDGE ( 'NONE', *, *, #6322, .T. ) ;
#2879=CARTESIAN_POINT ( 'NONE',  ( -0.5860051159906336515, -0.09842519685039370636, 0.1591122789105256785 ) ) ;
#2883=DIRECTION ( 'NONE',  ( 0.8660254037844405950, 2.369676336725575161E-14, -0.4999999999999967804 ) ) ;
#2885=LINE ( 'NONE', #8837, #7568 ) ;
#2886=AXIS2_PLACEMENT_3D ( 'NONE', #5358, #10389, #4203 ) ;
#2890=AXIS2_PLACEMENT_3D ( 'NONE', #2135, #2216, #8174 ) ;
#2891=ORIENTED_EDGE ( 'NONE', *, *, #4816, .F. ) ;
#2894=ADVANCED_FACE ( 'NONE', ( #10574 ), #5866, .T. ) ;
#2899=EDGE_LOOP ( 'NONE', ( #2580, #2204, #14160, #2173 ) ) ;
#2901=VERTEX_POINT ( 'NONE', #12847 ) ;
#2902=AXIS2_PLACEMENT_3D ( 'NONE', #9374, #5989, #920 ) ;
#2905=TOROIDAL_SURFACE ( 'NONE', #2418, 0.04330708661417328326, 0.003937007874015747977 ) ;
#2908=DIRECTION ( 'NONE',  ( 0.000000000000000000, -1.000000000000000000, 0.000000000000000000 ) ) ;
#2913=CYLINDRICAL_SURFACE ( 'NONE', #11163, 0.003937007874015721089 ) ;
#2914=ADVANCED_FACE ( 'NONE', ( #2273 ), #6853, .T. ) ;
#2917=CIRCLE ( 'NONE', #7405, 0.003937007874015758385 ) ;
#2918=DIRECTION ( 'NONE',  ( 0.000000000000000000, 0.000000000000000000, -1.000000000000000000 ) ) ;
#2919=SPHERICAL_SURFACE ( 'NONE', #12347, 0.003937007874015747977 ) ;
#2922=EDGE_LOOP ( 'NONE', ( #3582, #12448, #11039, #6838 ) ) ;
#2925=EDGE_LOOP ( 'NONE', ( #3616, #13200, #7237, #10231 ) ) ;
#2929=ADVANCED_FACE ( 'NONE', ( #960 ), #2119, .T. ) ;
#2931=CARTESIAN_POINT ( 'NONE',  ( -0.5418660417173573052, -0.4921259842519685179, 0.2355633981508970520 ) ) ;
#2933=DIRECTION ( 'NONE',  ( 0.000000000000000000, -1.000000000000000000, -0.000000000000000000 ) ) ;
#2934=CIRCLE ( 'NONE', #6931, 0.003937007874015758385 ) ;
#2936=DIRECTION ( 'NONE',  ( -0.8660254037844427044, 0.000000000000000000, 0.4999999999999929501 ) ) ;
#2938=DIRECTION ( 'NONE',  ( 1.000000000000000000, 0.000000000000000000, 3.476578583725179813E-16 ) ) ;
#2940=FACE_BOUND ( 'NONE', #7783, .T. ) ;
#2946=ORIENTED_EDGE ( 'NONE', *, *, #1468, .F. ) ;
#2948=ORIENTED_EDGE ( 'NONE', *, *, #7727, .T. ) ;
#2950=CARTESIAN_POINT ( 'NONE',  ( -0.1023622047242991467, -0.2952755905511811330, -0.4624047872104675161 ) ) ;
#2952=DIRECTION ( 'NONE',  ( 0.000000000000000000, -1.000000000000000000, 0.000000000000000000 ) ) ;
#2953=DIRECTION ( 'NONE',  ( 0.000000000000000000, 1.000000000000000000, 0.000000000000000000 ) ) ;
#2955=SPHERICAL_SURFACE ( 'NONE', #2886, 0.003937007874015747977 ) ;
#2957=CARTESIAN_POINT ( 'NONE',  ( 0.5398975377803496567, -0.4921259842519685179, 0.2389729469846946508 ) ) ;
#2961=ORIENTED_EDGE ( 'NONE', *, *, #4679, .T. ) ;
#2962=AXIS2_PLACEMENT_3D ( 'NONE', #13728, #7754, #10113 ) ;
#2963=VERTEX_POINT ( 'NONE', #19 ) ;
#2966=CIRCLE ( 'NONE', #6706, 0.003937007874015724558 ) ;
#2969=CARTESIAN_POINT ( 'NONE',  ( 0.000000000000000000, 0.003937007874015860734, 0.000000000000000000 ) ) ;
#2971=CARTESIAN_POINT ( 'NONE',  ( 0.5615510810874363434, -0.1023622047244094474, 0.2014679098129276424 ) ) ;
#2976=EDGE_LOOP ( 'NONE', ( #9926, #13230, #2009, #829 ) ) ;
#2979=VERTEX_POINT ( 'NONE', #4779 ) ;
#2984=ADVANCED_FACE ( 'NONE', ( #9564 ), #12360, .T. ) ;
#2985=CARTESIAN_POINT ( 'NONE',  ( -0.4330708661417336236, -0.003937007874015747977, 0.4318761856142863120 ) ) ;
#2986=FACE_OUTER_BOUND ( 'NONE', #2101, .T. ) ;
#2987=CARTESIAN_POINT ( 'NONE',  ( 0.2642136714278430776, -0.4881889763779528324, 0.03889220652927401906 ) ) ;
#2988=CARTESIAN_POINT ( 'NONE',  ( -0.3964138223131424832, -0.2952755905511811330, 0.1515865201236451798 ) ) ;
#2990=EDGE_LOOP ( 'NONE', ( #967, #4378, #8963 ) ) ;
#2991=DIRECTION ( 'NONE',  ( 0.5000000000000001110, -0.000000000000000000, -0.8660254037844388186 ) ) ;
#2992=DIRECTION ( 'NONE',  ( 1.445602896647339903E-16, 0.000000000000000000, -1.000000000000000000 ) ) ;
#2993=DIRECTION ( 'NONE',  ( 1.000000000000000000, -8.673617379884087537E-15, 1.504632769052536530E-28 ) ) ;
#2995=FACE_OUTER_BOUND ( 'NONE', #2063, .T. ) ;
#2996=EDGE_CURVE ( 'NONE', #10010, #3213, #1262, .T. ) ;
#2997=ADVANCED_FACE ( 'NONE', ( #3607 ), #5593, .T. ) ;
#3001=EDGE_CURVE ( 'NONE', #13986, #7182, #8239, .T. ) ;
#3004=CARTESIAN_POINT ( 'NONE',  ( 0.2681506793018588186, -0.1023622047244094474, 0.03207310886168000114 ) ) ;
#3006=DIRECTION ( 'NONE',  ( 0.000000000000000000, 0.000000000000000000, -1.000000000000000000 ) ) ;
#3007=DIRECTION ( 'NONE',  ( 0.000000000000000000, 0.000000000000000000, -1.000000000000000000 ) ) ;
#3009=CARTESIAN_POINT ( 'NONE',  ( 0.1618514667033794374, -0.4881889763779528324, 0.2161887458866224576 ) ) ;
#3011=EDGE_CURVE ( 'NONE', #2963, #3832, #5711, .T. ) ;
#3013=ORIENTED_EDGE ( 'NONE', *, *, #7286, .T. ) ;
#3015=ORIENTED_EDGE ( 'NONE', *, *, #8331, .T. ) ;
#3016=LINE ( 'NONE', #11721, #11627 ) ;
#3017=ORIENTED_EDGE ( 'NONE', *, *, #3386, .F. ) ;
#3018=EDGE_LOOP ( 'NONE', ( #9771, #12351, #5309, #9353 ) ) ;
#3019=EDGE_CURVE ( 'NONE', #12501, #2740, #9621, .T. ) ;
#3026=DIRECTION ( 'NONE',  ( 0.000000000000000000, 0.000000000000000000, 1.000000000000000000 ) ) ;
#3027=CARTESIAN_POINT ( 'NONE',  ( -0.1023622047242992716, -0.4881889763779528324, -0.2482618547482104143 ) ) ;
#3029=CARTESIAN_POINT ( 'NONE',  ( 0.1618514667033794374, -0.4921259842519685179, 0.2161887458866224576 ) ) ;
#3031=EDGE_LOOP ( 'NONE', ( #13988, #787, #14571, #12732 ) ) ;
#3032=ORIENTED_EDGE ( 'NONE', *, *, #5938, .F. ) ;
#3033=VERTEX_POINT ( 'NONE', #7348 ) ;
#3036=DIRECTION ( 'NONE',  ( -0.000000000000000000, 1.000000000000000000, -0.000000000000000000 ) ) ;
#3037=CARTESIAN_POINT ( 'NONE',  ( 0.2330381427387010207, -0.1023622047244094474, 0.06574460052804878551 ) ) ;
#3038=CARTESIAN_POINT ( 'NONE',  ( 0.4307978335858664853, -0.003937007874015747977, 0.4279391777402732910 ) ) ;
#3039=ADVANCED_FACE ( 'NONE', ( #5067 ), #2106, .T. ) ;
#3040=DIRECTION ( 'NONE',  ( -1.000000000000000000, 8.673617379884049672E-15, 0.000000000000000000 ) ) ;
#3044=DIRECTION ( 'NONE',  ( 0.000000000000000000, 0.000000000000000000, 1.000000000000000000 ) ) ;
#3046=CARTESIAN_POINT ( 'NONE',  ( -0.3478321452968090588, -0.2952755905511811330, 0.3144726105131496752 ) ) ;
#3051=EDGE_LOOP ( 'NONE', ( #5544, #7656, #320, #1336 ) ) ;
#3052=AXIS2_PLACEMENT_3D ( 'NONE', #2295, #14057, #9447 ) ;
#3055=DIRECTION ( 'NONE',  ( 0.000000000000000000, 0.000000000000000000, -1.000000000000000000 ) ) ;
#3056=SPHERICAL_SURFACE ( 'NONE', #7459, 0.003937007874015747977 ) ;
#3061=FACE_OUTER_BOUND ( 'NONE', #11521, .T. ) ;
#3062=CARTESIAN_POINT ( 'NONE',  ( -0.5452755905511542656, -0.1023622047244094474, 0.2375319020879049503 ) ) ;
#3066=EDGE_LOOP ( 'NONE', ( #13051, #11162, #10572, #6574 ) ) ;
#3070=DIRECTION ( 'NONE',  ( 0.8660254037844383745, 0.000000000000000000, -0.5000000000000004441 ) ) ;
#3071=CARTESIAN_POINT ( 'NONE',  ( -0.2364476915723336681, -0.4921259842519685179, 0.06377609659094583827 ) ) ;
#3072=AXIS2_PLACEMENT_3D ( 'NONE', #10554, #11816, #1081 ) ;
#3080=DIRECTION ( 'NONE',  ( 0.000000000000000000, 1.000000000000000000, -0.000000000000000000 ) ) ;
#3090=AXIS2_PLACEMENT_3D ( 'NONE', #10434, #14910, #14032 ) ;
#3092=EDGE_CURVE ( 'NONE', #14773, #1163, #12868, .T. ) ;
#3096=DIRECTION ( 'NONE',  ( 0.8660254037844387076, 0.000000000000000000, -0.4999999999999998890 ) ) ;
#3098=CARTESIAN_POINT ( 'NONE',  ( -0.2681506793016945611, -0.4881889763779528324, 0.03207310886158504931 ) ) ;
#3099=AXIS2_PLACEMENT_3D ( 'NONE', #10851, #8437, #14397 ) ;
#3103=EDGE_CURVE ( 'NONE', #8494, #12201, #11615, .T. ) ;
#3104=CARTESIAN_POINT ( 'NONE',  ( 0.06299212598430639631, -0.1023622047244094474, -0.5870514566507987197 ) ) ;
#3106=CIRCLE ( 'NONE', #6335, 0.003937007874015724558 ) ;
#3109=ORIENTED_EDGE ( 'NONE', *, *, #1959, .T. ) ;
#3110=EDGE_LOOP ( 'NONE', ( #14017, #11204, #4700 ) ) ;
#3111=EDGE_LOOP ( 'NONE', ( #6752, #5298, #6491, #14803 ) ) ;
#3118=TOROIDAL_SURFACE ( 'NONE', #13385, 0.04330708661417328326, 0.003937007874015747977 ) ;
#3119=CARTESIAN_POINT ( 'NONE',  ( 0.1724006475077544120, -0.4881889763779528324, 0.1768186671464649640 ) ) ;
#3121=DIRECTION ( 'NONE',  ( 0.8660254037844400399, -0.000000000000000000, 0.4999999999999976130 ) ) ;
#3122=CARTESIAN_POINT ( 'NONE',  ( 0.4749369078591172411, -0.4881889763779528324, 0.3514880584999470203 ) ) ;
#3123=DIRECTION ( 'NONE',  ( 0.000000000000000000, 1.000000000000000000, -0.000000000000000000 ) ) ;
#3125=DIRECTION ( 'NONE',  ( -0.000000000000000000, -1.000000000000000000, -0.000000000000000000 ) ) ;
#3127=VECTOR ( 'NONE', #9816, 39.37007874015748143 ) ;
#3128=VERTEX_POINT ( 'NONE', #6718 ) ;
#3131=ADVANCED_FACE ( 'NONE', ( #12607 ), #1862, .T. ) ;
#3135=VECTOR ( 'NONE', #1663, 39.37007874015748143 ) ;
#3138=FACE_OUTER_BOUND ( 'NONE', #609, .T. ) ;
#3139=DIRECTION ( 'NONE',  ( -1.000000000000000000, 0.000000000000000000, 0.000000000000000000 ) ) ;
#3142=DIRECTION ( 'NONE',  ( 0.000000000000000000, -1.000000000000000000, 0.000000000000000000 ) ) ;
#3143=ORIENTED_EDGE ( 'NONE', *, *, #8258, .F. ) ;
#3150=VECTOR ( 'NONE', #2641, 39.37007874015748143 ) ;
#3151=AXIS2_PLACEMENT_3D ( 'NONE', #2075, #1159, #5819 ) ;
#3154=EDGE_CURVE ( 'NONE', #10586, #8715, #9112, .T. ) ;
#3156=VECTOR ( 'NONE', #5997, 39.37007874015748143 ) ;
#3157=VERTEX_POINT ( 'NONE', #10255 ) ;
#3161=DIRECTION ( 'NONE',  ( 0.5000000000000069944, -7.511572993685774449E-15, -0.8660254037844347108 ) ) ;
#3162=DIRECTION ( 'NONE',  ( 0.000000000000000000, 0.000000000000000000, -1.000000000000000000 ) ) ;
#3164=DIRECTION ( 'NONE',  ( 0.000000000000000000, 0.000000000000000000, 1.000000000000000000 ) ) ;
#3166=CARTESIAN_POINT ( 'NONE',  ( 1.880363195541211833E-17, 2.161417322834645827, -0.1535433070866141780 ) ) ;
#3171=VERTEX_POINT ( 'NONE', #14971 ) ;
#3173=CARTESIAN_POINT ( 'NONE',  ( 0.3746568166374371622, -0.2952755905511811330, 0.1026565861461821993 ) ) ;
#3174=ORIENTED_EDGE ( 'NONE', *, *, #4138, .F. ) ;
#3175=CIRCLE ( 'NONE', #14690, 0.003937007874015721089 ) ;
#3177=ORIENTED_EDGE ( 'NONE', *, *, #9761, .F. ) ;
#3181=DIRECTION ( 'NONE',  ( 0.000000000000000000, 0.000000000000000000, -1.000000000000000000 ) ) ;
#3186=CARTESIAN_POINT ( 'NONE',  ( -0.1657884745773953450, -0.4921259842519685179, 0.2093696482190284258 ) ) ;
#3188=CARTESIAN_POINT ( 'NONE',  ( -0.3314531923919099565, -0.2952755905511811330, 0.2641016316388978824 ) ) ;
#3191=ORIENTED_EDGE ( 'NONE', *, *, #1306, .T. ) ;
#3193=EDGE_CURVE ( 'NONE', #675, #10534, #10625, .T. ) ;
#3195=ORIENTED_EDGE ( 'NONE', *, *, #4032, .F. ) ;
#3196=EDGE_CURVE ( 'NONE', #3157, #1093, #4348, .T. ) ;
#3197=ORIENTED_EDGE ( 'NONE', *, *, #3938, .T. ) ;
#3198=AXIS2_PLACEMENT_3D ( 'NONE', #4579, #9368, #8203 ) ;
#3203=SPHERICAL_SURFACE ( 'NONE', #8688, 0.003937007874015747977 ) ;
#3204=DIRECTION ( 'NONE',  ( -0.000000000000000000, 1.000000000000000000, -0.000000000000000000 ) ) ;
#3205=DIRECTION ( 'NONE',  ( 0.5000000000000004441, -0.000000000000000000, -0.8660254037844384856 ) ) ;
#3207=CARTESIAN_POINT ( 'NONE',  ( -0.5871416322685659717, -0.09448818897637796532, 0.1610807828475335490 ) ) ;
#3208=ORIENTED_EDGE ( 'NONE', *, *, #7006, .F. ) ;
#3209=DIRECTION ( 'NONE',  ( 0.000000000000000000, -1.000000000000000000, -0.000000000000000000 ) ) ;
#3211=CIRCLE ( 'NONE', #4957, 0.003937007874015754916 ) ;
#3213=VERTEX_POINT ( 'NONE', #5 ) ;
#3216=EDGE_LOOP ( 'NONE', ( #1317, #899, #14404, #4350 ) ) ;
#3219=EDGE_CURVE ( 'NONE', #1302, #11324, #3106, .T. ) ;
#3220=DIRECTION ( 'NONE',  ( 0.000000000000000000, 0.000000000000000000, -1.000000000000000000 ) ) ;
#3221=CARTESIAN_POINT ( 'NONE',  ( 0.06692913385832212347, -0.4881889763779528324, -0.5909884645248143498 ) ) ;
#3224=FACE_OUTER_BOUND ( 'NONE', #7501, .T. ) ;
#3227=EDGE_CURVE ( 'NONE', #11994, #6744, #14175, .T. ) ;
#3229=CARTESIAN_POINT ( 'NONE',  ( 0.5433070866142283295, -0.4921259842519685179, 0.2409414509217496780 ) ) ;
#3230=FACE_OUTER_BOUND ( 'NONE', #1118, .T. ) ;
#3233=EDGE_LOOP ( 'NONE', ( #15290, #6615, #1483, #1500 ) ) ;
#3236=FACE_BOUND ( 'NONE', #9146, .T. ) ;
#3237=CARTESIAN_POINT ( 'NONE',  ( 0.09842519685044806566, -0.4881889763779528324, -0.2482618547481154347 ) ) ;
#3239=LINE ( 'NONE', #11294, #15113 ) ;
#3241=CARTESIAN_POINT ( 'NONE',  ( 0.2762316197870728907, -0.2952755905511811330, 0.2731340278359848384 ) ) ;
#3242=CARTESIAN_POINT ( 'NONE',  ( 0.06692913385832209572, -0.4921259842519685179, -0.2377126739437405434 ) ) ;
#3243=ORIENTED_EDGE ( 'NONE', *, *, #14484, .F. ) ;
#3244=DIRECTION ( 'NONE',  ( 0.8660254037844385966, 0.000000000000000000, 0.5000000000000001110 ) ) ;
#3245=EDGE_CURVE ( 'NONE', #11911, #14594, #14083, .T. ) ;
#3246=LINE ( 'NONE', #12797, #13380 ) ;
#3250=ORIENTED_EDGE ( 'NONE', *, *, #7324, .T. ) ;
#3254=ORIENTED_EDGE ( 'NONE', *, *, #14337, .F. ) ;
#3255=CARTESIAN_POINT ( 'NONE',  ( 0.4307978335858663188, 0.000000000000000000, 0.4279391777402732910 ) ) ;
#3259=DIRECTION ( 'NONE',  ( -0.8660254037844308250, 0.000000000000000000, 0.5000000000000134337 ) ) ;
#3260=CARTESIAN_POINT ( 'NONE',  ( -0.06011003619056348030, -0.09842519685039370636, -0.2337756660698198097 ) ) ;
#3265=ORIENTED_EDGE ( 'NONE', *, *, #6677, .T. ) ;
#3274=ADVANCED_FACE ( 'NONE', ( #10722, #1176 ), #9395, .F. ) ;
#3281=ORIENTED_EDGE ( 'NONE', *, *, #11999, .T. ) ;
#3284=EDGE_CURVE ( 'NONE', #11649, #3451, #9838, .T. ) ;
#3285=CYLINDRICAL_SURFACE ( 'NONE', #7113, 0.003937007874015758385 ) ;
#3288=CARTESIAN_POINT ( 'NONE',  ( 0.1552072824047652233, -0.09448818897637796532, -0.5870514566507987197 ) ) ;
#3290=EDGE_CURVE ( 'NONE', #2262, #15003, #7076, .T. ) ;
#3298=ADVANCED_FACE ( 'NONE', ( #4983 ), #12280, .T. ) ;
#3300=ORIENTED_EDGE ( 'NONE', *, *, #2672, .T. ) ;
#3303=ORIENTED_EDGE ( 'NONE', *, *, #12800, .T. ) ;
#3304=CARTESIAN_POINT ( 'NONE',  ( 0.000000000000000000, 2.161417322834645827, 0.000000000000000000 ) ) ;
#3305=DIRECTION ( 'NONE',  ( 0.000000000000000000, 1.000000000000000000, -0.000000000000000000 ) ) ;
#3306=DIRECTION ( 'NONE',  ( 0.5000000000000001110, 0.000000000000000000, 0.8660254037844385966 ) ) ;
#3316=ORIENTED_EDGE ( 'NONE', *, *, #14821, .F. ) ;
#3318=ORIENTED_EDGE ( 'NONE', *, *, #11031, .F. ) ;
#3319=ORIENTED_EDGE ( 'NONE', *, *, #714, .F. ) ;
#3322=DIRECTION ( 'NONE',  ( -0.000000000000000000, 1.000000000000000000, 0.000000000000000000 ) ) ;
#3325=DIRECTION ( 'NONE',  ( -0.8660254037844482555, -0.000000000000000000, -0.4999999999999837907 ) ) ;
#3328=DIRECTION ( 'NONE',  ( -0.5000000000000209832, 0.000000000000000000, -0.8660254037844266062 ) ) ;
#3332=CIRCLE ( 'NONE', #8584, 0.003937007874015746242 ) ;
#3333=ORIENTED_EDGE ( 'NONE', *, *, #7051, .T. ) ;
#3335=VERTEX_POINT ( 'NONE', #8590 ) ;
#3341=DIRECTION ( 'NONE',  ( 0.000000000000000000, 0.000000000000000000, -1.000000000000000000 ) ) ;
#3343=CARTESIAN_POINT ( 'NONE',  ( 0.2796411686208698510, -0.2952755905511811330, 0.2751025317729927644 ) ) ;
#3348=AXIS2_PLACEMENT_3D ( 'NONE', #5405, #6735, #9179 ) ;
#3353=DIRECTION ( 'NONE',  ( -0.8660254037844398178, 0.000000000000000000, 0.4999999999999979461 ) ) ;
#3356=VECTOR ( 'NONE', #10960, 39.37007874015748143 ) ;
#3357=AXIS2_PLACEMENT_3D ( 'NONE', #4434, #820, #2073 ) ;
#3358=ADVANCED_FACE ( 'NONE', ( #7264 ), #10866, .F. ) ;
#3366=EDGE_CURVE ( 'NONE', #2230, #241, #7492, .T. ) ;
#3367=FACE_OUTER_BOUND ( 'NONE', #10027, .T. ) ;
#3368=DIRECTION ( 'NONE',  ( -1.000000000000000000, -8.673617379884013384E-15, 0.000000000000000000 ) ) ;
#3369=DIRECTION ( 'NONE',  ( 0.000000000000000000, 1.000000000000000000, 0.000000000000000000 ) ) ;
#3372=VECTOR ( 'NONE', #5343, 39.37007874015748143 ) ;
#3373=VECTOR ( 'NONE', #809, 39.37007874015748143 ) ;
#3375=CLOSED_SHELL ( 'NONE', ( #6514, #1739, #8747, #10679, #4028, #10850, #12204, #2441, #3423, #3390, #15096, #13546, #7794, #5987, #3039, #2984, #4995, #13673, #13545, #9675, #14527, #4144, #3358, #1488, #7299, #1392, #8111, #13367, #9133, #15005, #1837, #13001, #13053, #13157, #5419, #13148, #15175, #9742, #5781, #4228, #5482, #2719, #6524, #9045, #13905, #3780, #15024, #10780, #648, #3274, #7253, #7707, #6249, #5961, #8524, #1656, #9735, #8074, #2510, #14799, #9881, #7593, #2329, #9906, #1556, #14978, #13759, #14242, #4185, #2914, #12920, #12511, #818, #2413, #4549, #12373, #12502, #23, #4681, #9700, #6263, #6791, #2061, #11809, #4544, #10479, #13742, #2553, #3131, #14296, #9409, #1204, #2054, #7761, #10063, #7636, #200, #3674, #14921, #4075, #13724, #6455, #6756, #6810, #75, #1323, #12287, #4555, #9738, #801, #1524, #460, #10206, #10208, #725, #1653, #7479, #6601, #1422, #11899, #3298, #8467, #5739, #3913, #4002, #11933, #9163, #9760, #6642, #5538, #8172, #120, #3523, #916, #10709, #9229, #4715, #8055, #9834, #13249, #9929, #6321, #15437, #4626, #14600, #13128, #589, #9988, #6145, #10703, #2929, #606, #6817, #14037, #3973, #8816, #12806, #14014, #13828, #2894, #10225, #10258, #4529, #14216, #13840, #3835, #4426, #12557, #7876, #12052, #6951, #4961, #2081, #2217, #12840, #5894, #13963, #8558, #11327, #442, #11144, #5107, #12418, #11044, #6430, #4738, #1824, #11020, #8664, #15071, #10543, #8825, #5716, #10107, #12893, #3853, #13261, #9719, #9555, #3954, #13055, #11251, #6844, #5388, #8088, #3694, #5176, #2481, #14970, #13281, #12499, #585, #7969, #10894, #4528, #9301, #7572, #2327, #14505, #11682, #11052, #7304, #873, #11629, #8568, #7629, #929, #5198, #324, #11760, #6905, #2997, #11775, #9885 ) ) ;
#3377=DIRECTION ( 'NONE',  ( -0.8660254037844365982, 0.000000000000000000, -0.5000000000000035527 ) ) ;
#3380=DIRECTION ( 'NONE',  ( 0.000000000000000000, 0.000000000000000000, -1.000000000000000000 ) ) ;
#3381=FACE_OUTER_BOUND ( 'NONE', #5663, .T. ) ;
#3383=FACE_OUTER_BOUND ( 'NONE', #8553, .T. ) ;
#3384=ORIENTED_EDGE ( 'NONE', *, *, #10498, .T. ) ;
#3386=EDGE_CURVE ( 'NONE', #6985, #4753, #6227, .T. ) ;
#3387=AXIS2_PLACEMENT_3D ( 'NONE', #5543, #15209, #14026 ) ;
#3389=CIRCLE ( 'NONE', #8638, 0.04330708661417331101 ) ;
#3390=ADVANCED_FACE ( 'NONE', ( #13374 ), #12087, .T. ) ;
#3391=EDGE_LOOP ( 'NONE', ( #8662, #12658, #13247, #11053 ) ) ;
#3393=SPHERICAL_SURFACE ( 'NONE', #8830, 0.003937007874015747977 ) ;
#3394=DIRECTION ( 'NONE',  ( 0.000000000000000000, 0.000000000000000000, -1.000000000000000000 ) ) ;
#3395=AXIS2_PLACEMENT_3D ( 'NONE', #935, #4596, #6957 ) ;
#3404=CIRCLE ( 'NONE', #5381, 0.007874015748031482076 ) ;
#3407=AXIS2_PLACEMENT_3D ( 'NONE', #11848, #1043, #9337 ) ;
#3411=DIRECTION ( 'NONE',  ( 0.5000000000000037748, -0.000000000000000000, 0.8660254037844365982 ) ) ;
#3415=ORIENTED_EDGE ( 'NONE', *, *, #1306, .F. ) ;
#3416=AXIS2_PLACEMENT_3D ( 'NONE', #11466, #737, #9104 ) ;
#3417=DIRECTION ( 'NONE',  ( 0.8660254037844347108, 0.000000000000000000, 0.5000000000000069944 ) ) ;
#3418=AXIS2_PLACEMENT_3D ( 'NONE', #4041, #8679, #298 ) ;
#3421=LINE ( 'NONE', #12891, #14350 ) ;
#3422=DIRECTION ( 'NONE',  ( -0.8660254037844390407, 0.000000000000000000, 0.4999999999999994449 ) ) ;
#3423=ADVANCED_FACE ( 'NONE', ( #1540 ), #13579, .T. ) ;
#3427=CARTESIAN_POINT ( 'NONE',  ( 0.4749369078591172411, -0.4881889763779528324, 0.3514880584999470203 ) ) ;
#3428=DIRECTION ( 'NONE',  ( -1.000000000000000000, 0.000000000000000000, 0.000000000000000000 ) ) ;
#3430=CARTESIAN_POINT ( 'NONE',  ( -0.1618514667033796040, -0.1023622047244094474, 0.2161887458866224576 ) ) ;
#3438=DIRECTION ( 'NONE',  ( 0.5000000000000051070, 0.000000000000000000, -0.8660254037844358210 ) ) ;
#3443=VECTOR ( 'NONE', #11754, 39.37007874015748143 ) ;
#3446=DIRECTION ( 'NONE',  ( 0.000000000000000000, 0.000000000000000000, 1.000000000000000000 ) ) ;
#3447=EDGE_CURVE ( 'NONE', #15003, #9212, #12132, .T. ) ;
#3448=DIRECTION ( 'NONE',  ( 0.000000000000000000, -1.000000000000000000, 0.000000000000000000 ) ) ;
#3450=ORIENTED_EDGE ( 'NONE', *, *, #3245, .F. ) ;
#3451=VERTEX_POINT ( 'NONE', #6157 ) ;
#3452=CYLINDRICAL_SURFACE ( 'NONE', #4116, 0.003937007874015758385 ) ;
#3455=DIRECTION ( 'NONE',  ( 0.5000000000000004441, 0.000000000000000000, 0.8660254037844383745 ) ) ;
#3459=ORIENTED_EDGE ( 'NONE', *, *, #8930, .F. ) ;
#3461=DIRECTION ( 'NONE',  ( -0.5000000000000001110, -0.000000000000000000, -0.8660254037844385966 ) ) ;
#3463=CARTESIAN_POINT ( 'NONE',  ( -0.5398975377803494347, -0.4881889763779528324, 0.2389729469846940679 ) ) ;
#3464=DIRECTION ( 'NONE',  ( -1.504632769052536979E-28, 8.673617379884035472E-15, 1.000000000000000000 ) ) ;
#3465=EDGE_LOOP ( 'NONE', ( #8824, #2807, #10507, #14291, #6716, #5433 ) ) ;
#3466=DIRECTION ( 'NONE',  ( 0.000000000000000000, 0.000000000000000000, 1.000000000000000000 ) ) ;
#3469=ORIENTED_EDGE ( 'NONE', *, *, #8586, .F. ) ;
#3472=ORIENTED_EDGE ( 'NONE', *, *, #12982, .T. ) ;
#3475=FACE_OUTER_BOUND ( 'NONE', #13018, .T. ) ;
#3477=DIRECTION ( 'NONE',  ( 0.000000000000000000, 0.000000000000000000, 1.000000000000000000 ) ) ;
#3481=EDGE_CURVE ( 'NONE', #7462, #12817, #5566, .T. ) ;
#3483=CARTESIAN_POINT ( 'NONE',  ( 0.5418660417173575272, -0.4881889763779528324, 0.2355633981508975516 ) ) ;
#3490=CYLINDRICAL_SURFACE ( 'NONE', #7183, 0.03937007874015759773 ) ;
#3491=VERTEX_POINT ( 'NONE', #11411 ) ;
#3493=EDGE_LOOP ( 'NONE', ( #8230, #14225, #4400, #11566 ) ) ;
#3495=CARTESIAN_POINT ( 'NONE',  ( -0.05958257715034473434, -0.1023622047244094474, -0.2346892519263902022 ) ) ;
#3498=DIRECTION ( 'NONE',  ( -0.000000000000000000, 1.000000000000000000, 0.000000000000000000 ) ) ;
#3499=CARTESIAN_POINT ( 'NONE',  ( 1.976792077363838002E-17, 0.003937007874015860734, 0.1614173228346456879 ) ) ;
#3500=DIRECTION ( 'NONE',  ( 0.000000000000000000, 0.000000000000000000, -1.000000000000000000 ) ) ;
#3503=CARTESIAN_POINT ( 'NONE',  ( -0.4572203724260467950, -0.1023622047244094474, 0.3821739980041202744 ) ) ;
#3506=VERTEX_POINT ( 'NONE', #3104 ) ;
#3517=LINE ( 'NONE', #3583, #198 ) ;
#3518=DIRECTION ( 'NONE',  ( 1.000000000000000000, -0.000000000000000000, -0.000000000000000000 ) ) ;
#3521=EDGE_CURVE ( 'NONE', #13356, #7138, #10304, .T. ) ;
#3522=ORIENTED_EDGE ( 'NONE', *, *, #1889, .F. ) ;
#3523=ADVANCED_FACE ( 'NONE', ( #6467 ), #527, .F. ) ;
#3528=DIRECTION ( 'NONE',  ( 3.476578583725179813E-16, 0.000000000000000000, -1.000000000000000000 ) ) ;
#3531=DIRECTION ( 'NONE',  ( 0.8660254037844368202, 0.000000000000000000, -0.5000000000000032196 ) ) ;
#3535=ORIENTED_EDGE ( 'NONE', *, *, #4986, .T. ) ;
#3536=VERTEX_POINT ( 'NONE', #12670 ) ;
#3537=ORIENTED_EDGE ( 'NONE', *, *, #14769, .T. ) ;
#3538=DIRECTION ( 'NONE',  ( -8.673617379884087537E-15, 0.000000000000000000, -1.000000000000000000 ) ) ;
#3540=CARTESIAN_POINT ( 'NONE',  ( 0.5860051159906327634, -0.003937007874015747977, 0.1591122789105293700 ) ) ;
#3543=DIRECTION ( 'NONE',  ( -1.000000000000000000, -0.000000000000000000, -0.000000000000000000 ) ) ;
#3545=ORIENTED_EDGE ( 'NONE', *, *, #5318, .T. ) ;
#3546=CARTESIAN_POINT ( 'NONE',  ( 0.1724006475077543565, -0.1023622047244094474, 0.1768186671464649640 ) ) ;
#3552=VERTEX_POINT ( 'NONE', #10071 ) ;
#3554=ORIENTED_EDGE ( 'NONE', *, *, #1986, .F. ) ;
#3555=EDGE_CURVE ( 'NONE', #675, #9261, #11492, .T. ) ;
#3560=FACE_OUTER_BOUND ( 'NONE', #13634, .T. ) ;
#3561=EDGE_CURVE ( 'NONE', #12057, #2746, #15021, .T. ) ;
#3563=SPHERICAL_SURFACE ( 'NONE', #10872, 0.003937007874015747977 ) ;
#3565=CARTESIAN_POINT ( 'NONE',  ( -0.2762316197870718359, -0.2952755905511811330, 0.2731340278359842277 ) ) ;
#3566=ORIENTED_EDGE ( 'NONE', *, *, #14500, .T. ) ;
#3569=EDGE_LOOP ( 'NONE', ( #8308, #8704, #8962, #7352, #6449, #4058, #8937, #5159, #11416, #4259 ) ) ;
#3576=CARTESIAN_POINT ( 'NONE',  ( -0.05905511811012585655, -0.09842519685039370636, -0.5870514566507987197 ) ) ;
#3578=CARTESIAN_POINT ( 'NONE',  ( -0.2344791876353258253, -0.1023622047244094474, 0.06718564542474284029 ) ) ;
#3580=CIRCLE ( 'NONE', #12335, 0.003937007874015758385 ) ;
#3582=ORIENTED_EDGE ( 'NONE', *, *, #7503, .T. ) ;
#3583=CARTESIAN_POINT ( 'NONE',  ( 0.1552072824047652233, -0.09842519685039370636, -0.5909884645248143498 ) ) ;
#3584=AXIS2_PLACEMENT_3D ( 'NONE', #10161, #12516, #5277 ) ;
#3587=TOROIDAL_SURFACE ( 'NONE', #2824, 0.04330708661417328326, 0.003937007874015747977 ) ;
#3588=ORIENTED_EDGE ( 'NONE', *, *, #12047, .F. ) ;
#3592=AXIS2_PLACEMENT_3D ( 'NONE', #1168, #5039, #9840 ) ;
#3593=AXIS2_PLACEMENT_3D ( 'NONE', #10699, #8422, #13207 ) ;
#3595=CIRCLE ( 'NONE', #14599, 0.003937007874015750579 ) ;
#3596=AXIS2_PLACEMENT_3D ( 'NONE', #13349, #1596, #511 ) ;
#3600=EDGE_CURVE ( 'NONE', #713, #12819, #2080, .T. ) ;
#3605=EDGE_LOOP ( 'NONE', ( #6924, #14272, #14919 ) ) ;
#3607=FACE_OUTER_BOUND ( 'NONE', #73, .T. ) ;
#3609=AXIS2_PLACEMENT_3D ( 'NONE', #1518, #4019, #11059 ) ;
#3610=DIRECTION ( 'NONE',  ( 0.000000000000000000, -0.000000000000000000, -1.000000000000000000 ) ) ;
#3611=EDGE_LOOP ( 'NONE', ( #6278, #7784, #3639, #15302 ) ) ;
#3612=AXIS2_PLACEMENT_3D ( 'NONE', #13484, #1733, #6492 ) ;
#3614=AXIS2_PLACEMENT_3D ( 'NONE', #10666, #13078, #2435 ) ;
#3616=ORIENTED_EDGE ( 'NONE', *, *, #4138, .T. ) ;
#3618=CARTESIAN_POINT ( 'NONE',  ( -0.06692913385815728311, -0.2952755905511811330, -0.4190977005962941426 ) ) ;
#3620=CIRCLE ( 'NONE', #9124, 0.003937007874015750579 ) ;
#3621=CIRCLE ( 'NONE', #10871, 0.1614173228346456879 ) ;
#3632=DIRECTION ( 'NONE',  ( 0.5000000000000036637, -0.000000000000000000, 0.8660254037844364872 ) ) ;
#3635=CARTESIAN_POINT ( 'NONE',  ( -0.1743691514447623103, -0.1023622047244094474, 0.1734091183126679758 ) ) ;
#3636=CIRCLE ( 'NONE', #4861, 0.003937007874015741038 ) ;
#3637=CIRCLE ( 'NONE', #1631, 0.03937007874015751446 ) ;
#3639=ORIENTED_EDGE ( 'NONE', *, *, #409, .F. ) ;
#3640=VERTEX_POINT ( 'NONE', #8207 ) ;
#3641=EDGE_LOOP ( 'NONE', ( #8941, #11348, #1007, #6471 ) ) ;
#3642=ORIENTED_EDGE ( 'NONE', *, *, #2199, .F. ) ;
#3643=LINE ( 'NONE', #4798, #11920 ) ;
#3644=CYLINDRICAL_SURFACE ( 'NONE', #6579, 0.003937007874015743640 ) ;
#3648=FACE_OUTER_BOUND ( 'NONE', #4107, .T. ) ;
#3651=AXIS2_PLACEMENT_3D ( 'NONE', #13426, #3947, #1291 ) ;
#3654=CIRCLE ( 'NONE', #410, 0.003937007874015758385 ) ;
#3655=CARTESIAN_POINT ( 'NONE',  ( -0.1724006475077544398, -0.1023622047244094474, 0.1689446513984334541 ) ) ;
#3656=LINE ( 'NONE', #9693, #9683 ) ;
#3661=STYLED_ITEM('',(#15519),#9119);
#3666=CARTESIAN_POINT ( 'NONE',  ( -0.1574803149606299191, 0.000000000000000000, -0.5870514566507987197 ) ) ;
#3667=CARTESIAN_POINT ( 'NONE',  ( -0.06299212598414173636, -0.4921259842519685179, -0.2377126739438355507 ) ) ;
#3668=DIRECTION ( 'NONE',  ( 0.5000000000000035527, 0.000000000000000000, -0.8660254037844365982 ) ) ;
#3670=CARTESIAN_POINT ( 'NONE',  ( -0.1062992125983150266, -0.1023622047244094474, -0.2482618547482104143 ) ) ;
#3674=ADVANCED_FACE ( 'NONE', ( #1069 ), #2074, .T. ) ;
#3677=VERTEX_POINT ( 'NONE', #3260 ) ;
#3679=EDGE_CURVE ( 'NONE', #10253, #12219, #8031, .T. ) ;
#3680=ORIENTED_EDGE ( 'NONE', *, *, #12080, .F. ) ;
#3684=CARTESIAN_POINT ( 'NONE',  ( 0.4572203724260462399, -0.4881889763779528324, 0.3821739980041199969 ) ) ;
#3689=ORIENTED_EDGE ( 'NONE', *, *, #4242, .T. ) ;
#3694=ADVANCED_FACE ( 'NONE', ( #8115 ), #11740, .T. ) ;
#3698=EDGE_CURVE ( 'NONE', #8390, #6217, #10089, .T. ) ;
#3705=DIRECTION ( 'NONE',  ( 0.000000000000000000, -1.000000000000000000, -0.000000000000000000 ) ) ;
#3706=CIRCLE ( 'NONE', #13971, 0.003937007874015749712 ) ;
#3708=PLANE ( 'NONE',  #131 ) ;
#3709=ORIENTED_EDGE ( 'NONE', *, *, #5266, .F. ) ;
#3710=CARTESIAN_POINT ( 'NONE',  ( 0.4296613173079339432, -0.09448818897637796532, 0.4299076816772811060 ) ) ;
#3711=DIRECTION ( 'NONE',  ( 0.000000000000000000, 0.000000000000000000, -1.000000000000000000 ) ) ;
#3713=CARTESIAN_POINT ( 'NONE',  ( 0.06692913385832208184, -0.2952755905511811330, -0.4190977005962941426 ) ) ;
#3715=ORIENTED_EDGE ( 'NONE', *, *, #2300, .T. ) ;
#3724=DIRECTION ( 'NONE',  ( 0.000000000000000000, 1.000000000000000000, 0.000000000000000000 ) ) ;
#3725=CARTESIAN_POINT ( 'NONE',  ( 0.06299212598430634080, -0.4921259842519685179, -0.2377126739437405434 ) ) ;
#3727=VECTOR ( 'NONE', #4843, 39.37007874015748143 ) ;
#3730=CARTESIAN_POINT ( 'NONE',  ( -0.1724006475077544398, -0.09842519685039370636, 0.1768186671464649640 ) ) ;
#3735=CARTESIAN_POINT ( 'NONE',  ( -0.5576140732134202693, -0.1023622047244094474, 0.2082870074805209804 ) ) ;
#3737=ORIENTED_EDGE ( 'NONE', *, *, #11173, .F. ) ;
#3739=DIRECTION ( 'NONE',  ( 0.000000000000000000, 0.000000000000000000, 1.000000000000000000 ) ) ;
#3742=DIRECTION ( 'NONE',  ( 0.5000000000000001110, -0.000000000000000000, -0.8660254037844388186 ) ) ;
#3744=DIRECTION ( 'NONE',  ( 1.000000000000000000, -0.000000000000000000, 0.000000000000000000 ) ) ;
#3745=DIRECTION ( 'NONE',  ( 6.505213034913065258E-15, -1.000000000000000000, 0.000000000000000000 ) ) ;
#3747=DIRECTION ( 'NONE',  ( 0.5000000000000004441, -0.000000000000000000, -0.8660254037844383745 ) ) ;
#3748=ORIENTED_EDGE ( 'NONE', *, *, #3103, .T. ) ;
#3750=ORIENTED_EDGE ( 'NONE', *, *, #14016, .T. ) ;
#3752=DIRECTION ( 'NONE',  ( 0.000000000000000000, 0.000000000000000000, -1.000000000000000000 ) ) ;
#3753=EDGE_CURVE ( 'NONE', #2454, #2526, #9605, .T. ) ;
#3758=DIRECTION ( 'NONE',  ( -1.000000000000000000, 0.000000000000000000, 0.000000000000000000 ) ) ;
#3759=DIRECTION ( 'NONE',  ( 0.000000000000000000, 1.000000000000000000, 0.000000000000000000 ) ) ;
#3763=EDGE_CURVE ( 'NONE', #14414, #3640, #3595, .T. ) ;
#3769=EDGE_CURVE ( 'NONE', #10725, #11669, #13846, .T. ) ;
#3779=LINE ( 'NONE', #33, #11156 ) ;
#3780=ADVANCED_FACE ( 'NONE', ( #8429 ), #8504, .F. ) ;
#3781=LINE ( 'NONE', #11216, #2593 ) ;
#3783=DIRECTION ( 'NONE',  ( 0.5000000000000051070, 0.000000000000000000, -0.8660254037844358210 ) ) ;
#3785=ORIENTED_EDGE ( 'NONE', *, *, #4758, .F. ) ;
#3793=LINE ( 'NONE', #8564, #2601 ) ;
#3795=PLANE ( 'NONE',  #12116 ) ;
#3801=ORIENTED_EDGE ( 'NONE', *, *, #15337, .F. ) ;
#3808=FACE_OUTER_BOUND ( 'NONE', #5213, .T. ) ;
#3810=CARTESIAN_POINT ( 'NONE',  ( 0.1531294576121448037, -0.4921259842519685179, -0.08840933357323313424 ) ) ;
#3811=CARTESIAN_POINT ( 'NONE',  ( 0.2373612774290684013, -0.1023622047244094474, 0.06430355563125962626 ) ) ;
#3812=DIRECTION ( 'NONE',  ( 1.000000000000000000, 0.000000000000000000, 3.476578583725179813E-16 ) ) ;
#3818=ORIENTED_EDGE ( 'NONE', *, *, #4344, .T. ) ;
#3819=AXIS2_PLACEMENT_3D ( 'NONE', #3578, #9391, #11665 ) ;
#3820=CARTESIAN_POINT ( 'NONE',  ( -0.5576140732134202693, -0.4881889763779528324, 0.2082870074805209804 ) ) ;
#3828=DIRECTION ( 'NONE',  ( 0.000000000000000000, 0.000000000000000000, -1.000000000000000000 ) ) ;
#3830=ORIENTED_EDGE ( 'NONE', *, *, #11516, .T. ) ;
#3831=EDGE_CURVE ( 'NONE', #2464, #15288, #587, .T. ) ;
#3832=VERTEX_POINT ( 'NONE', #10773 ) ;
#3835=ADVANCED_FACE ( 'NONE', ( #54 ), #2919, .T. ) ;
#3836=AXIS2_PLACEMENT_3D ( 'NONE', #5912, #9373, #14236 ) ;
#3837=EDGE_LOOP ( 'NONE', ( #12569, #8807, #7053 ) ) ;
#3838=CARTESIAN_POINT ( 'NONE',  ( 0.5084014747882494856, -0.003937007874015747977, 0.2935257283254013583 ) ) ;
#3842=CIRCLE ( 'NONE', #11595, 0.003937007874015758385 ) ;
#3844=CIRCLE ( 'NONE', #853, 0.003937007874015747109 ) ;
#3847=CARTESIAN_POINT ( 'NONE',  ( 0.2359202325322792559, -0.4881889763779528324, 0.06286251073447048088 ) ) ;
#3849=LINE ( 'NONE', #12171, #6839 ) ;
#3851=DIRECTION ( 'NONE',  ( -4.865806668049467791E-32, 1.000000000000000000, 1.224646799147353207E-16 ) ) ;
#3853=ADVANCED_FACE ( 'NONE', ( #3230 ), #10124, .T. ) ;
#3855=EDGE_LOOP ( 'NONE', ( #10494, #6517, #8875, #5036 ) ) ;
#3857=EDGE_LOOP ( 'NONE', ( #1116, #7494, #22, #3642 ) ) ;
#3859=ORIENTED_EDGE ( 'NONE', *, *, #3227, .T. ) ;
#3860=AXIS2_PLACEMENT_3D ( 'NONE', #4384, #12704, #1968 ) ;
#3861=EDGE_CURVE ( 'NONE', #12353, #5050, #791, .T. ) ;
#3867=SPHERICAL_SURFACE ( 'NONE', #837, 0.003937007874015747977 ) ;
#3871=DIRECTION ( 'NONE',  ( -0.000000000000000000, -1.000000000000000000, -0.000000000000000000 ) ) ;
#3872=DIRECTION ( 'NONE',  ( 0.000000000000000000, 0.000000000000000000, 1.000000000000000000 ) ) ;
#3876=VECTOR ( 'NONE', #1023, 39.37007874015748143 ) ;
#3877=DIRECTION ( 'NONE',  ( -0.000000000000000000, -1.000000000000000000, -0.000000000000000000 ) ) ;
#3878=AXIS2_PLACEMENT_3D ( 'NONE', #4467, #15278, #3368 ) ;
#3882=EDGE_LOOP ( 'NONE', ( #11977, #1304, #2598 ) ) ;
#3884=AXIS2_PLACEMENT_3D ( 'NONE', #9319, #3369, #2201 ) ;
#3895=DIRECTION ( 'NONE',  ( -0.5000000000000004441, 0.000000000000000000, 0.8660254037844383745 ) ) ;
#3901=VECTOR ( 'NONE', #3747, 39.37007874015748143 ) ;
#3902=CIRCLE ( 'NONE', #5385, 0.1574803149606299191 ) ;
#3905=ORIENTED_EDGE ( 'NONE', *, *, #4166, .F. ) ;
#3906=AXIS2_PLACEMENT_3D ( 'NONE', #1311, #8355, #13141 ) ;
#3908=ORIENTED_EDGE ( 'NONE', *, *, #12241, .T. ) ;
#3912=DIRECTION ( 'NONE',  ( -1.000000000000000000, 8.673617379884035472E-15, -0.000000000000000000 ) ) ;
#3913=ADVANCED_FACE ( 'NONE', ( #1809 ), #11598, .T. ) ;
#3916=CIRCLE ( 'NONE', #1417, 0.003937007874015741038 ) ;
#3919=CARTESIAN_POINT ( 'NONE',  ( 0.4307978335858664853, -0.09842519685039370636, 0.4279391777402732910 ) ) ;
#3921=DIRECTION ( 'NONE',  ( -0.4999999999999996114, -0.000000000000000000, -0.8660254037844389297 ) ) ;
#3925=ORIENTED_EDGE ( 'NONE', *, *, #8096, .T. ) ;
#3929=CARTESIAN_POINT ( 'NONE',  ( -0.4783464566929145900, -0.1023622047244094474, 0.3534565624369550574 ) ) ;
#3935=SPHERICAL_SURFACE ( 'NONE', #15152, 0.003937007874015747977 ) ;
#3938=EDGE_CURVE ( 'NONE', #10200, #4047, #14354, .T. ) ;
#3942=ORIENTED_EDGE ( 'NONE', *, *, #7006, .T. ) ;
#3943=ORIENTED_EDGE ( 'NONE', *, *, #3193, .T. ) ;
#3944=CIRCLE ( 'NONE', #12709, 0.007874015748031482076 ) ;
#3947=DIRECTION ( 'NONE',  ( 0.4999999999999977240, -1.084202172485506012E-15, -0.8660254037844400399 ) ) ;
#3948=VECTOR ( 'NONE', #8091, 39.37007874015748143 ) ;
#3954=ADVANCED_FACE ( 'NONE', ( #7998 ), #10204, .T. ) ;
#3957=DIRECTION ( 'NONE',  ( -0.000000000000000000, -1.000000000000000000, 0.000000000000000000 ) ) ;
#3963=AXIS2_PLACEMENT_3D ( 'NONE', #12480, #11286, #2918 ) ;
#3966=ORIENTED_EDGE ( 'NONE', *, *, #3521, .T. ) ;
#3967=ORIENTED_EDGE ( 'NONE', *, *, #1933, .T. ) ;
#3973=ADVANCED_FACE ( 'NONE', ( #11692 ), #963, .F. ) ;
#3976=LINE ( 'NONE', #14630, #15084 ) ;
#3977=CARTESIAN_POINT ( 'NONE',  ( -0.09948011493072102251, -0.4921259842519685179, -0.2443248468741946733 ) ) ;
#3984=ORIENTED_EDGE ( 'NONE', *, *, #12469, .F. ) ;
#3985=ORIENTED_EDGE ( 'NONE', *, *, #2335, .F. ) ;
#3986=ORIENTED_EDGE ( 'NONE', *, *, #1585, .T. ) ;
#3987=VERTEX_POINT ( 'NONE', #3062 ) ;
#3990=DIRECTION ( 'NONE',  ( 8.673617379884035472E-15, 1.000000000000000000, 0.000000000000000000 ) ) ;
#3997=DIRECTION ( 'NONE',  ( 0.4999999999999998890, 0.000000000000000000, 0.8660254037844385966 ) ) ;
#4002=ADVANCED_FACE ( 'NONE', ( #3381 ), #7049, .F. ) ;
#4004=ORIENTED_EDGE ( 'NONE', *, *, #11604, .T. ) ;
#4006=DIRECTION ( 'NONE',  ( 0.000000000000000000, -1.000000000000000000, 0.000000000000000000 ) ) ;
#4007=CARTESIAN_POINT ( 'NONE',  ( 0.5379290338433416752, -0.09448818897637796532, 0.2423824958184915834 ) ) ;
#4010=ORIENTED_EDGE ( 'NONE', *, *, #13995, .F. ) ;
#4012=FACE_OUTER_BOUND ( 'NONE', #469, .T. ) ;
#4014=FACE_OUTER_BOUND ( 'NONE', #1961, .T. ) ;
#4016=ORIENTED_EDGE ( 'NONE', *, *, #13802, .T. ) ;
#4018=CARTESIAN_POINT ( 'NONE',  ( -0.2661821753646866906, -0.4921259842519685179, 0.03548265769538203052 ) ) ;
#4019=DIRECTION ( 'NONE',  ( -3.614007241618347785E-16, 0.000000000000000000, 1.000000000000000000 ) ) ;
#4022=PLANE ( 'NONE',  #358 ) ;
#4024=DIRECTION ( 'NONE',  ( -1.000000000000000000, -0.000000000000000000, -3.973232667114495301E-16 ) ) ;
#4025=FACE_OUTER_BOUND ( 'NONE', #2925, .T. ) ;
#4026=CARTESIAN_POINT ( 'NONE',  ( -0.2364476915723336681, -0.4881889763779528324, 0.06377609659094583827 ) ) ;
#4028=ADVANCED_FACE ( 'NONE', ( #8160 ), #8305, .T. ) ;
#4029=VERTEX_POINT ( 'NONE', #10577 ) ;
#4030=EDGE_CURVE ( 'NONE', #13855, #7381, #10506, .T. ) ;
#4031=VERTEX_POINT ( 'NONE', #9500 ) ;
#4032=EDGE_CURVE ( 'NONE', #15013, #8301, #15350, .T. ) ;
#4036=CARTESIAN_POINT ( 'NONE',  ( -0.09842519685028340570, -0.4881889763779528324, -0.5870514566507987197 ) ) ;
#4037=CARTESIAN_POINT ( 'NONE',  ( 0.5649606299212333038, -0.09448818897637796532, 0.2034364137499355130 ) ) ;
#4041=CARTESIAN_POINT ( 'NONE',  ( 0.000000000000000000, 2.165354330708661568, 0.000000000000000000 ) ) ;
#4045=EDGE_LOOP ( 'NONE', ( #4859, #4571 ) ) ;
#4047=VERTEX_POINT ( 'NONE', #9420 ) ;
#4048=ORIENTED_EDGE ( 'NONE', *, *, #9169, .T. ) ;
#4050=EDGE_CURVE ( 'NONE', #7774, #9271, #10599, .T. ) ;
#4051=DIRECTION ( 'NONE',  ( 0.5000000000000035527, 0.000000000000000000, -0.8660254037844365982 ) ) ;
#4054=CYLINDRICAL_SURFACE ( 'NONE', #1122, 0.003937007874015741038 ) ;
#4058=ORIENTED_EDGE ( 'NONE', *, *, #13630, .T. ) ;
#4059=DIRECTION ( 'NONE',  ( 0.000000000000000000, 0.000000000000000000, 1.000000000000000000 ) ) ;
#4061=VERTEX_POINT ( 'NONE', #3343 ) ;
#4062=ORIENTED_EDGE ( 'NONE', *, *, #7538, .F. ) ;
#4073=ORIENTED_EDGE ( 'NONE', *, *, #7538, .T. ) ;
#4075=ADVANCED_FACE ( 'NONE', ( #14073 ), #11871, .T. ) ;
#4077=CARTESIAN_POINT ( 'NONE',  ( -0.1062992125983150127, -0.1023622047244094474, -0.2482618547482104421 ) ) ;
#4088=CARTESIAN_POINT ( 'NONE',  ( -0.5860051159906336515, -0.09842519685039370636, 0.1591122789105256508 ) ) ;
#4092=AXIS2_PLACEMENT_3D ( 'NONE', #10740, #10668, #9326 ) ;
#4093=CARTESIAN_POINT ( 'NONE',  ( 0.3137366569588399545, -0.2952755905511811330, 0.2947875711430715251 ) ) ;
#4094=CARTESIAN_POINT ( 'NONE',  ( -0.2796411686208687963, -0.2952755905511811330, 0.2751025317729920427 ) ) ;
#4095=AXIS2_PLACEMENT_3D ( 'NONE', #11389, #671, #5427 ) ;
#4097=CARTESIAN_POINT ( 'NONE',  ( -0.1023622047242991467, -0.4881889763779528324, -0.5870514566507987197 ) ) ;
#4098=EDGE_CURVE ( 'NONE', #8667, #2746, #7338, .T. ) ;
#4099=DIRECTION ( 'NONE',  ( 0.5000000000000001110, -0.000000000000000000, -0.8660254037844385966 ) ) ;
#4102=AXIS2_PLACEMENT_3D ( 'NONE', #2971, #7739, #14963 ) ;
#4107=EDGE_LOOP ( 'NONE', ( #7379, #13511, #11346, #2397 ) ) ;
#4109=ORIENTED_EDGE ( 'NONE', *, *, #7108, .F. ) ;
#4113=CIRCLE ( 'NONE', #14641, 0.003937007874015758385 ) ;
#4114=VECTOR ( 'NONE', #13930, 39.37007874015748143 ) ;
#4116=AXIS2_PLACEMENT_3D ( 'NONE', #6971, #4534, #858 ) ;
#4118=DIRECTION ( 'NONE',  ( -0.8660254037844422603, -0.000000000000000000, 0.4999999999999939493 ) ) ;
#4123=DIRECTION ( 'NONE',  ( -0.000000000000000000, -1.000000000000000000, -0.000000000000000000 ) ) ;
#4124=VERTEX_POINT ( 'NONE', #9529 ) ;
#4125=EDGE_CURVE ( 'NONE', #4401, #12819, #11351, .T. ) ;
#4126=ORIENTED_EDGE ( 'NONE', *, *, #11173, .T. ) ;
#4127=EDGE_LOOP ( 'NONE', ( #11022, #1630, #4130, #223 ) ) ;
#4130=ORIENTED_EDGE ( 'NONE', *, *, #13553, .F. ) ;
#4132=CYLINDRICAL_SURFACE ( 'NONE', #11393, 0.003937007874015749712 ) ;
#4133=CYLINDRICAL_SURFACE ( 'NONE', #5820, 0.003937007874015758385 ) ;
#4137=CARTESIAN_POINT ( 'NONE',  ( 0.1657884745773951785, -0.4921259842519685179, 0.2093696482190284258 ) ) ;
#4138=EDGE_CURVE ( 'NONE', #9448, #6660, #2105, .T. ) ;
#4144=ADVANCED_FACE ( 'NONE', ( #8202 ), #11966, .F. ) ;
#4145=AXIS2_PLACEMENT_3D ( 'NONE', #13562, #5325, #7768 ) ;
#4147=AXIS2_PLACEMENT_3D ( 'NONE', #997, #5745, #11968 ) ;
#4148=EDGE_LOOP ( 'NONE', ( #2153, #5372, #12996, #9147 ) ) ;
#4152=ORIENTED_EDGE ( 'NONE', *, *, #10937, .F. ) ;
#4155=CARTESIAN_POINT ( 'NONE',  ( 0.06692913385832209572, -0.1023622047244094474, -0.2377126739437405434 ) ) ;
#4157=DIRECTION ( 'NONE',  ( -0.4999999999999998335, 0.000000000000000000, -0.8660254037844388186 ) ) ;
#4160=EDGE_LOOP ( 'NONE', ( #5101, #9488, #10429, #14250 ) ) ;
#4161=CARTESIAN_POINT ( 'NONE',  ( -0.1552072824047652233, -0.09448818897637796532, -0.5870514566507987197 ) ) ;
#4162=CARTESIAN_POINT ( 'NONE',  ( -0.3766253205744463650, -0.2952755905511811330, 0.09924703731238559978 ) ) ;
#4163=CIRCLE ( 'NONE', #12428, 0.003937007874015737569 ) ;
#4164=CARTESIAN_POINT ( 'NONE',  ( -0.5894146648244306119, -0.003937007874015747977, 0.1610807828475335490 ) ) ;
#4165=CARTESIAN_POINT ( 'NONE',  ( -0.2672370934451241409, -0.1023622047244094474, 0.03154564982136626866 ) ) ;
#4166=EDGE_CURVE ( 'NONE', #8120, #6985, #5087, .T. ) ;
#4167=CYLINDRICAL_SURFACE ( 'NONE', #5664, 0.003937007874015740171 ) ;
#4170=ORIENTED_EDGE ( 'NONE', *, *, #6509, .F. ) ;
#4172=EDGE_CURVE ( 'NONE', #1810, #13131, #1153, .T. ) ;
#4178=CARTESIAN_POINT ( 'NONE',  ( 0.000000000000000000, 0.003937007874015860734, 0.000000000000000000 ) ) ;
#4181=AXIS2_PLACEMENT_3D ( 'NONE', #9268, #14047, #2140 ) ;
#4182=CARTESIAN_POINT ( 'NONE',  ( -0.2953892001169318160, -0.2952755905511811330, 0.2478261411026162764 ) ) ;
#4185=ADVANCED_FACE ( 'NONE', ( #3648 ), #14871, .T. ) ;
#4188=ORIENTED_EDGE ( 'NONE', *, *, #1999, .T. ) ;
#4189=CARTESIAN_POINT ( 'NONE',  ( -0.5615510810874361214, -0.1023622047244094474, 0.2014679098129270318 ) ) ;
#4191=AXIS2_PLACEMENT_3D ( 'NONE', #7329, #8448, #3745 ) ;
#4192=EDGE_CURVE ( 'NONE', #11838, #3552, #13859, .T. ) ;
#4201=CARTESIAN_POINT ( 'NONE',  ( -0.4307978335858689278, -0.003937007874015747977, 0.4279391777402706820 ) ) ;
#4202=AXIS2_PLACEMENT_3D ( 'NONE', #7048, #4393, #4543 ) ;
#4203=DIRECTION ( 'NONE',  ( -1.000000000000000000, -8.673617379884013384E-15, 0.000000000000000000 ) ) ;
#4205=ORIENTED_EDGE ( 'NONE', *, *, #14574, .F. ) ;
#4208=EDGE_LOOP ( 'NONE', ( #7967, #9982, #7104 ) ) ;
#4210=EDGE_LOOP ( 'NONE', ( #5386, #4920, #9552, #5144 ) ) ;
#4211=AXIS2_PLACEMENT_3D ( 'NONE', #7409, #148, #9933 ) ;
#4213=DIRECTION ( 'NONE',  ( -0.4999999999999979461, -0.000000000000000000, -0.8660254037844398178 ) ) ;
#4214=DIRECTION ( 'NONE',  ( 0.5000000000000004441, -0.000000000000000000, -0.8660254037844384856 ) ) ;
#4218=DIRECTION ( 'NONE',  ( -1.000000000000000000, 0.000000000000000000, 0.000000000000000000 ) ) ;
#4219=CARTESIAN_POINT ( 'NONE',  ( -0.06692913385815749128, -0.4881889763779528324, -0.2377126739438355507 ) ) ;
#4221=ORIENTED_EDGE ( 'NONE', *, *, #1008, .F. ) ;
#4224=EDGE_LOOP ( 'NONE', ( #3303, #14565, #6370, #5715 ) ) ;
#4225=ORIENTED_EDGE ( 'NONE', *, *, #5196, .F. ) ;
#4227=ORIENTED_EDGE ( 'NONE', *, *, #13243, .F. ) ;
#4228=ADVANCED_FACE ( 'NONE', ( #6273, #13273 ), #4022, .F. ) ;
#4229=EDGE_CURVE ( 'NONE', #6660, #6983, #2840, .T. ) ;
#4233=DIRECTION ( 'NONE',  ( 2.168404344971007142E-16, 0.000000000000000000, -1.000000000000000000 ) ) ;
#4237=DIRECTION ( 'NONE',  ( -0.000000000000000000, 0.000000000000000000, 1.000000000000000000 ) ) ;
#4238=DIRECTION ( 'NONE',  ( -0.4999999999999975575, 0.000000000000000000, -0.8660254037844399289 ) ) ;
#4242=EDGE_CURVE ( 'NONE', #11911, #15201, #11612, .T. ) ;
#4245=DIRECTION ( 'NONE',  ( 0.000000000000000000, 1.000000000000000000, 0.000000000000000000 ) ) ;
#4246=DIRECTION ( 'NONE',  ( 0.000000000000000000, 0.000000000000000000, -1.000000000000000000 ) ) ;
#4248=CARTESIAN_POINT ( 'NONE',  ( 1.928577636452524610E-17, -0.4881889763779528324, -0.1574803149606299191 ) ) ;
#4256=CARTESIAN_POINT ( 'NONE',  ( 0.3314531923919106227, -0.2952755905511811330, 0.2641016316388982710 ) ) ;
#4259=ORIENTED_EDGE ( 'NONE', *, *, #12386, .T. ) ;
#4261=ORIENTED_EDGE ( 'NONE', *, *, #14413, .T. ) ;
#4262=CARTESIAN_POINT ( 'NONE',  ( -0.1023622047242991467, -0.1023622047244094474, -0.5870514566507987197 ) ) ;
#4264=DIRECTION ( 'NONE',  ( 0.000000000000000000, 0.000000000000000000, 1.000000000000000000 ) ) ;
#4266=DIRECTION ( 'NONE',  ( 0.4999999999999983347, -0.000000000000000000, 0.8660254037844397068 ) ) ;
#4269=DIRECTION ( 'NONE',  ( 0.000000000000000000, 0.000000000000000000, -1.000000000000000000 ) ) ;
#4271=EDGE_CURVE ( 'NONE', #1905, #11305, #11095, .T. ) ;
#4274=ORIENTED_EDGE ( 'NONE', *, *, #3092, .T. ) ;
#4276=EDGE_LOOP ( 'NONE', ( #12752, #7038, #9150 ) ) ;
#4280=CARTESIAN_POINT ( 'NONE',  ( 0.2661821753648509481, -0.1023622047244094474, 0.03548265769547701703 ) ) ;
#4283=DIRECTION ( 'NONE',  ( 0.000000000000000000, 1.000000000000000000, -0.000000000000000000 ) ) ;
#4284=LINE ( 'NONE', #4366, #7966 ) ;
#4287=CYLINDRICAL_SURFACE ( 'NONE', #7428, 0.03937007874015754916 ) ;
#4291=ORIENTED_EDGE ( 'NONE', *, *, #2805, .F. ) ;
#4292=ORIENTED_EDGE ( 'NONE', *, *, #3481, .F. ) ;
#4293=DIRECTION ( 'NONE',  ( 0.5000000000000004441, 0.000000000000000000, 0.8660254037844383745 ) ) ;
#4294=CYLINDRICAL_SURFACE ( 'NONE', #1124, 0.003937007874015744507 ) ;
#4296=CARTESIAN_POINT ( 'NONE',  ( 0.2393297813660762718, -0.4881889763779528324, 0.06089400679746261730 ) ) ;
#4297=FACE_OUTER_BOUND ( 'NONE', #6486, .T. ) ;
#4298=ORIENTED_EDGE ( 'NONE', *, *, #1265, .T. ) ;
#4299=DIRECTION ( 'NONE',  ( -0.4999999999999986122, 0.000000000000000000, 0.8660254037844395958 ) ) ;
#4302=EDGE_CURVE ( 'NONE', #6217, #15003, #14832, .T. ) ;
#4305=CARTESIAN_POINT ( 'NONE',  ( -0.5084014747882513729, -0.003937007874015747977, 0.2935257283253980831 ) ) ;
#4308=ORIENTED_EDGE ( 'NONE', *, *, #2335, .T. ) ;
#4309=ORIENTED_EDGE ( 'NONE', *, *, #9534, .F. ) ;
#4312=CYLINDRICAL_SURFACE ( 'NONE', #5340, 0.003937007874015758385 ) ;
#4316=CIRCLE ( 'NONE', #5810, 0.003937007874015749712 ) ;
#4318=VERTEX_POINT ( 'NONE', #13725 ) ;
#4319=CARTESIAN_POINT ( 'NONE',  ( 0.03346456692910664693, -0.4921259842519685179, -0.05796233017450188457 ) ) ;
#4320=AXIS2_PLACEMENT_3D ( 'NONE', #2259, #11906, #13146 ) ;
#4323=DIRECTION ( 'NONE',  ( 0.000000000000000000, -0.000000000000000000, -1.000000000000000000 ) ) ;
#4330=CIRCLE ( 'NONE', #8328, 0.003937007874015754916 ) ;
#4335=CARTESIAN_POINT ( 'NONE',  ( -0.4749369078591176296, -0.1023622047244094474, 0.3514880584999472424 ) ) ;
#4337=SHAPE_REPRESENTATION_RELATIONSHIP ( 'NONE' , 'NONE' ,  #12705, #8362 ) ;
#4341=TOROIDAL_SURFACE ( 'NONE', #1601, 0.007874015748031495954, 0.003937007874015747977 ) ;
#4343=PLANE ( 'NONE',  #7391 ) ;
#4344=EDGE_CURVE ( 'NONE', #14791, #10242, #7364, .T. ) ;
#4348=CIRCLE ( 'NONE', #616, 0.003937007874015758385 ) ;
#4350=ORIENTED_EDGE ( 'NONE', *, *, #14152, .F. ) ;
#4353=EDGE_CURVE ( 'NONE', #8715, #5216, #1431, .T. ) ;
#4361=CARTESIAN_POINT ( 'NONE',  ( -1.315994971760645248E-15, -0.003937007874015747977, 0.4279391777402719588 ) ) ;
#4366=CARTESIAN_POINT ( 'NONE',  ( -0.000000000000000000, -0.09842519685039370636, 0.1689446513984334541 ) ) ;
#4369=DIRECTION ( 'NONE',  ( -1.000000000000000000, 0.000000000000000000, 0.000000000000000000 ) ) ;
#4370=CARTESIAN_POINT ( 'NONE',  ( -0.3512416941306060192, -0.2952755905511811330, 0.3164411144501575457 ) ) ;
#4371=AXIS2_PLACEMENT_3D ( 'NONE', #9439, #8013, #9269 ) ;
#4372=AXIS2_PLACEMENT_3D ( 'NONE', #8090, #10452, #15231 ) ;
#4374=ORIENTED_EDGE ( 'NONE', *, *, #8690, .F. ) ;
#4378=ORIENTED_EDGE ( 'NONE', *, *, #10000, .F. ) ;
#4379=CARTESIAN_POINT ( 'NONE',  ( -0.5398975377803494347, -0.1023622047244094474, 0.2389729469846940679 ) ) ;
#4382=AXIS2_PLACEMENT_3D ( 'NONE', #4370, #11578, #5090 ) ;
#4384=CARTESIAN_POINT ( 'NONE',  ( -0.4591888763630546655, -0.09842519685039370636, 0.3787644491703233141 ) ) ;
#4389=CARTESIAN_POINT ( 'NONE',  ( 0.06299212598430634080, -0.1023622047244094474, -0.2377126739437405434 ) ) ;
#4392=LINE ( 'NONE', #13732, #11352 ) ;
#4393=DIRECTION ( 'NONE',  ( 0.000000000000000000, -1.000000000000000000, 0.000000000000000000 ) ) ;
#4394=DIRECTION ( 'NONE',  ( 0.000000000000000000, 0.000000000000000000, -1.000000000000000000 ) ) ;
#4396=DIRECTION ( 'NONE',  ( 0.000000000000000000, 0.000000000000000000, -1.000000000000000000 ) ) ;
#4399=CIRCLE ( 'NONE', #15418, 0.003937007874015749712 ) ;
#4400=ORIENTED_EDGE ( 'NONE', *, *, #1125, .F. ) ;
#4401=VERTEX_POINT ( 'NONE', #7683 ) ;
#4405=CARTESIAN_POINT ( 'NONE',  ( 0.5418660417173575272, -0.4881889763779528324, 0.2355633981508976349 ) ) ;
#4407=FACE_OUTER_BOUND ( 'NONE', #4148, .T. ) ;
#4410=CIRCLE ( 'NONE', #5902, 0.003937007874015758385 ) ;
#4417=DIRECTION ( 'NONE',  ( 0.5000000000000004441, 0.000000000000000000, -0.8660254037844383745 ) ) ;
#4419=ORIENTED_EDGE ( 'NONE', *, *, #10000, .T. ) ;
#4421=ORIENTED_EDGE ( 'NONE', *, *, #8396, .F. ) ;
#4425=AXIS2_PLACEMENT_3D ( 'NONE', #4161, #12624, #2817 ) ;
#4426=ADVANCED_FACE ( 'NONE', ( #10977 ), #1502, .T. ) ;
#4434=CARTESIAN_POINT ( 'NONE',  ( -0.3944453183761345572, -0.2952755905511811330, 0.1549960689574421957 ) ) ;
#4441=AXIS2_PLACEMENT_3D ( 'NONE', #7227, #3543, #8081 ) ;
#4444=EDGE_CURVE ( 'NONE', #11529, #13463, #11040, .T. ) ;
#4448=DIRECTION ( 'NONE',  ( -1.000000000000000000, 0.000000000000000000, -3.075191616504340279E-15 ) ) ;
#4450=DIRECTION ( 'NONE',  ( -1.000000000000000000, 0.000000000000000000, 0.000000000000000000 ) ) ;
#4459=AXIS2_PLACEMENT_3D ( 'NONE', #6730, #1971, #11519 ) ;
#4463=ORIENTED_EDGE ( 'NONE', *, *, #7029, .F. ) ;
#4464=FACE_OUTER_BOUND ( 'NONE', #9313, .T. ) ;
#4466=CYLINDRICAL_SURFACE ( 'NONE', #15377, 0.003937007874015721089 ) ;
#4467=CARTESIAN_POINT ( 'NONE',  ( -0.2681506793016945611, -0.1023622047244094474, 0.03207310886158500768 ) ) ;
#4471=ORIENTED_EDGE ( 'NONE', *, *, #8488, .T. ) ;
#4474=CARTESIAN_POINT ( 'NONE',  ( -0.1763376553817701808, -0.1023622047244094474, 0.1699995694788709877 ) ) ;
#4476=ORIENTED_EDGE ( 'NONE', *, *, #14152, .T. ) ;
#4481=ORIENTED_EDGE ( 'NONE', *, *, #13680, .F. ) ;
#4482=CARTESIAN_POINT ( 'NONE',  ( -0.2353927734918962178, -0.1023622047244094474, 0.06771310446496157931 ) ) ;
#4483=CARTESIAN_POINT ( 'NONE',  ( 0.1724006475077543565, -0.4881889763779528324, 0.1768186671464649640 ) ) ;
#4484=CARTESIAN_POINT ( 'NONE',  ( 0.5894146648244296127, -0.003937007874015747977, 0.1610807828475372405 ) ) ;
#4488=FACE_OUTER_BOUND ( 'NONE', #9537, .T. ) ;
#4490=DIRECTION ( 'NONE',  ( -0.000000000000000000, 1.000000000000000000, 0.000000000000000000 ) ) ;
#4494=ORIENTED_EDGE ( 'NONE', *, *, #6875, .T. ) ;
#4495=ORIENTED_EDGE ( 'NONE', *, *, #4050, .T. ) ;
#4496=DIRECTION ( 'NONE',  ( 0.8660254037844368202, 0.000000000000000000, -0.5000000000000032196 ) ) ;
#4497=VERTEX_POINT ( 'NONE', #5705 ) ;
#4499=VERTEX_POINT ( 'NONE', #13949 ) ;
#4504=FACE_OUTER_BOUND ( 'NONE', #7090, .T. ) ;
#4505=CARTESIAN_POINT ( 'NONE',  ( 0.4783464566929142014, -0.1023622047244094474, 0.3534565624369548908 ) ) ;
#4508=CARTESIAN_POINT ( 'NONE',  ( 0.4307978335858662633, -0.003937007874015747977, 0.4279391777402732910 ) ) ;
#4510=EDGE_CURVE ( 'NONE', #8715, #5518, #5102, .T. ) ;
#4511=ORIENTED_EDGE ( 'NONE', *, *, #235, .F. ) ;
#4514=ORIENTED_EDGE ( 'NONE', *, *, #5004, .T. ) ;
#4516=DIRECTION ( 'NONE',  ( -0.000000000000000000, -0.000000000000000000, 1.000000000000000000 ) ) ;
#4517=DIRECTION ( 'NONE',  ( 0.000000000000000000, -1.000000000000000000, 0.000000000000000000 ) ) ;
#4524=VERTEX_POINT ( 'NONE', #11681 ) ;
#4525=DIRECTION ( 'NONE',  ( 0.000000000000000000, -1.000000000000000000, 0.000000000000000000 ) ) ;
#4528=ADVANCED_FACE ( 'NONE', ( #3138 ), #4294, .T. ) ;
#4529=ADVANCED_FACE ( 'NONE', ( #10263 ), #3285, .F. ) ;
#4534=DIRECTION ( 'NONE',  ( 1.000000000000000000, 0.000000000000000000, 0.000000000000000000 ) ) ;
#4537=CARTESIAN_POINT ( 'NONE',  ( 0.06692913385832212347, -0.1023622047244094474, -0.5909884645248143498 ) ) ;
#4538=CARTESIAN_POINT ( 'NONE',  ( 0.1743691514447621993, -0.4921259842519685179, 0.1734091183126679481 ) ) ;
#4541=CARTESIAN_POINT ( 'NONE',  ( -0.5871416322685659717, -0.09448818897637796532, 0.1571437749735178357 ) ) ;
#4543=DIRECTION ( 'NONE',  ( 0.000000000000000000, -0.000000000000000000, -1.000000000000000000 ) ) ;
#4544=ADVANCED_FACE ( 'NONE', ( #10424 ), #4466, .T. ) ;
#4547=FACE_OUTER_BOUND ( 'NONE', #14936, .T. ) ;
#4549=ADVANCED_FACE ( 'NONE', ( #10330 ), #1618, .T. ) ;
#4555=ADVANCED_FACE ( 'NONE', ( #6727 ), #7913, .T. ) ;
#4556=CARTESIAN_POINT ( 'NONE',  ( -0.5379290338433415641, -0.09448818897637796532, 0.2423824958184910838 ) ) ;
#4559=DIRECTION ( 'NONE',  ( -0.000000000000000000, -1.000000000000000000, -0.000000000000000000 ) ) ;
#4563=CARTESIAN_POINT ( 'NONE',  ( 0.000000000000000000, -0.1023622047244094474, -0.1614173228346456879 ) ) ;
#4564=CIRCLE ( 'NONE', #3052, 0.003937007874015724558 ) ;
#4565=DIRECTION ( 'NONE',  ( 0.5000000000000005551, 0.000000000000000000, -0.8660254037844384856 ) ) ;
#4568=DIRECTION ( 'NONE',  ( 0.4999999999999979461, -0.000000000000000000, 0.8660254037844398178 ) ) ;
#4569=ORIENTED_EDGE ( 'NONE', *, *, #13482, .T. ) ;
#4570=VERTEX_POINT ( 'NONE', #9317 ) ;
#4571=ORIENTED_EDGE ( 'NONE', *, *, #8586, .T. ) ;
#4575=EDGE_CURVE ( 'NONE', #8847, #13377, #11517, .T. ) ;
#4579=CARTESIAN_POINT ( 'NONE',  ( -0.2919796512831349111, -0.2952755905511811330, 0.2458576371656082671 ) ) ;
#4580=CARTESIAN_POINT ( 'NONE',  ( -0.2364476915723336681, -0.1023622047244094474, 0.06377609659094583827 ) ) ;
#4583=DIRECTION ( 'NONE',  ( -1.000000000000000000, 1.734723475976817507E-14, 0.000000000000000000 ) ) ;
#4584=CARTESIAN_POINT ( 'NONE',  ( 0.4586614173228352742, -0.09448818897637796532, 0.3875520507749248833 ) ) ;
#4585=CIRCLE ( 'NONE', #6834, 0.03937007874015752140 ) ;
#4588=CIRCLE ( 'NONE', #6557, 0.007874015748031482076 ) ;
#4592=CIRCLE ( 'NONE', #2088, 0.003937007874015724558 ) ;
#4595=VECTOR ( 'NONE', #14298, 39.37007874015748143 ) ;
#4596=DIRECTION ( 'NONE',  ( 0.000000000000000000, 0.000000000000000000, -1.000000000000000000 ) ) ;
#4599=ORIENTED_EDGE ( 'NONE', *, *, #8540, .T. ) ;
#4600=CARTESIAN_POINT ( 'NONE',  ( -0.1586168312385622392, -0.003937007874015747977, -0.5890199605878065903 ) ) ;
#4601=EDGE_CURVE ( 'NONE', #1202, #984, #6558, .T. ) ;
#4603=FACE_OUTER_BOUND ( 'NONE', #9452, .T. ) ;
#4608=CIRCLE ( 'NONE', #870, 0.1535433070866141780 ) ;
#4612=CARTESIAN_POINT ( 'NONE',  ( -0.4749369078591176296, -0.4881889763779528324, 0.3514880584999472424 ) ) ;
#4616=CARTESIAN_POINT ( 'NONE',  ( -0.4330708661417336236, -0.09448818897637796532, 0.4318761856142863120 ) ) ;
#4620=LINE ( 'NONE', #6013, #3727 ) ;
#4621=CIRCLE ( 'NONE', #908, 0.003937007874015724558 ) ;
#4623=CARTESIAN_POINT ( 'NONE',  ( 0.2393297813660762996, -0.4921259842519685179, 0.06089400679746265199 ) ) ;
#4626=ADVANCED_FACE ( 'NONE', ( #12929 ), #15353, .T. ) ;
#4628=TOROIDAL_SURFACE ( 'NONE', #137, 0.04330708661417328326, 0.003937007874015747977 ) ;
#4632=DIRECTION ( 'NONE',  ( 0.000000000000000000, 1.000000000000000000, 0.000000000000000000 ) ) ;
#4634=CIRCLE ( 'NONE', #8391, 0.04330708661417331101 ) ;
#4639=CYLINDRICAL_SURFACE ( 'NONE', #8340, 0.003937007874015721089 ) ;
#4640=LINE ( 'NONE', #7058, #8395 ) ;
#4641=AXIS2_PLACEMENT_3D ( 'NONE', #5291, #10091, #13707 ) ;
#4644=CARTESIAN_POINT ( 'NONE',  ( -0.4342073824196659437, -0.003937007874015747977, 0.4299076816772785525 ) ) ;
#4646=DIRECTION ( 'NONE',  ( -0.8660254037844381525, 0.000000000000000000, -0.5000000000000009992 ) ) ;
#4648=ORIENTED_EDGE ( 'NONE', *, *, #6946, .F. ) ;
#4653=AXIS2_PLACEMENT_3D ( 'NONE', #3565, #11741, #1003 ) ;
#4657=AXIS2_PLACEMENT_3D ( 'NONE', #12037, #7473, #351 ) ;
#4658=ORIENTED_EDGE ( 'NONE', *, *, #750, .T. ) ;
#4659=EDGE_CURVE ( 'NONE', #10534, #13283, #7206, .T. ) ;
#4660=EDGE_LOOP ( 'NONE', ( #4514, #6469, #14892, #14745 ) ) ;
#4661=ORIENTED_EDGE ( 'NONE', *, *, #2300, .F. ) ;
#4662=ORIENTED_EDGE ( 'NONE', *, *, #15389, .T. ) ;
#4670=CIRCLE ( 'NONE', #6647, 0.003937007874015724558 ) ;
#4674=EDGE_CURVE ( 'NONE', #13441, #11452, #10656, .T. ) ;
#4675=CARTESIAN_POINT ( 'NONE',  ( -0.09842519685028340570, -0.09842519685039370636, -0.5870514566507987197 ) ) ;
#4677=CYLINDRICAL_SURFACE ( 'NONE', #14171, 0.003937007874015721089 ) ;
#4678=AXIS2_PLACEMENT_3D ( 'NONE', #1442, #11051, #14359 ) ;
#4679=EDGE_CURVE ( 'NONE', #12819, #4401, #4608, .T. ) ;
#4681=ADVANCED_FACE ( 'NONE', ( #8461 ), #13629, .T. ) ;
#4682=ORIENTED_EDGE ( 'NONE', *, *, #9953, .F. ) ;
#4683=EDGE_LOOP ( 'NONE', ( #12719, #14615, #8944 ) ) ;
#4685=EDGE_LOOP ( 'NONE', ( #4661, #10845, #3985, #15346, #7988, #4831, #10043, #875, #14390, #5370 ) ) ;
#4686=AXIS2_PLACEMENT_3D ( 'NONE', #3071, #5651, #7851 ) ;
#4691=CIRCLE ( 'NONE', #1936, 0.1574803149606299191 ) ;
#4692=DIRECTION ( 'NONE',  ( -0.000000000000000000, -1.000000000000000000, -0.000000000000000000 ) ) ;
#4694=FACE_OUTER_BOUND ( 'NONE', #6641, .T. ) ;
#4696=CIRCLE ( 'NONE', #4441, 0.003937007874015724558 ) ;
#4697=EDGE_LOOP ( 'NONE', ( #61, #4845, #7127, #2948 ) ) ;
#4700=ORIENTED_EDGE ( 'NONE', *, *, #614, .F. ) ;
#4701=VECTOR ( 'NONE', #11950, 39.37007874015748143 ) ;
#4702=CARTESIAN_POINT ( 'NONE',  ( -0.4749369078591176851, -0.4921259842519685179, 0.3514880584999471314 ) ) ;
#4703=DIRECTION ( 'NONE',  ( 0.000000000000000000, -1.000000000000000000, 0.000000000000000000 ) ) ;
#4705=CARTESIAN_POINT ( 'NONE',  ( 0.1618514667033794374, -0.4921259842519685179, 0.2161887458866224576 ) ) ;
#4710=CARTESIAN_POINT ( 'NONE',  ( 0.4625984251968510708, -0.4921259842519685179, 0.3807329531073309070 ) ) ;
#4713=VERTEX_POINT ( 'NONE', #14095 ) ;
#4715=ADVANCED_FACE ( 'NONE', ( #3367 ), #13236, .F. ) ;
#4717=VERTEX_POINT ( 'NONE', #3684 ) ;
#4718=ORIENTED_EDGE ( 'NONE', *, *, #9455, .F. ) ;
#4719=VECTOR ( 'NONE', #15279, 39.37007874015748854 ) ;
#4720=DIRECTION ( 'NONE',  ( 0.4999999999999998335, -0.000000000000000000, 0.8660254037844388186 ) ) ;
#4726=DIRECTION ( 'NONE',  ( 0.000000000000000000, 0.000000000000000000, -1.000000000000000000 ) ) ;
#4728=VERTEX_POINT ( 'NONE', #11829 ) ;
#4733=EDGE_CURVE ( 'NONE', #2079, #1202, #2338, .T. ) ;
#4735=ORIENTED_EDGE ( 'NONE', *, *, #6269, .F. ) ;
#4737=VERTEX_POINT ( 'NONE', #10879 ) ;
#4738=ADVANCED_FACE ( 'NONE', ( #13388 ), #4054, .T. ) ;
#4743=CARTESIAN_POINT ( 'NONE',  ( -0.3117681530218310848, -0.2952755905511811330, 0.2981971199768678193 ) ) ;
#4745=DIRECTION ( 'NONE',  ( 0.000000000000000000, 0.000000000000000000, 1.000000000000000000 ) ) ;
#4750=ORIENTED_EDGE ( 'NONE', *, *, #11500, .T. ) ;
#4753=VERTEX_POINT ( 'NONE', #1721 ) ;
#4758=EDGE_CURVE ( 'NONE', #2746, #4753, #13868, .T. ) ;
#4764=CARTESIAN_POINT ( 'NONE',  ( 0.1023622047244638067, -0.4921259842519685179, -0.2472069366676780122 ) ) ;
#4765=CARTESIAN_POINT ( 'NONE',  ( -0.2393297813659119588, -0.4881889763779528324, 0.06089400679736758221 ) ) ;
#4775=CARTESIAN_POINT ( 'NONE',  ( -0.06692913385815749128, -0.4881889763779528324, -0.2377126739438355507 ) ) ;
#4776=DIRECTION ( 'NONE',  ( -0.4999999999999998335, -0.000000000000000000, -0.8660254037844388186 ) ) ;
#4777=ORIENTED_EDGE ( 'NONE', *, *, #13134, .F. ) ;
#4779=CARTESIAN_POINT ( 'NONE',  ( 0.5379290338433416752, -0.09842519685039370636, 0.2423824958184916112 ) ) ;
#4783=CARTESIAN_POINT ( 'NONE',  ( 0.1763376553817700698, -0.09842519685039370636, 0.1699995694788709322 ) ) ;
#4786=LINE ( 'NONE', #10811, #11193 ) ;
#4787=EDGE_CURVE ( 'NONE', #713, #6899, #1489, .T. ) ;
#4790=CARTESIAN_POINT ( 'NONE',  ( -0.1552072824047652788, -0.003937007874015747977, -0.5870514566507987197 ) ) ;
#4793=EDGE_CURVE ( 'NONE', #7774, #2681, #6398, .T. ) ;
#4797=ORIENTED_EDGE ( 'NONE', *, *, #5024, .T. ) ;
#4798=CARTESIAN_POINT ( 'NONE',  ( -0.1734555655881918346, -0.4881889763779528324, 0.1728816592724491952 ) ) ;
#4812=VERTEX_POINT ( 'NONE', #9866 ) ;
#4816=EDGE_CURVE ( 'NONE', #6744, #5934, #2844, .T. ) ;
#4818=CARTESIAN_POINT ( 'NONE',  ( -0.05905511811012598145, -0.1023622047244094474, -0.2377126739438355507 ) ) ;
#4819=EDGE_CURVE ( 'NONE', #13305, #3451, #7111, .T. ) ;
#4821=CARTESIAN_POINT ( 'NONE',  ( -0.2393297813659119588, -0.4921259842519685179, 0.06089400679736759608 ) ) ;
#4824=AXIS2_PLACEMENT_3D ( 'NONE', #4201, #10301, #11171 ) ;
#4827=CARTESIAN_POINT ( 'NONE',  ( 0.4586614173228352742, -0.1023622047244094474, 0.3875520507749248833 ) ) ;
#4830=CARTESIAN_POINT ( 'NONE',  ( 0.05905511811029059283, -0.1023622047244094474, -0.2377126739437405434 ) ) ;
#4831=ORIENTED_EDGE ( 'NONE', *, *, #8258, .T. ) ;
#4833=EDGE_CURVE ( 'NONE', #10116, #13891, #2564, .T. ) ;
#4836=CIRCLE ( 'NONE', #6317, 0.04330708661417329020 ) ;
#4840=CARTESIAN_POINT ( 'NONE',  ( 0.09842519685044814892, -0.2952755905511811330, -0.4190977005962941426 ) ) ;
#4843=DIRECTION ( 'NONE',  ( -1.000000000000000000, 0.000000000000000000, 0.000000000000000000 ) ) ;
#4845=ORIENTED_EDGE ( 'NONE', *, *, #9761, .T. ) ;
#4849=AXIS2_PLACEMENT_3D ( 'NONE', #282, #934, #13210 ) ;
#4850=CIRCLE ( 'NONE', #12112, 0.003937007874015724558 ) ;
#4852=AXIS2_PLACEMENT_3D ( 'NONE', #12967, #6926, #985 ) ;
#4853=ORIENTED_EDGE ( 'NONE', *, *, #10764, .T. ) ;
#4858=ORIENTED_EDGE ( 'NONE', *, *, #998, .F. ) ;
#4859=ORIENTED_EDGE ( 'NONE', *, *, #550, .T. ) ;
#4861=AXIS2_PLACEMENT_3D ( 'NONE', #11151, #13501, #9039 ) ;
#4862=AXIS2_PLACEMENT_3D ( 'NONE', #6477, #8691, #11264 ) ;
#4863=CIRCLE ( 'NONE', #6862, 0.03937007874015752140 ) ;
#4868=CARTESIAN_POINT ( 'NONE',  ( 0.2393297813660762718, -0.1023622047244094474, 0.06089400679746260342 ) ) ;
#4870=CARTESIAN_POINT ( 'NONE',  ( -0.1734555655881918346, -0.4921259842519685179, 0.1728816592724491952 ) ) ;
#4875=LINE ( 'NONE', #1512, #8675 ) ;
#4876=CIRCLE ( 'NONE', #13895, 0.003937007874015721089 ) ;
#4877=CIRCLE ( 'NONE', #10884, 0.003937007874015741038 ) ;
#4878=AXIS2_PLACEMENT_3D ( 'NONE', #9453, #7164, #12592 ) ;
#4881=EDGE_LOOP ( 'NONE', ( #7931, #14271, #5145 ) ) ;
#4883=VERTEX_POINT ( 'NONE', #12599 ) ;
#4884=FACE_OUTER_BOUND ( 'NONE', #9, .T. ) ;
#4885=CARTESIAN_POINT ( 'NONE',  ( 0.4330708661417309036, 0.000000000000000000, 0.4279391777402732910 ) ) ;
#4889=CARTESIAN_POINT ( 'NONE',  ( -0.6582248459352179060, -0.2952755905511811330, -0.3018834747714004840 ) ) ;
#4890=CIRCLE ( 'NONE', #4382, 0.003937007874015724558 ) ;
#4892=AXIS2_PLACEMENT_3D ( 'NONE', #4483, #8248, #15459 ) ;
#4896=CIRCLE ( 'NONE', #9413, 0.003937007874015724558 ) ;
#4901=VECTOR ( 'NONE', #799, 39.37007874015748143 ) ;
#4903=CIRCLE ( 'NONE', #4653, 0.003937007874015758385 ) ;
#4906=ORIENTED_EDGE ( 'NONE', *, *, #7223, .F. ) ;
#4907=TOROIDAL_SURFACE ( 'NONE', #10169, 0.04330708661417328326, 0.003937007874015747977 ) ;
#4909=DIRECTION ( 'NONE',  ( 1.770352960217306852E-32, 1.000000000000000000, -1.224646799147353207E-16 ) ) ;
#4910=LINE ( 'NONE', #8510, #13985 ) ;
#4911=CARTESIAN_POINT ( 'NONE',  ( 0.4572203724260462399, -0.1023622047244094474, 0.3821739980041199969 ) ) ;
#4912=CARTESIAN_POINT ( 'NONE',  ( 0.4788739157331329821, -0.1023622047244094474, 0.3446689608323529885 ) ) ;
#4913=DIRECTION ( 'NONE',  ( 0.8660254037844383745, 0.000000000000000000, -0.5000000000000004441 ) ) ;
#4916=DIRECTION ( 'NONE',  ( -0.000000000000000000, -1.000000000000000000, -0.000000000000000000 ) ) ;
#4917=CARTESIAN_POINT ( 'NONE',  ( -0.09842519685028335019, -0.2952755905511811330, -0.4190977005962941981 ) ) ;
#4919=AXIS2_PLACEMENT_3D ( 'NONE', #647, #12313, #14817 ) ;
#4920=ORIENTED_EDGE ( 'NONE', *, *, #6921, .T. ) ;
#4921=ORIENTED_EDGE ( 'NONE', *, *, #12573, .F. ) ;
#4923=EDGE_CURVE ( 'NONE', #14663, #10930, #3620, .T. ) ;
#4924=ORIENTED_EDGE ( 'NONE', *, *, #2126, .F. ) ;
#4931=LINE ( 'NONE', #311, #15127 ) ;
#4932=VECTOR ( 'NONE', #8234, 39.37007874015748143 ) ;
#4933=DIRECTION ( 'NONE',  ( 0.000000000000000000, 1.000000000000000000, -0.000000000000000000 ) ) ;
#4936=ORIENTED_EDGE ( 'NONE', *, *, #11508, .T. ) ;
#4937=CARTESIAN_POINT ( 'NONE',  ( -0.09842519685028361387, -0.4921259842519685179, -3.421829314686310476E-17 ) ) ;
#4940=ORIENTED_EDGE ( 'NONE', *, *, #7525, .F. ) ;
#4941=EDGE_LOOP ( 'NONE', ( #9242, #1530, #13526, #9681 ) ) ;
#4942=AXIS2_PLACEMENT_3D ( 'NONE', #1441, #5018, #12253 ) ;
#4944=DIRECTION ( 'NONE',  ( -0.8660254037844405950, -7.511572993685826514E-15, -0.4999999999999967248 ) ) ;
#4946=AXIS2_PLACEMENT_3D ( 'NONE', #7789, #4266, #12341 ) ;
#4948=DIRECTION ( 'NONE',  ( 0.000000000000000000, 0.000000000000000000, -1.000000000000000000 ) ) ;
#4950=DIRECTION ( 'NONE',  ( -0.000000000000000000, 1.000000000000000000, -0.000000000000000000 ) ) ;
#4953=CARTESIAN_POINT ( 'NONE',  ( -0.1574803149606299191, -0.09448818897637796532, -0.5870514566507987197 ) ) ;
#4955=CARTESIAN_POINT ( 'NONE',  ( 0.05905511811029064834, -0.1023622047244094474, -0.5909884645248143498 ) ) ;
#4957=AXIS2_PLACEMENT_3D ( 'NONE', #5629, #10427, #12773 ) ;
#4959=ORIENTED_EDGE ( 'NONE', *, *, #10498, .F. ) ;
#4960=ORIENTED_EDGE ( 'NONE', *, *, #1427, .T. ) ;
#4961=ADVANCED_FACE ( 'NONE', ( #6782 ), #12529, .T. ) ;
#4964=DIRECTION ( 'NONE',  ( 0.4999999999999966693, 0.000000000000000000, 0.8660254037844405950 ) ) ;
#4968=CARTESIAN_POINT ( 'NONE',  ( -0.1023622047242991467, -0.4921259842519685179, -0.5870514566507987197 ) ) ;
#4970=CARTESIAN_POINT ( 'NONE',  ( 0.000000000000000000, -0.4921259842519685179, 0.000000000000000000 ) ) ;
#4975=DIRECTION ( 'NONE',  ( -0.000000000000000000, 1.000000000000000000, 0.000000000000000000 ) ) ;
#4976=CARTESIAN_POINT ( 'NONE',  ( -0.06692913385815735250, -0.1023622047244094474, -0.5870514566507987197 ) ) ;
#4977=DIRECTION ( 'NONE',  ( 0.000000000000000000, -1.734723475976802677E-14, -1.000000000000000000 ) ) ;
#4982=EDGE_CURVE ( 'NONE', #2526, #9714, #1613, .T. ) ;
#4983=FACE_OUTER_BOUND ( 'NONE', #15229, .T. ) ;
#4986=EDGE_CURVE ( 'NONE', #12009, #13441, #10369, .T. ) ;
#4987=ORIENTED_EDGE ( 'NONE', *, *, #14159, .T. ) ;
#4988=ORIENTED_EDGE ( 'NONE', *, *, #1305, .T. ) ;
#4992=CARTESIAN_POINT ( 'NONE',  ( 0.000000000000000000, -0.09842519685039370636, -0.1614173228346456879 ) ) ;
#4993=CARTESIAN_POINT ( 'NONE',  ( 0.5894146648244296127, -0.09842519685039370636, 0.1571437749735215827 ) ) ;
#4995=ADVANCED_FACE ( 'NONE', ( #8041 ), #7589, .T. ) ;
#4996=DIRECTION ( 'NONE',  ( 0.8660254037844389297, 0.000000000000000000, -0.4999999999999996669 ) ) ;
#5002=DIRECTION ( 'NONE',  ( 0.5000000000000004441, 0.000000000000000000, -0.8660254037844384856 ) ) ;
#5004=EDGE_CURVE ( 'NONE', #8246, #3213, #9371, .T. ) ;
#5005=EDGE_LOOP ( 'NONE', ( #4292, #12268, #6015, #10184, #14292, #6120, #9669, #1038, #406, #6880 ) ) ;
#5014=ORIENTED_EDGE ( 'NONE', *, *, #5861, .T. ) ;
#5015=DIRECTION ( 'NONE',  ( -0.000000000000000000, -1.000000000000000000, -0.000000000000000000 ) ) ;
#5016=DIRECTION ( 'NONE',  ( -3.469446951953635015E-14, 0.000000000000000000, -1.000000000000000000 ) ) ;
#5018=DIRECTION ( 'NONE',  ( -0.4999999999999986122, -0.000000000000000000, -0.8660254037844394848 ) ) ;
#5021=ORIENTED_EDGE ( 'NONE', *, *, #944, .T. ) ;
#5024=EDGE_CURVE ( 'NONE', #3640, #9446, #13363, .T. ) ;
#5025=DIRECTION ( 'NONE',  ( -0.000000000000000000, -1.000000000000000000, -0.000000000000000000 ) ) ;
#5036=ORIENTED_EDGE ( 'NONE', *, *, #1585, .F. ) ;
#5037=EDGE_LOOP ( 'NONE', ( #13372, #9567, #1783, #8262 ) ) ;
#5038=EDGE_CURVE ( 'NONE', #5966, #15216, #2473, .T. ) ;
#5039=DIRECTION ( 'NONE',  ( 0.5000000000000004441, -7.511572993685840713E-15, 0.8660254037844384856 ) ) ;
#5043=CYLINDRICAL_SURFACE ( 'NONE', #9141, 0.003937007874015749712 ) ;
#5047=DIRECTION ( 'NONE',  ( 0.4999999999999979461, 0.000000000000000000, 0.8660254037844398178 ) ) ;
#5050=VERTEX_POINT ( 'NONE', #7244 ) ;
#5054=FACE_OUTER_BOUND ( 'NONE', #11023, .T. ) ;
#5057=AXIS2_PLACEMENT_3D ( 'NONE', #4764, #8360, #13063 ) ;
#5061=TOROIDAL_SURFACE ( 'NONE', #13836, 0.04330708661417328326, 0.003937007874015747977 ) ;
#5067=FACE_OUTER_BOUND ( 'NONE', #3611, .T. ) ;
#5069=ORIENTED_EDGE ( 'NONE', *, *, #12584, .T. ) ;
#5071=CIRCLE ( 'NONE', #13843, 0.003937007874015741038 ) ;
#5072=AXIS2_PLACEMENT_3D ( 'NONE', #6527, #5356, #3026 ) ;
#5074=AXIS2_PLACEMENT_3D ( 'NONE', #12648, #11477, #10754 ) ;
#5082=CARTESIAN_POINT ( 'NONE',  ( 0.06692913385832208184, -0.2952755905511811330, -0.4190977005962941426 ) ) ;
#5083=AXIS2_PLACEMENT_3D ( 'NONE', #7388, #12187, #13206 ) ;
#5085=VERTEX_POINT ( 'NONE', #10837 ) ;
#5086=DIRECTION ( 'NONE',  ( 1.000000000000000000, -0.000000000000000000, -0.000000000000000000 ) ) ;
#5087=CIRCLE ( 'NONE', #13606, 0.003937007874015747109 ) ;
#5088=DIRECTION ( 'NONE',  ( 1.000000000000000000, -0.000000000000000000, -0.000000000000000000 ) ) ;
#5089=VECTOR ( 'NONE', #9498, 39.37007874015748143 ) ;
#5090=DIRECTION ( 'NONE',  ( 0.000000000000000000, 0.000000000000000000, -1.000000000000000000 ) ) ;
#5095=ORIENTED_EDGE ( 'NONE', *, *, #10460, .F. ) ;
#5098=VERTEX_POINT ( 'NONE', #1295 ) ;
#5099=AXIS2_PLACEMENT_3D ( 'NONE', #6276, #130, #7398 ) ;
#5100=EDGE_CURVE ( 'NONE', #11872, #13296, #3793, .T. ) ;
#5101=ORIENTED_EDGE ( 'NONE', *, *, #182, .F. ) ;
#5102=CIRCLE ( 'NONE', #2860, 0.003937007874015741038 ) ;
#5103=DIRECTION ( 'NONE',  ( 0.5000000000000004441, 0.000000000000000000, -0.8660254037844382635 ) ) ;
#5104=CARTESIAN_POINT ( 'NONE',  ( 0.06299212598430634080, -0.4921259842519685179, -0.2366577558633030653 ) ) ;
#5107=ADVANCED_FACE ( 'NONE', ( #14607 ), #11000, .T. ) ;
#5108=CYLINDRICAL_SURFACE ( 'NONE', #12849, 0.003937007874015740171 ) ;
#5109=CARTESIAN_POINT ( 'NONE',  ( 0.3137366569588399545, -0.2952755905511811330, 0.2947875711430715251 ) ) ;
#5110=SHAPE_DEFINITION_REPRESENTATION ( #9430, #12705 ) ;
#5111=DIRECTION ( 'NONE',  ( 0.8660254037844383745, -0.000000000000000000, 0.5000000000000002220 ) ) ;
#5113=CARTESIAN_POINT ( 'NONE',  ( -0.1724006475077544398, -0.09842519685039370636, 0.1689446513984334541 ) ) ;
#5114=DIRECTION ( 'NONE',  ( 0.5000000000000004441, 0.000000000000000000, -0.8660254037844382635 ) ) ;
#5116=AXIS2_PLACEMENT_3D ( 'NONE', #3546, #197, #7372 ) ;
#5120=ORIENTED_EDGE ( 'NONE', *, *, #14129, .F. ) ;
#5123=VECTOR ( 'NONE', #7993, 39.37007874015748143 ) ;
#5125=CIRCLE ( 'NONE', #3651, 0.003937007874015750579 ) ;
#5126=DIRECTION ( 'NONE',  ( 1.060575238724907285E-16, 1.000000000000000000, -6.123233995736759873E-17 ) ) ;
#5130=AXIS2_PLACEMENT_3D ( 'NONE', #14735, #1722, #13848 ) ;
#5131=CARTESIAN_POINT ( 'NONE',  ( 0.1618514667033794374, -0.09842519685039370636, 0.2161887458866224576 ) ) ;
#5140=AXIS2_PLACEMENT_3D ( 'NONE', #12346, #3744, #11083 ) ;
#5142=EDGE_LOOP ( 'NONE', ( #4016, #12538, #9502, #9655 ) ) ;
#5144=ORIENTED_EDGE ( 'NONE', *, *, #5004, .F. ) ;
#5145=ORIENTED_EDGE ( 'NONE', *, *, #4242, .F. ) ;
#5149=CARTESIAN_POINT ( 'NONE',  ( -0.1028896637645180384, -0.4881889763779528324, -0.2462933508112025438 ) ) ;
#5155=ORIENTED_EDGE ( 'NONE', *, *, #12182, .F. ) ;
#5157=CIRCLE ( 'NONE', #8943, 0.003937007874015780069 ) ;
#5158=UNCERTAINTY_MEASURE_WITH_UNIT (LENGTH_MEASURE( 1.000000000000000082E-05 ), #9292, 'distance_accuracy_value', 'NONE');
#5159=ORIENTED_EDGE ( 'NONE', *, *, #14082, .T. ) ;
#5160=VECTOR ( 'NONE', #15124, 39.37007874015748143 ) ;
#5162=AXIS2_PLACEMENT_3D ( 'NONE', #1792, #15034, #15102 ) ;
#5171=AXIS2_PLACEMENT_3D ( 'NONE', #3919, #11198, #4059 ) ;
#5176=ADVANCED_FACE ( 'NONE', ( #8798 ), #12634, .T. ) ;
#5177=ORIENTED_EDGE ( 'NONE', *, *, #2996, .T. ) ;
#5178=VECTOR ( 'NONE', #6767, 39.37007874015748143 ) ;
#5181=FACE_OUTER_BOUND ( 'NONE', #7888, .T. ) ;
#5190=DIRECTION ( 'NONE',  ( -1.000000000000000000, 0.000000000000000000, -1.445602896647338424E-16 ) ) ;
#5191=CIRCLE ( 'NONE', #968, 0.003937007874015724558 ) ;
#5192=EDGE_CURVE ( 'NONE', #7138, #14594, #3636, .T. ) ;
#5196=EDGE_CURVE ( 'NONE', #14862, #7482, #15134, .T. ) ;
#5197=FACE_OUTER_BOUND ( 'NONE', #8574, .T. ) ;
#5198=ADVANCED_FACE ( 'NONE', ( #7773 ), #10220, .T. ) ;
#5199=ORIENTED_EDGE ( 'NONE', *, *, #11637, .F. ) ;
#5204=CARTESIAN_POINT ( 'NONE',  ( 0.1618514667033794374, -0.1023622047244094474, 0.2161887458866224576 ) ) ;
#5206=CARTESIAN_POINT ( 'NONE',  ( -0.5894146648244306119, -0.09448818897637796532, 0.1571437749735178357 ) ) ;
#5208=DIRECTION ( 'NONE',  ( -0.4999999999999966693, 0.000000000000000000, -0.8660254037844405950 ) ) ;
#5210=DIRECTION ( 'NONE',  ( -0.5000000000000001110, -0.000000000000000000, -0.8660254037844385966 ) ) ;
#5213=EDGE_LOOP ( 'NONE', ( #7767, #2850, #1854, #15453, #15089, #10334, #4569, #40, #12072, #10045, #13787, #6908, #3109, #8223, #5069, #12985 ) ) ;
#5214=ORIENTED_EDGE ( 'NONE', *, *, #7986, .F. ) ;
#5216=VERTEX_POINT ( 'NONE', #12415 ) ;
#5224=CARTESIAN_POINT ( 'NONE',  ( 0.1724006475077543565, -0.1023622047244094474, 0.1689446513984334541 ) ) ;
#5228=ORIENTED_EDGE ( 'NONE', *, *, #998, .T. ) ;
#5231=ORIENTED_EDGE ( 'NONE', *, *, #12228, .T. ) ;
#5233=ORIENTED_EDGE ( 'NONE', *, *, #2028, .F. ) ;
#5235=DIRECTION ( 'NONE',  ( -0.8660254037844405950, 0.000000000000000000, -0.4999999999999966693 ) ) ;
#5238=EDGE_LOOP ( 'NONE', ( #14060, #5771, #989 ) ) ;
#5239=FACE_OUTER_BOUND ( 'NONE', #734, .T. ) ;
#5240=FACE_BOUND ( 'NONE', #15419, .T. ) ;
#5242=CARTESIAN_POINT ( 'NONE',  ( -0.09842519685028333631, -0.2952755905511811330, -0.4584677793364517195 ) ) ;
#5245=DIRECTION ( 'NONE',  ( 0.000000000000000000, 0.000000000000000000, -1.000000000000000000 ) ) ;
#5247=ORIENTED_EDGE ( 'NONE', *, *, #3938, .F. ) ;
#5252=DIRECTION ( 'NONE',  ( -0.5000000000000209832, -0.000000000000000000, -0.8660254037844266062 ) ) ;
#5256=CARTESIAN_POINT ( 'NONE',  ( 0.4749369078591172966, -0.4881889763779528324, 0.3514880584999470203 ) ) ;
#5257=EDGE_CURVE ( 'NONE', #12689, #13984, #4113, .T. ) ;
#5260=CARTESIAN_POINT ( 'NONE',  ( -0.4625984251968516259, -0.4881889763779528324, 0.3807329531073311846 ) ) ;
#5264=ORIENTED_EDGE ( 'NONE', *, *, #8307, .T. ) ;
#5266=EDGE_CURVE ( 'NONE', #2421, #6774, #15002, .T. ) ;
#5271=CARTESIAN_POINT ( 'NONE',  ( -0.4625984251968516259, -0.1023622047244094474, 0.3807329531073311846 ) ) ;
#5272=EDGE_CURVE ( 'NONE', #11465, #15025, #14379, .T. ) ;
#5277=DIRECTION ( 'NONE',  ( 0.4999999999999966693, 0.000000000000000000, -0.8660254037844405950 ) ) ;
#5284=EDGE_CURVE ( 'NONE', #10725, #675, #14767, .T. ) ;
#5286=CYLINDRICAL_SURFACE ( 'NONE', #2331, 0.003937007874015754916 ) ;
#5287=DIRECTION ( 'NONE',  ( -0.000000000000000000, -0.000000000000000000, -1.000000000000000000 ) ) ;
#5288=DIRECTION ( 'NONE',  ( 3.614007241618347785E-16, -0.000000000000000000, -1.000000000000000000 ) ) ;
#5290=EDGE_CURVE ( 'NONE', #15055, #3552, #7708, .T. ) ;
#5291=CARTESIAN_POINT ( 'NONE',  ( -0.1552072824047652788, -0.09842519685039370636, -0.5870514566507987197 ) ) ;
#5295=DIRECTION ( 'NONE',  ( -0.000000000000000000, -1.000000000000000000, -0.000000000000000000 ) ) ;
#5298=ORIENTED_EDGE ( 'NONE', *, *, #11437, .T. ) ;
#5301=EDGE_LOOP ( 'NONE', ( #3943, #9757, #10992, #5655 ) ) ;
#5303=VECTOR ( 'NONE', #6943, 39.37007874015748143 ) ;
#5305=CARTESIAN_POINT ( 'NONE',  ( -0.3294846884549020305, -0.2952755905511811330, 0.2675111804726948983 ) ) ;
#5309=ORIENTED_EDGE ( 'NONE', *, *, #14781, .F. ) ;
#5310=CARTESIAN_POINT ( 'NONE',  ( 0.2647411304680618027, -0.4881889763779528324, 0.03404161279868787859 ) ) ;
#5313=AXIS2_PLACEMENT_3D ( 'NONE', #8989, #4118, #5208 ) ;
#5315=EDGE_CURVE ( 'NONE', #253, #15013, #6751, .T. ) ;
#5318=EDGE_CURVE ( 'NONE', #14839, #8213, #11120, .T. ) ;
#5320=AXIS2_PLACEMENT_3D ( 'NONE', #10541, #4218, #11339 ) ;
#5324=LINE ( 'NONE', #6266, #168 ) ;
#5325=DIRECTION ( 'NONE',  ( 0.5000000000000001110, 0.000000000000000000, -0.8660254037844385966 ) ) ;
#5331=CIRCLE ( 'NONE', #3348, 0.1614173228346456879 ) ;
#5334=CARTESIAN_POINT ( 'NONE',  ( 0.4342073824196633347, -0.09842519685039370636, 0.4299076816772810505 ) ) ;
#5340=AXIS2_PLACEMENT_3D ( 'NONE', #9110, #5649, #9036 ) ;
#5343=DIRECTION ( 'NONE',  ( 0.5000000000000004441, -0.000000000000000000, -0.8660254037844383745 ) ) ;
#5344=VECTOR ( 'NONE', #14191, 39.37007874015748143 ) ;
#5345=VERTEX_POINT ( 'NONE', #6995 ) ;
#5348=CARTESIAN_POINT ( 'NONE',  ( -0.09842519685028340570, -0.1023622047244094474, -0.5909884645248143498 ) ) ;
#5351=CIRCLE ( 'NONE', #9384, 0.003937007874015724558 ) ;
#5352=CIRCLE ( 'NONE', #6361, 0.003937007874015749712 ) ;
#5353=CARTESIAN_POINT ( 'NONE',  ( -0.4307978335858689278, -0.09842519685039370636, 0.4279391777402706265 ) ) ;
#5356=DIRECTION ( 'NONE',  ( -1.000000000000000000, 0.000000000000000000, 0.000000000000000000 ) ) ;
#5357=TOROIDAL_SURFACE ( 'NONE', #2363, 0.04330708661417328326, 0.003937007874015747977 ) ;
#5358=CARTESIAN_POINT ( 'NONE',  ( 0.1618514667033794652, -0.1023622047244094474, 0.2161887458866224576 ) ) ;
#5359=EDGE_CURVE ( 'NONE', #105, #10242, #11738, .T. ) ;
#5364=ORIENTED_EDGE ( 'NONE', *, *, #708, .T. ) ;
#5365=ORIENTED_EDGE ( 'NONE', *, *, #9953, .T. ) ;
#5366=AXIS2_PLACEMENT_3D ( 'NONE', #12711, #13954, #4233 ) ;
#5368=CIRCLE ( 'NONE', #9398, 0.003937007874015750579 ) ;
#5370=ORIENTED_EDGE ( 'NONE', *, *, #14763, .T. ) ;
#5371=EDGE_CURVE ( 'NONE', #11768, #517, #13881, .T. ) ;
#5372=ORIENTED_EDGE ( 'NONE', *, *, #4271, .T. ) ;
#5375=DIRECTION ( 'NONE',  ( 0.000000000000000000, 0.000000000000000000, 1.000000000000000000 ) ) ;
#5379=DIRECTION ( 'NONE',  ( 0.000000000000000000, 0.000000000000000000, 1.000000000000000000 ) ) ;
#5381=AXIS2_PLACEMENT_3D ( 'NONE', #11057, #7531, #1586 ) ;
#5383=CIRCLE ( 'NONE', #3151, 0.003937007874015724558 ) ;
#5385=AXIS2_PLACEMENT_3D ( 'NONE', #8312, #6910, #6746 ) ;
#5386=ORIENTED_EDGE ( 'NONE', *, *, #1148, .F. ) ;
#5388=ADVANCED_FACE ( 'NONE', ( #4488 ), #5498, .T. ) ;
#5392=ORIENTED_EDGE ( 'NONE', *, *, #13235, .T. ) ;
#5393=ORIENTED_EDGE ( 'NONE', *, *, #14484, .T. ) ;
#5394=EDGE_CURVE ( 'NONE', #11324, #15288, #13135, .T. ) ;
#5402=DIRECTION ( 'NONE',  ( -0.5000000000000035527, -0.000000000000000000, 0.8660254037844365982 ) ) ;
#5403=ORIENTED_EDGE ( 'NONE', *, *, #12241, .F. ) ;
#5404=CARTESIAN_POINT ( 'NONE',  ( -0.06351958502436047538, -0.4881889763779528324, -0.2357441700068276802 ) ) ;
#5405=CARTESIAN_POINT ( 'NONE',  ( 0.000000000000000000, 0.000000000000000000, 0.000000000000000000 ) ) ;
#5414=ORIENTED_EDGE ( 'NONE', *, *, #13630, .F. ) ;
#5415=ORIENTED_EDGE ( 'NONE', *, *, #1773, .F. ) ;
#5418=VECTOR ( 'NONE', #11952, 39.37007874015748143 ) ;
#5419=ADVANCED_FACE ( 'NONE', ( #14126 ), #12956, .T. ) ;
#5422=CARTESIAN_POINT ( 'NONE',  ( -0.02952755905509086426, -0.09842519685039370636, -0.05114323250690790829 ) ) ;
#5426=DIRECTION ( 'NONE',  ( 0.5000000000000037748, -0.000000000000000000, 0.8660254037844365982 ) ) ;
#5427=DIRECTION ( 'NONE',  ( 0.4999999999999966693, 0.000000000000000000, -0.8660254037844405950 ) ) ;
#5428=AXIS2_PLACEMENT_3D ( 'NONE', #14186, #1191, #3455 ) ;
#5429=DIRECTION ( 'NONE',  ( 0.000000000000000000, 0.000000000000000000, 1.000000000000000000 ) ) ;
#5431=ORIENTED_EDGE ( 'NONE', *, *, #15304, .T. ) ;
#5433=ORIENTED_EDGE ( 'NONE', *, *, #3245, .T. ) ;
#5434=SPHERICAL_SURFACE ( 'NONE', #14135, 0.003937007874015747977 ) ;
#5436=CIRCLE ( 'NONE', #8445, 0.007874015748031504627 ) ;
#5439=DIRECTION ( 'NONE',  ( -0.8660254037844388186, 0.000000000000000000, 0.4999999999999998335 ) ) ;
#5441=DIRECTION ( 'NONE',  ( 1.000000000000000000, 0.000000000000000000, 0.000000000000000000 ) ) ;
#5446=AXIS2_PLACEMENT_3D ( 'NONE', #7440, #9565, #13173 ) ;
#5448=DIRECTION ( 'NONE',  ( -0.5000000000000035527, 0.000000000000000000, 0.8660254037844365982 ) ) ;
#5449=LINE ( 'NONE', #12517, #12660 ) ;
#5451=EDGE_LOOP ( 'NONE', ( #12154, #5365, #3191, #8245 ) ) ;
#5453=ORIENTED_EDGE ( 'NONE', *, *, #4125, .F. ) ;
#5454=ORIENTED_EDGE ( 'NONE', *, *, #6336, .F. ) ;
#5458=EDGE_CURVE ( 'NONE', #2367, #11305, #7852, .T. ) ;
#5459=DIRECTION ( 'NONE',  ( 0.000000000000000000, 0.000000000000000000, 1.000000000000000000 ) ) ;
#5462=LINE ( 'NONE', #8110, #15088 ) ;
#5466=DIRECTION ( 'NONE',  ( 0.5000000000000004441, -1.162044386198250571E-15, -0.8660254037844384856 ) ) ;
#5469=EDGE_LOOP ( 'NONE', ( #632, #3017, #3905, #1331 ) ) ;
#5475=DIRECTION ( 'NONE',  ( -0.5000000000000004441, 0.000000000000000000, 0.8660254037844384856 ) ) ;
#5478=FACE_OUTER_BOUND ( 'NONE', #7497, .T. ) ;
#5479=LINE ( 'NONE', #6731, #5123 ) ;
#5482=ADVANCED_FACE ( 'NONE', ( #2364 ), #3708, .F. ) ;
#5484=FACE_OUTER_BOUND ( 'NONE', #10149, .T. ) ;
#5485=DIRECTION ( 'NONE',  ( 0.000000000000000000, -1.000000000000000000, 0.000000000000000000 ) ) ;
#5494=DIRECTION ( 'NONE',  ( 0.8660254037844385966, 0.000000000000000000, 0.5000000000000001110 ) ) ;
#5498=CYLINDRICAL_SURFACE ( 'NONE', #9632, 0.003937007874015758385 ) ;
#5502=PLANE ( 'NONE',  #382 ) ;
#5503=DIRECTION ( 'NONE',  ( -0.5000000000000069944, -0.000000000000000000, -0.8660254037844347108 ) ) ;
#5506=EDGE_CURVE ( 'NONE', #14774, #13179, #8621, .T. ) ;
#5507=FACE_OUTER_BOUND ( 'NONE', #12554, .T. ) ;
#5510=FACE_OUTER_BOUND ( 'NONE', #7000, .T. ) ;
#5514=CARTESIAN_POINT ( 'NONE',  ( -0.1618514667033796040, -0.1023622047244094474, 0.2161887458866224854 ) ) ;
#5515=FACE_OUTER_BOUND ( 'NONE', #3837, .T. ) ;
#5518=VERTEX_POINT ( 'NONE', #12019 ) ;
#5520=VERTEX_POINT ( 'NONE', #7149 ) ;
#5522=ORIENTED_EDGE ( 'NONE', *, *, #7705, .T. ) ;
#5524=DIRECTION ( 'NONE',  ( 0.000000000000000000, -1.000000000000000000, 0.000000000000000000 ) ) ;
#5526=CARTESIAN_POINT ( 'NONE',  ( -0.4307978335858689278, -0.09448818897637796532, 0.4279391777402706265 ) ) ;
#5527=CARTESIAN_POINT ( 'NONE',  ( 0.1574803149606299191, -0.09842519685039370636, -0.5909884645248143498 ) ) ;
#5528=FACE_OUTER_BOUND ( 'NONE', #1253, .T. ) ;
#5531=CARTESIAN_POINT ( 'NONE',  ( 0.1618514667033794374, -0.09842519685039372024, 0.2122517380126066888 ) ) ;
#5535=VERTEX_POINT ( 'NONE', #6110 ) ;
#5536=ORIENTED_EDGE ( 'NONE', *, *, #224, .T. ) ;
#5538=ADVANCED_FACE ( 'NONE', ( #14281 ), #12168, .T. ) ;
#5540=DIRECTION ( 'NONE',  ( 0.4999999999999998890, 0.000000000000000000, 0.8660254037844385966 ) ) ;
#5542=DIRECTION ( 'NONE',  ( -1.000000000000000000, -0.000000000000000000, -0.000000000000000000 ) ) ;
#5543=CARTESIAN_POINT ( 'NONE',  ( 0.4749369078591172411, -0.4881889763779528324, 0.3514880584999470203 ) ) ;
#5544=ORIENTED_EDGE ( 'NONE', *, *, #11278, .T. ) ;
#5547=DIRECTION ( 'NONE',  ( -0.000000000000000000, -1.000000000000000000, -0.000000000000000000 ) ) ;
#5552=ORIENTED_EDGE ( 'NONE', *, *, #7286, .F. ) ;
#5555=ORIENTED_EDGE ( 'NONE', *, *, #4192, .T. ) ;
#5559=DIRECTION ( 'NONE',  ( -0.5000000000000001110, 0.000000000000000000, 0.8660254037844385966 ) ) ;
#5560=DIRECTION ( 'NONE',  ( -0.8660254037844381525, 0.000000000000000000, -0.5000000000000006661 ) ) ;
#5561=AXIS2_PLACEMENT_3D ( 'NONE', #2879, #1786, #5375 ) ;
#5562=VECTOR ( 'NONE', #13826, 39.37007874015748854 ) ;
#5564=EDGE_LOOP ( 'NONE', ( #14055, #7496, #1571, #7150 ) ) ;
#5566=CIRCLE ( 'NONE', #15086, 0.007874015748031482076 ) ;
#5567=DIRECTION ( 'NONE',  ( 0.000000000000000000, 1.000000000000000000, 0.000000000000000000 ) ) ;
#5568=CIRCLE ( 'NONE', #14846, 0.03937007874015754222 ) ;
#5572=EDGE_LOOP ( 'NONE', ( #8738, #3737, #15161, #7354 ) ) ;
#5575=DIRECTION ( 'NONE',  ( -0.5000000000000035527, -0.000000000000000000, 0.8660254037844365982 ) ) ;
#5581=AXIS2_PLACEMENT_3D ( 'NONE', #3009, #1825, #15006 ) ;
#5586=CARTESIAN_POINT ( 'NONE',  ( 0.5860051159906326523, -0.003937007874015747977, 0.1591122789105293422 ) ) ;
#5587=DIRECTION ( 'NONE',  ( 8.673617379884051249E-15, 1.000000000000000000, 0.000000000000000000 ) ) ;
#5593=TOROIDAL_SURFACE ( 'NONE', #9375, 0.1535433070866141780, 0.003937007874015747977 ) ;
#5594=AXIS2_PLACEMENT_3D ( 'NONE', #3004, #13744, #1682 ) ;
#5603=VECTOR ( 'NONE', #2511, 39.37007874015748143 ) ;
#5605=FACE_OUTER_BOUND ( 'NONE', #11699, .T. ) ;
#5611=DIRECTION ( 'NONE',  ( -0.000000000000000000, 1.000000000000000000, -0.000000000000000000 ) ) ;
#5617=LINE ( 'NONE', #7978, #12440 ) ;
#5618=DIRECTION ( 'NONE',  ( 0.000000000000000000, -1.000000000000000000, 0.000000000000000000 ) ) ;
#5622=ORIENTED_EDGE ( 'NONE', *, *, #14572, .T. ) ;
#5623=LINE ( 'NONE', #6725, #11630 ) ;
#5624=VECTOR ( 'NONE', #14983, 39.37007874015748143 ) ;
#5626=CIRCLE ( 'NONE', #2890, 0.03937007874015754222 ) ;
#5629=CARTESIAN_POINT ( 'NONE',  ( -0.2325106836983179270, -0.1023622047244094474, 0.06483101467138334406 ) ) ;
#5631=LINE ( 'NONE', #786, #5875 ) ;
#5633=CARTESIAN_POINT ( 'NONE',  ( 0.06692913385832212347, -0.09842519685039370636, -0.5909884645248143498 ) ) ;
#5635=DIRECTION ( 'NONE',  ( 0.000000000000000000, 0.000000000000000000, 1.000000000000000000 ) ) ;
#5636=CARTESIAN_POINT ( 'NONE',  ( -0.2393297813659119588, -0.4881889763779528324, 0.06089400679736758221 ) ) ;
#5637=ORIENTED_EDGE ( 'NONE', *, *, #3521, .F. ) ;
#5640=AXIS2_PLACEMENT_3D ( 'NONE', #234, #1626, #8818 ) ;
#5646=FACE_OUTER_BOUND ( 'NONE', #14112, .T. ) ;
#5649=DIRECTION ( 'NONE',  ( 0.000000000000000000, -1.000000000000000000, 0.000000000000000000 ) ) ;
#5651=DIRECTION ( 'NONE',  ( -0.4999999999999996114, 0.000000000000000000, -0.8660254037844389297 ) ) ;
#5653=EDGE_CURVE ( 'NONE', #7766, #15055, #11360, .T. ) ;
#5655=ORIENTED_EDGE ( 'NONE', *, *, #3555, .F. ) ;
#5656=DIRECTION ( 'NONE',  ( 1.000000000000000000, 0.000000000000000000, 0.000000000000000000 ) ) ;
#5657=CIRCLE ( 'NONE', #15180, 0.003937007874015758385 ) ;
#5661=ORIENTED_EDGE ( 'NONE', *, *, #13819, .F. ) ;
#5662=DIRECTION ( 'NONE',  ( -1.000000000000000000, -0.000000000000000000, -3.476578583725179813E-16 ) ) ;
#5663=EDGE_LOOP ( 'NONE', ( #3680, #13835, #322 ) ) ;
#5664=AXIS2_PLACEMENT_3D ( 'NONE', #11134, #12631, #10207 ) ;
#5665=ORIENTED_EDGE ( 'NONE', *, *, #5024, .F. ) ;
#5672=CARTESIAN_POINT ( 'NONE',  ( -0.4121618538092055584, -0.2952755905511811330, 0.1243101294532693024 ) ) ;
#5673=CARTESIAN_POINT ( 'NONE',  ( -0.4783464566929145900, -0.4881889763779528324, 0.3534565624369550574 ) ) ;
#5674=AXIS2_PLACEMENT_3D ( 'NONE', #12782, #10344, #15287 ) ;
#5675=EDGE_CURVE ( 'NONE', #12501, #897, #10115, .T. ) ;
#5679=ORIENTED_EDGE ( 'NONE', *, *, #6760, .F. ) ;
#5683=TOROIDAL_SURFACE ( 'NONE', #3884, 0.007874015748031495954, 0.003937007874015747977 ) ;
#5686=CARTESIAN_POINT ( 'NONE',  ( -0.06299212598414161146, -0.09842519685039372024, -0.5870514566507987197 ) ) ;
#5696=EDGE_CURVE ( 'NONE', #6393, #10309, #10644, .T. ) ;
#5697=DIRECTION ( 'NONE',  ( 0.000000000000000000, 0.000000000000000000, -1.000000000000000000 ) ) ;
#5698=AXIS2_PLACEMENT_3D ( 'NONE', #10904, #4950, #13952 ) ;
#5701=( GEOMETRIC_REPRESENTATION_CONTEXT ( 3 ) GLOBAL_UNCERTAINTY_ASSIGNED_CONTEXT ( ( #9080 ) ) GLOBAL_UNIT_ASSIGNED_CONTEXT ( ( #10155, #10298, #2777 ) ) REPRESENTATION_CONTEXT ( 'NONE', 'WORKASPACE' ) );
#5704=DIRECTION ( 'NONE',  ( -0.8660254037844384856, 6.349528607487585212E-15, 0.5000000000000004441 ) ) ;
#5705=CARTESIAN_POINT ( 'NONE',  ( 0.2325106836984822400, -0.09842519685039370636, 0.06483101467147835140 ) ) ;
#5707=CARTESIAN_POINT ( 'NONE',  ( -0.1638199706403874467, -0.1023622047244094474, 0.2127791970528254695 ) ) ;
#5708=SPHERICAL_SURFACE ( 'NONE', #3387, 0.003937007874015747977 ) ;
#5709=VERTEX_POINT ( 'NONE', #11212 ) ;
#5711=LINE ( 'NONE', #4710, #8356 ) ;
#5712=DIRECTION ( 'NONE',  ( -0.8660254037844384856, 0.000000000000000000, -0.5000000000000002220 ) ) ;
#5713=ORIENTED_EDGE ( 'NONE', *, *, #1778, .F. ) ;
#5714=CARTESIAN_POINT ( 'NONE',  ( 0.1540707661268329032, -0.09448818897637796532, -0.5890199605878065903 ) ) ;
#5715=ORIENTED_EDGE ( 'NONE', *, *, #7024, .T. ) ;
#5716=ADVANCED_FACE ( 'NONE', ( #494 ), #7637, .F. ) ;
#5719=DIRECTION ( 'NONE',  ( 0.8660254037844347108, -0.000000000000000000, -0.5000000000000069944 ) ) ;
#5721=CARTESIAN_POINT ( 'NONE',  ( -0.3137366569588388998, -0.2952755905511811330, 0.2947875711430708590 ) ) ;
#5723=DIRECTION ( 'NONE',  ( 0.000000000000000000, -1.000000000000000000, 0.000000000000000000 ) ) ;
#5725=EDGE_LOOP ( 'NONE', ( #5899, #13158, #5247, #13901 ) ) ;
#5727=DIRECTION ( 'NONE',  ( 0.4999999999999922284, -0.000000000000000000, -0.8660254037844430375 ) ) ;
#5728=CARTESIAN_POINT ( 'NONE',  ( 0.4749369078591172411, -0.4881889763779528324, 0.3514880584999470203 ) ) ;
#5729=DIRECTION ( 'NONE',  ( -8.673617379884032317E-15, 0.000000000000000000, -1.000000000000000000 ) ) ;
#5732=ORIENTED_EDGE ( 'NONE', *, *, #6051, .F. ) ;
#5733=ORIENTED_EDGE ( 'NONE', *, *, #2020, .T. ) ;
#5738=FACE_OUTER_BOUND ( 'NONE', #6452, .T. ) ;
#5739=ADVANCED_FACE ( 'NONE', ( #3224 ), #5708, .T. ) ;
#5740=DIRECTION ( 'NONE',  ( 0.000000000000000000, -1.000000000000000000, 0.000000000000000000 ) ) ;
#5743=DIRECTION ( 'NONE',  ( 0.000000000000000000, 0.000000000000000000, -1.000000000000000000 ) ) ;
#5745=DIRECTION ( 'NONE',  ( 3.476578583725179813E-16, 0.000000000000000000, -1.000000000000000000 ) ) ;
#5746=DIRECTION ( 'NONE',  ( 0.8660254037844309360, 0.000000000000000000, -0.5000000000000134337 ) ) ;
#5751=ORIENTED_EDGE ( 'NONE', *, *, #8214, .F. ) ;
#5752=EDGE_CURVE ( 'NONE', #7829, #4717, #5479, .T. ) ;
#5753=VERTEX_POINT ( 'NONE', #4389 ) ;
#5754=EDGE_CURVE ( 'NONE', #11599, #9415, #5631, .T. ) ;
#5756=EDGE_CURVE ( 'NONE', #7384, #15055, #4876, .T. ) ;
#5757=DIRECTION ( 'NONE',  ( 0.5000000000000035527, 0.000000000000000000, -0.8660254037844365982 ) ) ;
#5760=CYLINDRICAL_SURFACE ( 'NONE', #3072, 0.003937007874015754916 ) ;
#5761=CARTESIAN_POINT ( 'NONE',  ( 0.5452755905511544876, -0.4921259842519685179, 0.2375319020879054499 ) ) ;
#5763=CYLINDRICAL_SURFACE ( 'NONE', #2442, 0.003937007874015724558 ) ;
#5770=EDGE_CURVE ( 'NONE', #8667, #4753, #2870, .T. ) ;
#5771=ORIENTED_EDGE ( 'NONE', *, *, #5359, .F. ) ;
#5773=EDGE_CURVE ( 'NONE', #13377, #13441, #1972, .T. ) ;
#5774=CARTESIAN_POINT ( 'NONE',  ( 0.5610236220472175628, -0.09842519685039370636, 0.2102555114175294892 ) ) ;
#5776=CARTESIAN_POINT ( 'NONE',  ( 0.05314960629921190033, -0.09842519685039370636, 0.09205781851251784720 ) ) ;
#5777=FACE_OUTER_BOUND ( 'NONE', #3233, .T. ) ;
#5779=ORIENTED_EDGE ( 'NONE', *, *, #2782, .T. ) ;
#5781=ADVANCED_FACE ( 'NONE', ( #4297 ), #9176, .T. ) ;
#5782=DIRECTION ( 'NONE',  ( 0.000000000000000000, -1.000000000000000000, 0.000000000000000000 ) ) ;
#5783=FACE_OUTER_BOUND ( 'NONE', #5953, .T. ) ;
#5784=CARTESIAN_POINT ( 'NONE',  ( 0.2359202325322792559, -0.4921259842519685179, 0.06286251073447048088 ) ) ;
#5786=DIRECTION ( 'NONE',  ( -0.000000000000000000, -1.000000000000000000, -0.000000000000000000 ) ) ;
#5787=ORIENTED_EDGE ( 'NONE', *, *, #7503, .F. ) ;
#5788=ORIENTED_EDGE ( 'NONE', *, *, #11515, .F. ) ;
#5790=EDGE_CURVE ( 'NONE', #11240, #4737, #9899, .T. ) ;
#5793=CARTESIAN_POINT ( 'NONE',  ( 0.5629921259843070347, -0.4881889763779528324, 0.2068459625837795746 ) ) ;
#5794=DIRECTION ( 'NONE',  ( 0.000000000000000000, 1.000000000000000000, 0.000000000000000000 ) ) ;
#5802=CARTESIAN_POINT ( 'NONE',  ( 0.2681506793018587631, -0.1023622047244094474, 0.03207310886168001501 ) ) ;
#5805=DIRECTION ( 'NONE',  ( 1.060575238724906792E-16, 1.000000000000000000, 6.123233995736767268E-17 ) ) ;
#5806=ORIENTED_EDGE ( 'NONE', *, *, #4098, .F. ) ;
#5810=AXIS2_PLACEMENT_3D ( 'NONE', #2317, #14314, #7190 ) ;
#5812=DIRECTION ( 'NONE',  ( -0.8660254037844398178, 0.000000000000000000, 0.4999999999999979461 ) ) ;
#5814=CIRCLE ( 'NONE', #5320, 0.003937007874015758385 ) ;
#5815=FACE_OUTER_BOUND ( 'NONE', #8005, .T. ) ;
#5816=CARTESIAN_POINT ( 'NONE',  ( 0.3294846884549027521, -0.2952755905511811330, 0.2675111804726952314 ) ) ;
#5819=DIRECTION ( 'NONE',  ( 0.000000000000000000, 0.000000000000000000, -1.000000000000000000 ) ) ;
#5820=AXIS2_PLACEMENT_3D ( 'NONE', #9066, #12451, #10976 ) ;
#5822=EDGE_LOOP ( 'NONE', ( #489, #4309, #8392, #11620 ) ) ;
#5824=EDGE_LOOP ( 'NONE', ( #7610, #9562, #12301, #6949 ) ) ;
#5827=ORIENTED_EDGE ( 'NONE', *, *, #59, .T. ) ;
#5835=VECTOR ( 'NONE', #3518, 39.37007874015748143 ) ;
#5836=CARTESIAN_POINT ( 'NONE',  ( 0.06692913385832209572, -0.2952755905511811330, -0.4584677793364516640 ) ) ;
#5839=VERTEX_POINT ( 'NONE', #4623 ) ;
#5844=ORIENTED_EDGE ( 'NONE', *, *, #14885, .T. ) ;
#5847=VECTOR ( 'NONE', #1801, 39.37007874015748143 ) ;
#5850=AXIS2_PLACEMENT_3D ( 'NONE', #14830, #1912, #3070 ) ;
#5851=FACE_OUTER_BOUND ( 'NONE', #8665, .T. ) ;
#5857=DIRECTION ( 'NONE',  ( 1.000000000000000000, 1.734723475976817507E-14, 0.000000000000000000 ) ) ;
#5861=EDGE_CURVE ( 'NONE', #3171, #14774, #7045, .T. ) ;
#5866=CYLINDRICAL_SURFACE ( 'NONE', #1361, 0.003937007874015758385 ) ;
#5868=CARTESIAN_POINT ( 'NONE',  ( -0.2393297813659120143, -0.4881889763779528324, 0.06089400679736763772 ) ) ;
#5869=DIRECTION ( 'NONE',  ( 0.000000000000000000, 0.000000000000000000, -1.000000000000000000 ) ) ;
#5872=EDGE_CURVE ( 'NONE', #6983, #7883, #9658, .T. ) ;
#5875=VECTOR ( 'NONE', #10333, 39.37007874015748143 ) ;
#5876=VERTEX_POINT ( 'NONE', #3046 ) ;
#5878=ORIENTED_EDGE ( 'NONE', *, *, #14416, .T. ) ;
#5879=DIRECTION ( 'NONE',  ( 0.5000000000000134337, 0.000000000000000000, 0.8660254037844309360 ) ) ;
#5881=AXIS2_PLACEMENT_3D ( 'NONE', #5224, #7740, #5379 ) ;
#5887=LINE ( 'NONE', #12796, #10912 ) ;
#5888=DIRECTION ( 'NONE',  ( -0.000000000000000000, -1.000000000000000000, 0.000000000000000000 ) ) ;
#5892=VECTOR ( 'NONE', #3305, 39.37007874015748143 ) ;
#5893=CARTESIAN_POINT ( 'NONE',  ( -0.2373612774289040883, -0.1023622047244094474, 0.06430355563116459117 ) ) ;
#5894=ADVANCED_FACE ( 'NONE', ( #7813 ), #9305, .T. ) ;
#5898=VERTEX_POINT ( 'NONE', #10180 ) ;
#5899=ORIENTED_EDGE ( 'NONE', *, *, #797, .F. ) ;
#5902=AXIS2_PLACEMENT_3D ( 'NONE', #8570, #6214, #14471 ) ;
#5909=DIRECTION ( 'NONE',  ( -0.4999999999999998335, 0.000000000000000000, -0.8660254037844388186 ) ) ;
#5911=DIRECTION ( 'NONE',  ( -0.8660254037844365982, 0.000000000000000000, -0.5000000000000035527 ) ) ;
#5912=CARTESIAN_POINT ( 'NONE',  ( 0.000000000000000000, -0.4881889763779528324, -0.5870514566507987197 ) ) ;
#5913=( NAMED_UNIT ( * ) SI_UNIT ( $, .STERADIAN. ) SOLID_ANGLE_UNIT ( ) );
#5921=TOROIDAL_SURFACE ( 'NONE', #206, 0.007874015748031495954, 0.003937007874015747977 ) ;
#5926=DIRECTION ( 'NONE',  ( 0.5000000000000001110, 0.000000000000000000, 0.8660254037844385966 ) ) ;
#5929=CARTESIAN_POINT ( 'NONE',  ( -0.000000000000000000, -0.09842519685039370636, -0.5870514566507987197 ) ) ;
#5930=DIRECTION ( 'NONE',  ( -0.000000000000000000, -1.000000000000000000, 0.000000000000000000 ) ) ;
#5931=AXIS2_PLACEMENT_3D ( 'NONE', #2987, #9019, #6650 ) ;
#5934=VERTEX_POINT ( 'NONE', #12760 ) ;
#5936=ORIENTED_EDGE ( 'NONE', *, *, #7029, .T. ) ;
#5937=AXIS2_PLACEMENT_3D ( 'NONE', #6426, #4237, #729 ) ;
#5938=EDGE_CURVE ( 'NONE', #3128, #6292, #11908, .T. ) ;
#5944=DIRECTION ( 'NONE',  ( 0.000000000000000000, 0.000000000000000000, -1.000000000000000000 ) ) ;
#5950=VECTOR ( 'NONE', #8773, 39.37007874015748143 ) ;
#5953=EDGE_LOOP ( 'NONE', ( #11506, #11786, #3818, #3384, #10512, #11482 ) ) ;
#5955=ORIENTED_EDGE ( 'NONE', *, *, #3366, .F. ) ;
#5956=CIRCLE ( 'NONE', #2472, 0.003937007874015758385 ) ;
#5958=DIRECTION ( 'NONE',  ( 0.4999999999999966693, 0.000000000000000000, -0.8660254037844405950 ) ) ;
#5960=AXIS2_PLACEMENT_3D ( 'NONE', #5204, #8810, #683 ) ;
#5961=ADVANCED_FACE ( 'NONE', ( #15336, #13225 ), #2412, .F. ) ;
#5962=DIRECTION ( 'NONE',  ( -0.8660254037844385966, -0.000000000000000000, -0.5000000000000001110 ) ) ;
#5963=CYLINDRICAL_SURFACE ( 'NONE', #2609, 0.003937007874015724558 ) ;
#5966=VERTEX_POINT ( 'NONE', #8222 ) ;
#5967=DIRECTION ( 'NONE',  ( -0.8660254037844383745, 0.000000000000000000, -0.5000000000000004441 ) ) ;
#5968=FACE_OUTER_BOUND ( 'NONE', #11742, .T. ) ;
#5970=CARTESIAN_POINT ( 'NONE',  ( 0.000000000000000000, 2.165354330708661568, -0.1574803149606299191 ) ) ;
#5972=ORIENTED_EDGE ( 'NONE', *, *, #13834, .F. ) ;
#5974=EDGE_CURVE ( 'NONE', #14414, #12552, #7262, .T. ) ;
#5975=ORIENTED_EDGE ( 'NONE', *, *, #13171, .T. ) ;
#5979=DIRECTION ( 'NONE',  ( -0.5000000000000001110, -0.000000000000000000, -0.8660254037844385966 ) ) ;
#5981=EDGE_CURVE ( 'NONE', #5876, #12044, #143, .T. ) ;
#5982=DIRECTION ( 'NONE',  ( -0.8660254037844398178, 0.000000000000000000, 0.4999999999999979461 ) ) ;
#5983=CARTESIAN_POINT ( 'NONE',  ( 0.1023622047244639455, -0.4921259842519685179, -0.5870514566507987197 ) ) ;
#5985=FACE_OUTER_BOUND ( 'NONE', #11904, .T. ) ;
#5987=ADVANCED_FACE ( 'NONE', ( #7103 ), #9397, .T. ) ;
#5989=DIRECTION ( 'NONE',  ( 0.000000000000000000, -1.000000000000000000, 0.000000000000000000 ) ) ;
#5990=ORIENTED_EDGE ( 'NONE', *, *, #4050, .F. ) ;
#5993=ORIENTED_EDGE ( 'NONE', *, *, #988, .F. ) ;
#5996=EDGE_CURVE ( 'NONE', #13507, #4728, #4634, .T. ) ;
#5997=DIRECTION ( 'NONE',  ( -1.000000000000000000, -0.000000000000000000, -0.000000000000000000 ) ) ;
#6006=EDGE_LOOP ( 'NONE', ( #13197, #13788, #9904, #3715 ) ) ;
#6007=VERTEX_POINT ( 'NONE', #14403 ) ;
#6008=DIRECTION ( 'NONE',  ( 0.5000000000000035527, 0.000000000000000000, -0.8660254037844365982 ) ) ;
#6011=DIRECTION ( 'NONE',  ( -0.5000000000000008882, 0.000000000000000000, 0.8660254037844380415 ) ) ;
#6012=LINE ( 'NONE', #7208, #10833 ) ;
#6013=CARTESIAN_POINT ( 'NONE',  ( -0.1574803149606299191, -0.09448818897637796532, -0.5909884645248143498 ) ) ;
#6015=ORIENTED_EDGE ( 'NONE', *, *, #12323, .F. ) ;
#6020=VERTEX_POINT ( 'NONE', #14172 ) ;
#6021=EDGE_LOOP ( 'NONE', ( #11258, #9148, #8614, #14306 ) ) ;
#6022=CARTESIAN_POINT ( 'NONE',  ( 0.1618514667033794652, -0.1023622047244094474, 0.2161887458866224576 ) ) ;
#6025=DIRECTION ( 'NONE',  ( -0.4999999999999966693, 0.000000000000000000, 0.8660254037844405950 ) ) ;
#6032=DIRECTION ( 'NONE',  ( -0.8660254037844383745, 0.000000000000000000, -0.5000000000000004441 ) ) ;
#6043=DIRECTION ( 'NONE',  ( -0.5000000000000001110, -0.000000000000000000, 0.8660254037844385966 ) ) ;
#6050=CARTESIAN_POINT ( 'NONE',  ( 0.3512416941306070739, -0.2952755905511811330, 0.3164411144501581563 ) ) ;
#6051=EDGE_CURVE ( 'NONE', #12320, #6775, #2186, .T. ) ;
#6052=CARTESIAN_POINT ( 'NONE',  ( -0.06692913385815726923, -0.2952755905511811330, -0.4624047872104674606 ) ) ;
#6053=DIRECTION ( 'NONE',  ( 0.000000000000000000, 1.000000000000000000, 0.000000000000000000 ) ) ;
#6054=ORIENTED_EDGE ( 'NONE', *, *, #7223, .T. ) ;
#6056=ORIENTED_EDGE ( 'NONE', *, *, #5394, .T. ) ;
#6059=CARTESIAN_POINT ( 'NONE',  ( 0.06692913385832208184, -0.2952755905511811330, -0.3757906139821208247 ) ) ;
#6060=LINE ( 'NONE', #3667, #1472 ) ;
#6062=CARTESIAN_POINT ( 'NONE',  ( 0.3294846884549027521, -0.2952755905511811330, 0.2675111804726952314 ) ) ;
#6063=CARTESIAN_POINT ( 'NONE',  ( -0.4606299212598433113, -0.1023622047244094474, 0.3841425019411278674 ) ) ;
#6064=AXIS2_PLACEMENT_3D ( 'NONE', #4482, #9264, #11700 ) ;
#6069=LINE ( 'NONE', #7265, #3901 ) ;
#6071=EDGE_LOOP ( 'NONE', ( #3318, #4225, #1270, #4421 ) ) ;
#6076=CIRCLE ( 'NONE', #5083, 0.003937007874015758385 ) ;
#6077=DIRECTION ( 'NONE',  ( -0.5000000000000003331, -0.000000000000000000, 0.8660254037844387076 ) ) ;
#6078=AXIS2_PLACEMENT_3D ( 'NONE', #14269, #15285, #5869 ) ;
#6080=AXIS2_PLACEMENT_3D ( 'NONE', #6334, #6423, #5016 ) ;
#6085=DIRECTION ( 'NONE',  ( -1.000000000000000000, -0.000000000000000000, -0.000000000000000000 ) ) ;
#6087=ORIENTED_EDGE ( 'NONE', *, *, #14812, .T. ) ;
#6090=DIRECTION ( 'NONE',  ( 0.000000000000000000, -1.000000000000000000, 0.000000000000000000 ) ) ;
#6092=VECTOR ( 'NONE', #9826, 39.37007874015748143 ) ;
#6097=ORIENTED_EDGE ( 'NONE', *, *, #12419, .F. ) ;
#6098=CARTESIAN_POINT ( 'NONE',  ( -0.5860051159906336515, -0.003937007874015747977, 0.1591122789105256785 ) ) ;
#6101=AXIS2_PLACEMENT_3D ( 'NONE', #15300, #15383, #12731 ) ;
#6102=AXIS2_PLACEMENT_3D ( 'NONE', #4361, #4448, #15258 ) ;
#6103=AXIS2_PLACEMENT_3D ( 'NONE', #14468, #284, #7312 ) ;
#6104=AXIS2_PLACEMENT_3D ( 'NONE', #9506, #14273, #3538 ) ;
#6105=CARTESIAN_POINT ( 'NONE',  ( 0.3294846884549027521, -0.2952755905511811330, 0.2675111804726952314 ) ) ;
#6106=DIRECTION ( 'NONE',  ( -6.505213034913010038E-15, 0.000000000000000000, -1.000000000000000000 ) ) ;
#6110=CARTESIAN_POINT ( 'NONE',  ( 0.4788739157331329266, -0.4881889763779528324, 0.3514880584999470203 ) ) ;
#6116=CIRCLE ( 'NONE', #14899, 0.04330708661417329020 ) ;
#6118=EDGE_LOOP ( 'NONE', ( #164, #13769, #8211, #1143 ) ) ;
#6119=EDGE_LOOP ( 'NONE', ( #2296, #1973, #2060 ) ) ;
#6120=ORIENTED_EDGE ( 'NONE', *, *, #7495, .T. ) ;
#6122=ORIENTED_EDGE ( 'NONE', *, *, #2782, .F. ) ;
#6127=DIRECTION ( 'NONE',  ( 0.8660254037844405950, -0.000000000000000000, -0.4999999999999967804 ) ) ;
#6131=AXIS2_PLACEMENT_3D ( 'NONE', #1177, #5930, #6 ) ;
#6133=AXIS2_PLACEMENT_3D ( 'NONE', #12862, #13970, #15140 ) ;
#6140=CARTESIAN_POINT ( 'NONE',  ( -0.03346456692910660530, -0.4921259842519685179, -0.05796233017450189845 ) ) ;
#6145=ADVANCED_FACE ( 'NONE', ( #7328 ), #9779, .F. ) ;
#6146=AXIS2_PLACEMENT_3D ( 'NONE', #9272, #4490, #9514 ) ;
#6149=CARTESIAN_POINT ( 'NONE',  ( 0.4572203724260462399, -0.09842519685039372024, 0.3821739980041199969 ) ) ;
#6150=DIRECTION ( 'NONE',  ( -0.000000000000000000, -0.000000000000000000, 1.000000000000000000 ) ) ;
#6151=DIRECTION ( 'NONE',  ( 1.060575238724906792E-16, 1.000000000000000000, 6.123233995736766036E-17 ) ) ;
#6153=DIRECTION ( 'NONE',  ( 0.8660254037844365982, -0.000000000000000000, 0.5000000000000035527 ) ) ;
#6154=VECTOR ( 'NONE', #1761, 39.37007874015748143 ) ;
#6157=CARTESIAN_POINT ( 'NONE',  ( -0.1638199706403874467, -0.4881889763779528324, 0.2127791970528254695 ) ) ;
#6159=AXIS2_PLACEMENT_3D ( 'NONE', #9324, #3377, #8157 ) ;
#6161=ORIENTED_EDGE ( 'NONE', *, *, #14605, .T. ) ;
#6165=AXIS2_PLACEMENT_3D ( 'NONE', #4305, #6572, #6429 ) ;
#6166=EDGE_CURVE ( 'NONE', #5839, #3335, #8585, .T. ) ;
#6172=CARTESIAN_POINT ( 'NONE',  ( 0.2393297813660762718, -0.4921259842519685179, 0.06089400679746260342 ) ) ;
#6174=EDGE_LOOP ( 'NONE', ( #11197, #12222, #5095, #15196 ) ) ;
#6177=VERTEX_POINT ( 'NONE', #3977 ) ;
#6179=EDGE_LOOP ( 'NONE', ( #4987, #13989, #8754, #9075 ) ) ;
#6180=CIRCLE ( 'NONE', #11975, 0.003937007874015724558 ) ;
#6181=EDGE_LOOP ( 'NONE', ( #4936, #11118, #74, #10205 ) ) ;
#6185=CARTESIAN_POINT ( 'NONE',  ( 1.928577636452524610E-17, 2.165354330708661568, 0.1574803149606299191 ) ) ;
#6189=AXIS2_PLACEMENT_3D ( 'NONE', #15050, #420, #15449 ) ;
#6190=DIRECTION ( 'NONE',  ( -0.000000000000000000, -1.734723475976817823E-14, -1.000000000000000000 ) ) ;
#6193=CARTESIAN_POINT ( 'NONE',  ( -0.000000000000000000, -0.09842519685039370636, -0.5870514566507987197 ) ) ;
#6196=EDGE_CURVE ( 'NONE', #6434, #14775, #14419, .T. ) ;
#6201=ORIENTED_EDGE ( 'NONE', *, *, #13638, .F. ) ;
#6204=FACE_OUTER_BOUND ( 'NONE', #2990, .T. ) ;
#6206=CARTESIAN_POINT ( 'NONE',  ( 0.5860051159906326523, -0.003937007874015747977, 0.1591122789105293422 ) ) ;
#6207=CARTESIAN_POINT ( 'NONE',  ( -0.4591888763630546655, -0.4881889763779528324, 0.3787644491703233141 ) ) ;
#6214=DIRECTION ( 'NONE',  ( 1.000000000000000000, 0.000000000000000000, -1.224646799147353207E-16 ) ) ;
#6217=VERTEX_POINT ( 'NONE', #7647 ) ;
#6219=DIRECTION ( 'NONE',  ( 0.8660254037844365982, -0.000000000000000000, 0.5000000000000035527 ) ) ;
#6222=FACE_OUTER_BOUND ( 'NONE', #13924, .T. ) ;
#6227=LINE ( 'NONE', #156, #2322 ) ;
#6230=ORIENTED_EDGE ( 'NONE', *, *, #15337, .T. ) ;
#6240=CARTESIAN_POINT ( 'NONE',  ( 0.05905511811029064834, -0.09448818897637796532, -0.5870514566507987197 ) ) ;
#6242=ORIENTED_EDGE ( 'NONE', *, *, #14885, .F. ) ;
#6249=ADVANCED_FACE ( 'NONE', ( #10160 ), #4343, .F. ) ;
#6250=ORIENTED_EDGE ( 'NONE', *, *, #6051, .T. ) ;
#6253=DIRECTION ( 'NONE',  ( -0.000000000000000000, 1.000000000000000000, -0.000000000000000000 ) ) ;
#6255=ORIENTED_EDGE ( 'NONE', *, *, #11709, .F. ) ;
#6256=LINE ( 'NONE', #6193, #9942 ) ;
#6263=ADVANCED_FACE ( 'NONE', ( #6769 ), #2955, .F. ) ;
#6264=ORIENTED_EDGE ( 'NONE', *, *, #2802, .F. ) ;
#6266=CARTESIAN_POINT ( 'NONE',  ( -0.1023622047242992716, -0.1023622047244094474, -0.2472069366677729363 ) ) ;
#6269=EDGE_CURVE ( 'NONE', #10807, #5518, #14912, .T. ) ;
#6271=DIRECTION ( 'NONE',  ( -8.673617379884087537E-15, -1.000000000000000000, 0.000000000000000000 ) ) ;
#6273=FACE_BOUND ( 'NONE', #9945, .T. ) ;
#6276=CARTESIAN_POINT ( 'NONE',  ( 0.06692913385832215123, -0.4881889763779528324, -0.5870514566507987197 ) ) ;
#6278=ORIENTED_EDGE ( 'NONE', *, *, #2177, .F. ) ;
#6283=LINE ( 'NONE', #1767, #12344 ) ;
#6285=CARTESIAN_POINT ( 'NONE',  ( 0.1657884745773951785, -0.4881889763779528324, 0.2093696482190284258 ) ) ;
#6287=SPHERICAL_SURFACE ( 'NONE', #2332, 0.003937007874015747977 ) ;
#6292=VERTEX_POINT ( 'NONE', #3027 ) ;
#6303=DIRECTION ( 'NONE',  ( 1.000000000000000000, 0.000000000000000000, 3.973232667114492835E-16 ) ) ;
#6304=DIRECTION ( 'NONE',  ( -0.5000000000000001110, -0.000000000000000000, -0.8660254037844385966 ) ) ;
#6305=AXIS2_PLACEMENT_3D ( 'NONE', #11194, #3328, #5746 ) ;
#6306=CARTESIAN_POINT ( 'NONE',  ( 0.4496668909809713455, -0.2952755905511811330, 0.1459636727603555173 ) ) ;
#6309=ORIENTED_EDGE ( 'NONE', *, *, #3679, .F. ) ;
#6316=AXIS2_PLACEMENT_3D ( 'NONE', #6952, #1009, #5757 ) ;
#6317=AXIS2_PLACEMENT_3D ( 'NONE', #4743, #5979, #3422 ) ;
#6321=ADVANCED_FACE ( 'NONE', ( #5515 ), #12747, .T. ) ;
#6322=EDGE_CURVE ( 'NONE', #2117, #5520, #13403, .T. ) ;
#6325=DIRECTION ( 'NONE',  ( -3.973232667114494807E-16, 0.000000000000000000, 1.000000000000000000 ) ) ;
#6326=CIRCLE ( 'NONE', #3099, 0.003937007874015741038 ) ;
#6327=CARTESIAN_POINT ( 'NONE',  ( 0.000000000000000000, -0.1023622047244094474, 0.000000000000000000 ) ) ;
#6328=VECTOR ( 'NONE', #10996, 39.37007874015748143 ) ;
#6332=AXIS2_PLACEMENT_3D ( 'NONE', #14232, #47, #7169 ) ;
#6334=CARTESIAN_POINT ( 'NONE',  ( 0.4307978335858663188, -0.003937007874015747977, 0.4279391777402732910 ) ) ;
#6335=AXIS2_PLACEMENT_3D ( 'NONE', #11756, #9482, #14319 ) ;
#6336=EDGE_CURVE ( 'NONE', #777, #8, #3404, .T. ) ;
#6340=DIRECTION ( 'NONE',  ( 0.000000000000000000, -1.000000000000000000, 0.000000000000000000 ) ) ;
#6341=ORIENTED_EDGE ( 'NONE', *, *, #7804, .F. ) ;
#6342=AXIS2_PLACEMENT_3D ( 'NONE', #243, #8694, #8762 ) ;
#6343=ORIENTED_EDGE ( 'NONE', *, *, #9992, .T. ) ;
#6346=VECTOR ( 'NONE', #9245, 39.37007874015748143 ) ;
#6350=VECTOR ( 'NONE', #172, 39.37007874015748143 ) ;
#6355=CARTESIAN_POINT ( 'NONE',  ( -0.1552072824047652788, -0.09448818897637796532, -0.5870514566507987197 ) ) ;
#6357=DIRECTION ( 'NONE',  ( 1.000000000000000000, -0.000000000000000000, 1.224646799147353207E-16 ) ) ;
#6359=DIRECTION ( 'NONE',  ( 0.000000000000000000, -1.000000000000000000, 0.000000000000000000 ) ) ;
#6361=AXIS2_PLACEMENT_3D ( 'NONE', #5802, #6826, #5729 ) ;
#6367=ORIENTED_EDGE ( 'NONE', *, *, #11214, .T. ) ;
#6368=EDGE_CURVE ( 'NONE', #12059, #9714, #9907, .T. ) ;
#6369=DIRECTION ( 'NONE',  ( -0.8660254037844398178, 0.000000000000000000, 0.4999999999999979461 ) ) ;
#6370=ORIENTED_EDGE ( 'NONE', *, *, #12982, .F. ) ;
#6372=AXIS2_PLACEMENT_3D ( 'NONE', #2319, #5926, #12051 ) ;
#6373=CIRCLE ( 'NONE', #7377, 0.003937007874015749712 ) ;
#6374=CIRCLE ( 'NONE', #3407, 0.03937007874015751446 ) ;
#6375=DIRECTION ( 'NONE',  ( -0.8660254037844385966, 0.000000000000000000, 0.5000000000000000000 ) ) ;
#6385=MECHANICAL_DESIGN_GEOMETRIC_PRESENTATION_REPRESENTATION('',(#3661),#907);
#6387=ORIENTED_EDGE ( 'NONE', *, *, #12419, .T. ) ;
#6388=EDGE_CURVE ( 'NONE', #4713, #4318, #6631, .T. ) ;
#6393=VERTEX_POINT ( 'NONE', #4088 ) ;
#6395=CARTESIAN_POINT ( 'NONE',  ( 0.1062992125984796032, -0.4881889763779528324, -0.2482618547481154347 ) ) ;
#6397=DIRECTION ( 'NONE',  ( -0.8660254037844385966, -0.000000000000000000, 0.5000000000000001110 ) ) ;
#6398=LINE ( 'NONE', #11191, #3356 ) ;
#6399=CYLINDRICAL_SURFACE ( 'NONE', #5130, 0.003937007874015724558 ) ;
#6400=CYLINDRICAL_SURFACE ( 'NONE', #588, 0.03937007874015751446 ) ;
#6402=CIRCLE ( 'NONE', #7420, 0.003937007874015721089 ) ;
#6405=CYLINDRICAL_SURFACE ( 'NONE', #5171, 0.003937007874015724558 ) ;
#6412=CIRCLE ( 'NONE', #14197, 0.003937007874015721089 ) ;
#6416=DIRECTION ( 'NONE',  ( 3.476578583725179813E-16, 0.000000000000000000, -1.000000000000000000 ) ) ;
#6417=AXIS2_PLACEMENT_3D ( 'NONE', #6240, #6085, #1416 ) ;
#6423=DIRECTION ( 'NONE',  ( -1.000000000000000000, -0.000000000000000000, 3.469446951953635015E-14 ) ) ;
#6425=CIRCLE ( 'NONE', #6673, 0.003937007874015724558 ) ;
#6426=CARTESIAN_POINT ( 'NONE',  ( -0.4307978335858689833, -0.09448818897637796532, 0.4279391777402706265 ) ) ;
#6427=DIRECTION ( 'NONE',  ( -4.425882400543264939E-32, 1.000000000000000000, 1.224646799147353207E-16 ) ) ;
#6429=DIRECTION ( 'NONE',  ( -0.8660254037844383745, 0.000000000000000000, 0.5000000000000004441 ) ) ;
#6430=ADVANCED_FACE ( 'NONE', ( #9983 ), #7385, .T. ) ;
#6434=VERTEX_POINT ( 'NONE', #2692 ) ;
#6436=DIRECTION ( 'NONE',  ( 0.000000000000000000, 0.000000000000000000, 1.000000000000000000 ) ) ;
#6442=DIRECTION ( 'NONE',  ( 0.000000000000000000, -1.000000000000000000, 0.000000000000000000 ) ) ;
#6443=CARTESIAN_POINT ( 'NONE',  ( -0.6582248459352179060, -0.2952755905511811330, -0.3018834747714004840 ) ) ;
#6445=LINE ( 'NONE', #576, #8893 ) ;
#6446=TOROIDAL_SURFACE ( 'NONE', #2461, 0.1614173228346456879, 0.003937007874015747977 ) ;
#6447=EDGE_CURVE ( 'NONE', #4124, #4812, #5324, .T. ) ;
#6448=DIRECTION ( 'NONE',  ( 0.5000000000000036637, -0.000000000000000000, 0.8660254037844364872 ) ) ;
#6449=ORIENTED_EDGE ( 'NONE', *, *, #3555, .T. ) ;
#6450=CIRCLE ( 'NONE', #2207, 0.003937007874015724558 ) ;
#6452=EDGE_LOOP ( 'NONE', ( #6161, #11458, #709 ) ) ;
#6454=ORIENTED_EDGE ( 'NONE', *, *, #15099, .F. ) ;
#6455=ADVANCED_FACE ( 'NONE', ( #6204 ), #14827, .T. ) ;
#6461=FACE_OUTER_BOUND ( 'NONE', #1030, .T. ) ;
#6463=DIRECTION ( 'NONE',  ( 0.4999999999999995004, 0.000000000000000000, 0.8660254037844390407 ) ) ;
#6467=FACE_OUTER_BOUND ( 'NONE', #11955, .T. ) ;
#6469=ORIENTED_EDGE ( 'NONE', *, *, #2996, .F. ) ;
#6471=ORIENTED_EDGE ( 'NONE', *, *, #8307, .F. ) ;
#6477=CARTESIAN_POINT ( 'NONE',  ( 0.2393297813660762996, -0.4881889763779528324, 0.06089400679746265199 ) ) ;
#6483=CARTESIAN_POINT ( 'NONE',  ( 0.1062992125984796865, -0.09842519685039370636, -0.5870514566507987197 ) ) ;
#6484=DIRECTION ( 'NONE',  ( 0.000000000000000000, 0.000000000000000000, -1.000000000000000000 ) ) ;
#6486=EDGE_LOOP ( 'NONE', ( #1054, #2961 ) ) ;
#6487=LINE ( 'NONE', #8770, #1440 ) ;
#6491=ORIENTED_EDGE ( 'NONE', *, *, #14094, .F. ) ;
#6492=DIRECTION ( 'NONE',  ( 1.000000000000000000, -1.734723475976817507E-14, 0.000000000000000000 ) ) ;
#6493=CARTESIAN_POINT ( 'NONE',  ( 0.2681506793018588741, -0.1023622047244094474, 0.03207310886168006359 ) ) ;
#6494=DIRECTION ( 'NONE',  ( 0.5000000000000035527, 0.000000000000000000, -0.8660254037844365982 ) ) ;
#6495=CARTESIAN_POINT ( 'NONE',  ( -0.5860051159906336515, -0.09448818897637796532, 0.1591122789105256508 ) ) ;
#6496=EDGE_LOOP ( 'NONE', ( #14552, #9244, #5733, #5177 ) ) ;
#6497=DIRECTION ( 'NONE',  ( -0.5000000000000004441, 0.000000000000000000, -0.8660254037844383745 ) ) ;
#6505=DIRECTION ( 'NONE',  ( -3.469446951953612927E-14, 0.000000000000000000, -1.000000000000000000 ) ) ;
#6506=FACE_OUTER_BOUND ( 'NONE', #7578, .T. ) ;
#6509=EDGE_CURVE ( 'NONE', #2574, #7829, #6909, .T. ) ;
#6511=DIRECTION ( 'NONE',  ( 0.8660254037844383745, 0.000000000000000000, -0.5000000000000004441 ) ) ;
#6513=CARTESIAN_POINT ( 'NONE',  ( -0.2642136714276788201, -0.4921259842519685179, 0.03889220652917903254 ) ) ;
#6514=ADVANCED_FACE ( 'NONE', ( #15059 ), #8915, .T. ) ;
#6515=LINE ( 'NONE', #4026, #9424 ) ;
#6516=ORIENTED_EDGE ( 'NONE', *, *, #13927, .F. ) ;
#6517=ORIENTED_EDGE ( 'NONE', *, *, #13276, .F. ) ;
#6520=EDGE_CURVE ( 'NONE', #10948, #14791, #14925, .T. ) ;
#6524=ADVANCED_FACE ( 'NONE', ( #3236, #5646 ), #12638, .F. ) ;
#6527=CARTESIAN_POINT ( 'NONE',  ( 0.000000000000000000, -0.4881889763779528324, -0.5870514566507987197 ) ) ;
#6531=CARTESIAN_POINT ( 'NONE',  ( -0.5595825771504281398, -0.4921259842519685179, 0.2048774586467239367 ) ) ;
#6532=CARTESIAN_POINT ( 'NONE',  ( -0.1629063847838169987, -0.4921259842519685179, 0.2122517380126066888 ) ) ;
#6535=ORIENTED_EDGE ( 'NONE', *, *, #14776, .F. ) ;
#6536=EDGE_LOOP ( 'NONE', ( #10760, #15280, #7585, #6242 ) ) ;
#6537=ORIENTED_EDGE ( 'NONE', *, *, #9047, .T. ) ;
#6539=FACE_OUTER_BOUND ( 'NONE', #4210, .T. ) ;
#6540=DIRECTION ( 'NONE',  ( 0.000000000000000000, 0.000000000000000000, 1.000000000000000000 ) ) ;
#6545=CARTESIAN_POINT ( 'NONE',  ( -0.5860051159906336515, -0.09448818897637796532, 0.1591122789105256785 ) ) ;
#6549=CARTESIAN_POINT ( 'NONE',  ( -0.2613315816341005848, -0.4881889763779528324, 0.03601011673560078341 ) ) ;
#6552=ORIENTED_EDGE ( 'NONE', *, *, #1543, .F. ) ;
#6555=CIRCLE ( 'NONE', #8069, 0.007874015748031501158 ) ;
#6556=VECTOR ( 'NONE', #5448, 39.37007874015748143 ) ;
#6557=AXIS2_PLACEMENT_3D ( 'NONE', #12602, #11428, #705 ) ;
#6558=LINE ( 'NONE', #11354, #14120 ) ;
#6559=DIRECTION ( 'NONE',  ( 0.8660254037844254960, -0.000000000000000000, 0.5000000000000228706 ) ) ;
#6560=LINE ( 'NONE', #11356, #202 ) ;
#6561=DIRECTION ( 'NONE',  ( 0.4999999999999996114, 0.000000000000000000, 0.8660254037844389297 ) ) ;
#6563=EDGE_CURVE ( 'NONE', #5839, #13855, #7403, .T. ) ;
#6568=CIRCLE ( 'NONE', #13587, 0.003937007874015750579 ) ;
#6571=VECTOR ( 'NONE', #15450, 39.37007874015748143 ) ;
#6572=DIRECTION ( 'NONE',  ( -0.4999999999999979461, 0.000000000000000000, -0.8660254037844398178 ) ) ;
#6574=ORIENTED_EDGE ( 'NONE', *, *, #7051, .F. ) ;
#6576=VERTEX_POINT ( 'NONE', #659 ) ;
#6579=AXIS2_PLACEMENT_3D ( 'NONE', #3495, #2384, #7166 ) ;
#6586=CARTESIAN_POINT ( 'NONE',  ( 0.5433070866142283295, -0.4881889763779528324, 0.2409414509217496780 ) ) ;
#6589=CARTESIAN_POINT ( 'NONE',  ( 0.1638199706403873079, -0.1023622047244094474, 0.2127791970528254417 ) ) ;
#6592=CIRCLE ( 'NONE', #2603, 0.003937007874015721089 ) ;
#6593=VERTEX_POINT ( 'NONE', #10441 ) ;
#6594=EDGE_CURVE ( 'NONE', #9393, #9540, #11582, .T. ) ;
#6596=ORIENTED_EDGE ( 'NONE', *, *, #12228, .F. ) ;
#6597=CIRCLE ( 'NONE', #9880, 0.003937007874015737569 ) ;
#6599=ORIENTED_EDGE ( 'NONE', *, *, #10460, .T. ) ;
#6601=ADVANCED_FACE ( 'NONE', ( #1814 ), #2215, .T. ) ;
#6603=FACE_OUTER_BOUND ( 'NONE', #6836, .T. ) ;
#6604=AXIS2_PLACEMENT_3D ( 'NONE', #11297, #11386, #10137 ) ;
#6606=CYLINDRICAL_SURFACE ( 'NONE', #12464, 0.003937007874015759253 ) ;
#6609=CARTESIAN_POINT ( 'NONE',  ( -0.03346456692913318126, -0.4921259842519685179, 0.05796233017454786168 ) ) ;
#6610=AXIS2_PLACEMENT_3D ( 'NONE', #4155, #2908, #7684 ) ;
#6615=ORIENTED_EDGE ( 'NONE', *, *, #1426, .F. ) ;
#6621=ORIENTED_EDGE ( 'NONE', *, *, #614, .T. ) ;
#6626=CARTESIAN_POINT ( 'NONE',  ( -0.4319503555479016765, -0.2952755905511811330, 0.1766496122645288547 ) ) ;
#6629=DIRECTION ( 'NONE',  ( -0.000000000000000000, 1.000000000000000000, 0.000000000000000000 ) ) ;
#6630=FACE_OUTER_BOUND ( 'NONE', #12486, .T. ) ;
#6631=CIRCLE ( 'NONE', #9156, 0.003937007874015758385 ) ;
#6633=CIRCLE ( 'NONE', #3418, 0.1535433070866141780 ) ;
#6636=ORIENTED_EDGE ( 'NONE', *, *, #2648, .F. ) ;
#6638=CARTESIAN_POINT ( 'NONE',  ( 0.5576140732134206024, -0.4881889763779528324, 0.2082870074805215910 ) ) ;
#6641=EDGE_LOOP ( 'NONE', ( #13801, #987, #1160, #1941 ) ) ;
#6642=ADVANCED_FACE ( 'NONE', ( #13251 ), #4639, .T. ) ;
#6643=ORIENTED_EDGE ( 'NONE', *, *, #5290, .F. ) ;
#6647=AXIS2_PLACEMENT_3D ( 'NONE', #4790, #5015, #7370 ) ;
#6649=CARTESIAN_POINT ( 'NONE',  ( -0.1724006475077544953, -0.4921259842519685179, 0.1768186671464649640 ) ) ;
#6650=DIRECTION ( 'NONE',  ( -0.4999999999999975575, 0.000000000000000000, 0.8660254037844399289 ) ) ;
#6652=DIRECTION ( 'NONE',  ( 0.5000000000000004441, 1.502314598737158676E-14, -0.8660254037844383745 ) ) ;
#6653=EDGE_LOOP ( 'NONE', ( #110, #10461, #8686 ) ) ;
#6654=DIRECTION ( 'NONE',  ( 0.8660254037844387076, 0.000000000000000000, -0.4999999999999999445 ) ) ;
#6655=EDGE_CURVE ( 'NONE', #9377, #10277, #1338, .T. ) ;
#6656=CARTESIAN_POINT ( 'NONE',  ( 0.5894146648244296127, -0.09842519685039370636, 0.1610807828475372405 ) ) ;
#6659=CARTESIAN_POINT ( 'NONE',  ( -0.1574803149606299191, -0.09448818897637796532, -0.5870514566507987197 ) ) ;
#6660=VERTEX_POINT ( 'NONE', #14438 ) ;
#6661=CIRCLE ( 'NONE', #6159, 0.003937007874015721089 ) ;
#6663=AXIS2_PLACEMENT_3D ( 'NONE', #887, #1914, #12793 ) ;
#6665=ORIENTED_EDGE ( 'NONE', *, *, #11434, .F. ) ;
#6666=DIRECTION ( 'NONE',  ( 0.000000000000000000, 0.000000000000000000, 1.000000000000000000 ) ) ;
#6668=VECTOR ( 'NONE', #8511, 39.37007874015748143 ) ;
#6669=CARTESIAN_POINT ( 'NONE',  ( -0.000000000000000000, -0.09842519685039370636, -0.5870514566507987197 ) ) ;
#6672=CARTESIAN_POINT ( 'NONE',  ( -0.2681506793016945611, -0.1023622047244094474, 0.03207310886158502850 ) ) ;
#6673=AXIS2_PLACEMENT_3D ( 'NONE', #9394, #3209, #3446 ) ;
#6676=FACE_OUTER_BOUND ( 'NONE', #13656, .T. ) ;
#6677=EDGE_CURVE ( 'NONE', #2728, #2681, #8583, .T. ) ;
#6685=VERTEX_POINT ( 'NONE', #2512 ) ;
#6691=AXIS2_PLACEMENT_3D ( 'NONE', #3427, #102, #9138 ) ;
#6696=VECTOR ( 'NONE', #11525, 39.37007874015748143 ) ;
#6701=EDGE_CURVE ( 'NONE', #13962, #7115, #10677, .T. ) ;
#6702=ORIENTED_EDGE ( 'NONE', *, *, #2467, .F. ) ;
#6706=AXIS2_PLACEMENT_3D ( 'NONE', #4976, #11078, #12207 ) ;
#6707=CARTESIAN_POINT ( 'NONE',  ( 0.05905511811029055813, -0.09842519685039370636, 8.537024980208681893E-18 ) ) ;
#6708=DIRECTION ( 'NONE',  ( -0.000000000000000000, 1.000000000000000000, -0.000000000000000000 ) ) ;
#6710=DIRECTION ( 'NONE',  ( 0.000000000000000000, 1.000000000000000000, 0.000000000000000000 ) ) ;
#6712=PLANE ( 'NONE',  #386 ) ;
#6715=EDGE_CURVE ( 'NONE', #4524, #12161, #4330, .T. ) ;
#6716=ORIENTED_EDGE ( 'NONE', *, *, #13995, .T. ) ;
#6718=CARTESIAN_POINT ( 'NONE',  ( -0.09842519685028353060, -0.4921259842519685179, -0.2482618547482104143 ) ) ;
#6719=DIRECTION ( 'NONE',  ( -1.000000000000000000, 0.000000000000000000, 0.000000000000000000 ) ) ;
#6720=EDGE_LOOP ( 'NONE', ( #10294, #5732, #13543, #5552 ) ) ;
#6723=PRODUCT_DEFINITION_CONTEXT ( 'detailed design', #11291, 'design' ) ;
#6724=ORIENTED_EDGE ( 'NONE', *, *, #13680, .T. ) ;
#6725=CARTESIAN_POINT ( 'NONE',  ( 0.1023622047244638067, -0.4921259842519685179, -0.2482618547481154347 ) ) ;
#6727=FACE_OUTER_BOUND ( 'NONE', #12586, .T. ) ;
#6730=CARTESIAN_POINT ( 'NONE',  ( -0.3589087851413753083, -0.2952755905511811330, 0.1299329768165586318 ) ) ;
#6731=CARTESIAN_POINT ( 'NONE',  ( 0.1629063847838169432, -0.4881889763779528324, 0.2122517380126066888 ) ) ;
#6735=DIRECTION ( 'NONE',  ( 0.000000000000000000, -1.000000000000000000, 0.000000000000000000 ) ) ;
#6740=CARTESIAN_POINT ( 'NONE',  ( 0.000000000000000000, 2.161417322834645827, 0.000000000000000000 ) ) ;
#6744=VERTEX_POINT ( 'NONE', #9336 ) ;
#6746=DIRECTION ( 'NONE',  ( 0.000000000000000000, 0.000000000000000000, -1.000000000000000000 ) ) ;
#6748=DIRECTION ( 'NONE',  ( -0.8660254037844347108, 0.000000000000000000, -0.5000000000000069944 ) ) ;
#6750=FACE_BOUND ( 'NONE', #273, .T. ) ;
#6751=LINE ( 'NONE', #14048, #9886 ) ;
#6752=ORIENTED_EDGE ( 'NONE', *, *, #9270, .F. ) ;
#6755=CARTESIAN_POINT ( 'NONE',  ( -0.1552072824047652788, -0.003937007874015747977, -0.5909884645248143498 ) ) ;
#6756=ADVANCED_FACE ( 'NONE', ( #14114 ), #3393, .T. ) ;
#6759=ORIENTED_EDGE ( 'NONE', *, *, #10390, .T. ) ;
#6760=EDGE_CURVE ( 'NONE', #5345, #1627, #7359, .T. ) ;
#6761=VERTEX_POINT ( 'NONE', #2581 ) ;
#6764=DIRECTION ( 'NONE',  ( 0.4999999999999971134, 0.000000000000000000, 0.8660254037844402619 ) ) ;
#6765=DIRECTION ( 'NONE',  ( 0.000000000000000000, -1.000000000000000000, 0.000000000000000000 ) ) ;
#6767=DIRECTION ( 'NONE',  ( 0.8660254037844385966, -0.000000000000000000, 0.5000000000000001110 ) ) ;
#6768=DIRECTION ( 'NONE',  ( 0.5000000000000004441, 0.000000000000000000, -0.8660254037844383745 ) ) ;
#6769=FACE_OUTER_BOUND ( 'NONE', #5238, .T. ) ;
#6773=ORIENTED_EDGE ( 'NONE', *, *, #1933, .F. ) ;
#6774=VERTEX_POINT ( 'NONE', #13702 ) ;
#6775=VERTEX_POINT ( 'NONE', #188 ) ;
#6779=CARTESIAN_POINT ( 'NONE',  ( 0.000000000000000000, -0.09842519685039370636, 0.000000000000000000 ) ) ;
#6782=FACE_OUTER_BOUND ( 'NONE', #484, .T. ) ;
#6785=CARTESIAN_POINT ( 'NONE',  ( -0.09842519685028353060, -0.4881889763779528324, -0.2482618547482104143 ) ) ;
#6787=CARTESIAN_POINT ( 'NONE',  ( -0.5860051159906336515, -0.09448818897637796532, 0.1591122789105256785 ) ) ;
#6791=ADVANCED_FACE ( 'NONE', ( #15028 ), #4133, .F. ) ;
#6798=DIRECTION ( 'NONE',  ( 0.000000000000000000, -1.000000000000000000, 0.000000000000000000 ) ) ;
#6799=DIRECTION ( 'NONE',  ( -0.8660254037844385966, 0.000000000000000000, 0.5000000000000000000 ) ) ;
#6804=CARTESIAN_POINT ( 'NONE',  ( -0.1062992125983148878, -0.09448818897637796532, -0.5870514566507987197 ) ) ;
#6805=DIRECTION ( 'NONE',  ( 0.000000000000000000, 0.000000000000000000, 1.000000000000000000 ) ) ;
#6808=EDGE_LOOP ( 'NONE', ( #6724, #2, #13442, #2589 ) ) ;
#6810=ADVANCED_FACE ( 'NONE', ( #6539 ), #7564, .T. ) ;
#6812=DIRECTION ( 'NONE',  ( -0.4999999999999983347, -1.560416818047080642E-14, -0.8660254037844395958 ) ) ;
#6817=ADVANCED_FACE ( 'NONE', ( #14960 ), #13607, .T. ) ;
#6820=CIRCLE ( 'NONE', #2066, 0.003937007874015749712 ) ;
#6821=DIRECTION ( 'NONE',  ( -0.5000000000000001110, 0.000000000000000000, 0.8660254037844385966 ) ) ;
#6825=VECTOR ( 'NONE', #2659, 39.37007874015748143 ) ;
#6826=DIRECTION ( 'NONE',  ( -0.000000000000000000, 1.000000000000000000, -0.000000000000000000 ) ) ;
#6828=LINE ( 'NONE', #12877, #8179 ) ;
#6834=AXIS2_PLACEMENT_3D ( 'NONE', #2385, #10465, #9366 ) ;
#6835=EDGE_CURVE ( 'NONE', #5898, #6393, #7805, .T. ) ;
#6836=EDGE_LOOP ( 'NONE', ( #4227, #6264, #6945, #7110 ) ) ;
#6838=ORIENTED_EDGE ( 'NONE', *, *, #145, .F. ) ;
#6839=VECTOR ( 'NONE', #5088, 39.37007874015748143 ) ;
#6844=ADVANCED_FACE ( 'NONE', ( #7661 ), #5286, .F. ) ;
#6845=DIRECTION ( 'NONE',  ( 0.000000000000000000, 1.000000000000000000, 0.000000000000000000 ) ) ;
#6852=PLANE ( 'NONE',  #2902 ) ;
#6853=TOROIDAL_SURFACE ( 'NONE', #3614, 0.04330708661417328326, 0.003937007874015747977 ) ;
#6861=AXIS2_PLACEMENT_3D ( 'NONE', #11066, #12195, #11003 ) ;
#6862=AXIS2_PLACEMENT_3D ( 'NONE', #9554, #6077, #7269 ) ;
#6863=CARTESIAN_POINT ( 'NONE',  ( 0.5649606299212333038, -0.1023622047244094474, 0.2034364137499354852 ) ) ;
#6868=CARTESIAN_POINT ( 'NONE',  ( -0.5413385826771385245, -0.09448818897637796532, 0.2443509997554989266 ) ) ;
#6869=CARTESIAN_POINT ( 'NONE',  ( 0.3964138223131414840, -0.2952755905511811330, 0.1515865201236449578 ) ) ;
#6874=DIRECTION ( 'NONE',  ( -0.4999999999999981681, 0.000000000000000000, -0.8660254037844397068 ) ) ;
#6875=EDGE_CURVE ( 'NONE', #15288, #11324, #14088, .T. ) ;
#6876=DIRECTION ( 'NONE',  ( 1.000000000000000000, 0.000000000000000000, -0.000000000000000000 ) ) ;
#6878=VECTOR ( 'NONE', #10755, 39.37007874015748143 ) ;
#6880=ORIENTED_EDGE ( 'NONE', *, *, #1468, .T. ) ;
#6881=VERTEX_POINT ( 'NONE', #15422 ) ;
#6882=AXIS2_PLACEMENT_3D ( 'NONE', #11336, #7810, #10176 ) ;
#6887=AXIS2_PLACEMENT_3D ( 'NONE', #11467, #1910, #4246 ) ;
#6890=DIRECTION ( 'NONE',  ( 0.000000000000000000, -1.000000000000000000, 0.000000000000000000 ) ) ;
#6891=DIRECTION ( 'NONE',  ( 0.8660254037844398178, -0.000000000000000000, -0.4999999999999979461 ) ) ;
#6892=CIRCLE ( 'NONE', #11657, 0.03937007874015751446 ) ;
#6895=DIRECTION ( 'NONE',  ( -4.336808689942014285E-16, 0.000000000000000000, 1.000000000000000000 ) ) ;
#6896=DIRECTION ( 'NONE',  ( 0.000000000000000000, 0.000000000000000000, -1.000000000000000000 ) ) ;
#6898=CARTESIAN_POINT ( 'NONE',  ( 0.4769054117961250561, -0.4921259842519685179, 0.3480785096661500599 ) ) ;
#6899=VERTEX_POINT ( 'NONE', #2250 ) ;
#6900=DIRECTION ( 'NONE',  ( -0.4999999999999981681, 0.000000000000000000, -0.8660254037844397068 ) ) ;
#6903=CIRCLE ( 'NONE', #12880, 0.003937007874015758385 ) ;
#6905=ADVANCED_FACE ( 'NONE', ( #12911 ), #11330, .F. ) ;
#6908=ORIENTED_EDGE ( 'NONE', *, *, #9584, .T. ) ;
#6909=LINE ( 'NONE', #10280, #4901 ) ;
#6910=DIRECTION ( 'NONE',  ( 0.000000000000000000, -1.000000000000000000, 0.000000000000000000 ) ) ;
#6911=CARTESIAN_POINT ( 'NONE',  ( 0.5629921259843070347, -0.4921259842519685179, 0.2068459625837795746 ) ) ;
#6912=FACE_OUTER_BOUND ( 'NONE', #8640, .T. ) ;
#6914=VECTOR ( 'NONE', #8736, 39.37007874015748854 ) ;
#6916=ORIENTED_EDGE ( 'NONE', *, *, #14337, .T. ) ;
#6918=CARTESIAN_POINT ( 'NONE',  ( 0.09842519685044820443, -0.4881889763779528324, -0.5909884645248143498 ) ) ;
#6919=AXIS2_PLACEMENT_3D ( 'NONE', #8956, #1665, #14985 ) ;
#6920=LINE ( 'NONE', #9516, #4701 ) ;
#6921=EDGE_CURVE ( 'NONE', #11634, #13283, #11082, .T. ) ;
#6923=ORIENTED_EDGE ( 'NONE', *, *, #8733, .F. ) ;
#6924=ORIENTED_EDGE ( 'NONE', *, *, #11278, .F. ) ;
#6926=DIRECTION ( 'NONE',  ( 0.000000000000000000, 1.000000000000000000, 0.000000000000000000 ) ) ;
#6927=ORIENTED_EDGE ( 'NONE', *, *, #308, .T. ) ;
#6931=AXIS2_PLACEMENT_3D ( 'NONE', #11670, #10490, #15339 ) ;
#6934=AXIS2_PLACEMENT_3D ( 'NONE', #4007, #12309, #2585 ) ;
#6935=DIRECTION ( 'NONE',  ( 0.8660254037844368202, 0.000000000000000000, -0.5000000000000032196 ) ) ;
#6938=CARTESIAN_POINT ( 'NONE',  ( 0.1552072824047652233, -0.09842519685039370636, -0.5870514566507987197 ) ) ;
#6941=TOROIDAL_SURFACE ( 'NONE', #11702, 0.1535433070866141780, 0.003937007874015747977 ) ;
#6943=DIRECTION ( 'NONE',  ( -0.4999999999999979461, -0.000000000000000000, -0.8660254037844398178 ) ) ;
#6945=ORIENTED_EDGE ( 'NONE', *, *, #10743, .T. ) ;
#6946=EDGE_CURVE ( 'NONE', #13356, #6947, #5071, .T. ) ;
#6947=VERTEX_POINT ( 'NONE', #8279 ) ;
#6949=ORIENTED_EDGE ( 'NONE', *, *, #14681, .F. ) ;
#6950=VECTOR ( 'NONE', #2452, 39.37007874015748143 ) ;
#6951=ADVANCED_FACE ( 'NONE', ( #5605 ), #13094, .T. ) ;
#6952=CARTESIAN_POINT ( 'NONE',  ( 0.5379290338433416752, -0.1023622047244094474, 0.2423824958184916112 ) ) ;
#6954=CARTESIAN_POINT ( 'NONE',  ( -0.5576140732134202693, -0.4881889763779528324, 0.2082870074805209248 ) ) ;
#6957=DIRECTION ( 'NONE',  ( -1.000000000000000000, 0.000000000000000000, -0.000000000000000000 ) ) ;
#6958=CARTESIAN_POINT ( 'NONE',  ( 0.3117681530218320840, -0.2952755905511811330, 0.2981971199768684855 ) ) ;
#6963=CARTESIAN_POINT ( 'NONE',  ( 0.000000000000000000, -0.4881889763779528324, 0.000000000000000000 ) ) ;
#6964=CIRCLE ( 'NONE', #5698, 0.003937007874015758385 ) ;
#6968=CIRCLE ( 'NONE', #13727, 0.003937007874015758385 ) ;
#6969=ORIENTED_EDGE ( 'NONE', *, *, #2241, .F. ) ;
#6971=CARTESIAN_POINT ( 'NONE',  ( -0.1734555655881918346, -0.1023622047244094474, 0.1689446513984334541 ) ) ;
#6972=EDGE_CURVE ( 'NONE', #14775, #6434, #7581, .T. ) ;
#6973=CARTESIAN_POINT ( 'NONE',  ( 0.2681506793018588186, -0.4921259842519685179, 0.03207310886168001501 ) ) ;
#6981=FACE_OUTER_BOUND ( 'NONE', #7441, .T. ) ;
#6983=VERTEX_POINT ( 'NONE', #10310 ) ;
#6984=FACE_OUTER_BOUND ( 'NONE', #12159, .T. ) ;
#6985=VERTEX_POINT ( 'NONE', #15092 ) ;
#6990=DIRECTION ( 'NONE',  ( 0.000000000000000000, -1.734723475976802677E-14, 1.000000000000000000 ) ) ;
#6991=CARTESIAN_POINT ( 'NONE',  ( 0.09842519685044806566, -0.4921259842519685179, -0.2482618547481154347 ) ) ;
#6994=DIRECTION ( 'NONE',  ( 0.000000000000000000, 0.000000000000000000, 1.000000000000000000 ) ) ;
#6995=CARTESIAN_POINT ( 'NONE',  ( 0.05905511811029064834, -0.09842519685039370636, -0.5870514566507987197 ) ) ;
#6997=SPHERICAL_SURFACE ( 'NONE', #11937, 0.003937007874015747977 ) ;
#6998=DIRECTION ( 'NONE',  ( 0.5000000000000003331, 0.000000000000000000, -0.8660254037844387076 ) ) ;
#6999=DIRECTION ( 'NONE',  ( 0.000000000000000000, 1.000000000000000000, 0.000000000000000000 ) ) ;
#7000=EDGE_LOOP ( 'NONE', ( #11255, #4988, #762, #943 ) ) ;
#7005=ORIENTED_EDGE ( 'NONE', *, *, #11420, .T. ) ;
#7006=EDGE_CURVE ( 'NONE', #4717, #10145, #14476, .T. ) ;
#7009=EDGE_CURVE ( 'NONE', #7744, #4401, #6326, .T. ) ;
#7010=LINE ( 'NONE', #2067, #2345 ) ;
#7012=DIRECTION ( 'NONE',  ( -0.4999999999999971134, 0.000000000000000000, -0.8660254037844402619 ) ) ;
#7013=CARTESIAN_POINT ( 'NONE',  ( 0.5610236220472175628, -0.1023622047244094474, 0.2102555114175294892 ) ) ;
#7018=( NAMED_UNIT ( * ) PLANE_ANGLE_UNIT ( ) SI_UNIT ( $, .RADIAN. ) );
#7020=ORIENTED_EDGE ( 'NONE', *, *, #9712, .T. ) ;
#7021=EDGE_LOOP ( 'NONE', ( #6621, #1794, #14270, #3319 ) ) ;
#7024=EDGE_CURVE ( 'NONE', #6020, #13296, #1342, .T. ) ;
#7029=EDGE_CURVE ( 'NONE', #6744, #3640, #11896, .T. ) ;
#7030=DIRECTION ( 'NONE',  ( -0.8660254037844383745, 0.000000000000000000, -0.5000000000000003331 ) ) ;
#7032=ORIENTED_EDGE ( 'NONE', *, *, #277, .T. ) ;
#7034=LINE ( 'NONE', #8138, #14409 ) ;
#7036=ORIENTED_EDGE ( 'NONE', *, *, #2702, .F. ) ;
#7037=ORIENTED_EDGE ( 'NONE', *, *, #8348, .F. ) ;
#7038=ORIENTED_EDGE ( 'NONE', *, *, #9316, .T. ) ;
#7041=DIRECTION ( 'NONE',  ( 0.4999999999999979461, 0.000000000000000000, 0.8660254037844398178 ) ) ;
#7043=CYLINDRICAL_SURFACE ( 'NONE', #1235, 0.003937007874015758385 ) ;
#7044=LINE ( 'NONE', #11831, #4719 ) ;
#7045=LINE ( 'NONE', #12003, #15405 ) ;
#7048=CARTESIAN_POINT ( 'NONE',  ( 0.000000000000000000, -0.09842519685039370636, 0.000000000000000000 ) ) ;
#7049=SPHERICAL_SURFACE ( 'NONE', #4092, 0.003937007874015747977 ) ;
#7050=ORIENTED_EDGE ( 'NONE', *, *, #878, .T. ) ;
#7051=EDGE_CURVE ( 'NONE', #7115, #9504, #3842, .T. ) ;
#7053=ORIENTED_EDGE ( 'NONE', *, *, #49, .T. ) ;
#7058=CARTESIAN_POINT ( 'NONE',  ( 0.05314960629918537988, -0.09842519685039370636, -0.09205781851247189784 ) ) ;
#7061=CARTESIAN_POINT ( 'NONE',  ( -0.6923203342731879539, -0.2952755905511811330, -0.2821984354013215568 ) ) ;
#7064=CARTESIAN_POINT ( 'NONE',  ( 0.4121618538092042261, -0.2952755905511811330, 0.1243101294532688583 ) ) ;
#7065=CARTESIAN_POINT ( 'NONE',  ( -0.1023622047242992161, -0.2952755905511811330, -0.4190977005962941981 ) ) ;
#7068=DIRECTION ( 'NONE',  ( -0.8660254037844427044, 0.000000000000000000, -0.4999999999999929501 ) ) ;
#7069=ORIENTED_EDGE ( 'NONE', *, *, #13638, .T. ) ;
#7070=DIRECTION ( 'NONE',  ( -0.000000000000000000, -1.000000000000000000, -0.000000000000000000 ) ) ;
#7076=CIRCLE ( 'NONE', #11321, 0.003937007874015741038 ) ;
#7079=CIRCLE ( 'NONE', #336, 0.03937007874015752140 ) ;
#7081=DIRECTION ( 'NONE',  ( 0.8660254037844388186, 0.000000000000000000, -0.4999999999999996669 ) ) ;
#7084=DIRECTION ( 'NONE',  ( 0.000000000000000000, 0.000000000000000000, -1.000000000000000000 ) ) ;
#7090=EDGE_LOOP ( 'NONE', ( #8342, #5555, #10815 ) ) ;
#7091=CIRCLE ( 'NONE', #5074, 0.04330708661417331101 ) ;
#7092=ORIENTED_EDGE ( 'NONE', *, *, #13418, .T. ) ;
#7093=ORIENTED_EDGE ( 'NONE', *, *, #14318, .T. ) ;
#7094=EDGE_CURVE ( 'NONE', #8301, #12057, #8599, .T. ) ;
#7096=AXIS2_PLACEMENT_3D ( 'NONE', #12991, #11813, #14005 ) ;
#7100=AXIS2_PLACEMENT_3D ( 'NONE', #6638, #13623, #848 ) ;
#7102=CIRCLE ( 'NONE', #9376, 0.03937007874015751446 ) ;
#7103=FACE_OUTER_BOUND ( 'NONE', #7454, .T. ) ;
#7104=ORIENTED_EDGE ( 'NONE', *, *, #13311, .F. ) ;
#7108=EDGE_CURVE ( 'NONE', #4737, #9204, #4592, .T. ) ;
#7110=ORIENTED_EDGE ( 'NONE', *, *, #10583, .F. ) ;
#7111=CIRCLE ( 'NONE', #6342, 0.003937007874015758385 ) ;
#7112=TOROIDAL_SURFACE ( 'NONE', #7860, 0.04330708661417328326, 0.003937007874015747977 ) ;
#7113=AXIS2_PLACEMENT_3D ( 'NONE', #860, #952, #3220 ) ;
#7115=VERTEX_POINT ( 'NONE', #8669 ) ;
#7118=FACE_OUTER_BOUND ( 'NONE', #12739, .T. ) ;
#7120=DIRECTION ( 'NONE',  ( 0.000000000000000000, 1.000000000000000000, 0.000000000000000000 ) ) ;
#7122=AXIS2_PLACEMENT_3D ( 'NONE', #509, #13567, #437 ) ;
#7127=ORIENTED_EDGE ( 'NONE', *, *, #7425, .F. ) ;
#7133=DIRECTION ( 'NONE',  ( 0.000000000000000000, 0.000000000000000000, -1.000000000000000000 ) ) ;
#7136=ORIENTED_EDGE ( 'NONE', *, *, #4674, .F. ) ;
#7138=VERTEX_POINT ( 'NONE', #4262 ) ;
#7141=AXIS2_PLACEMENT_3D ( 'NONE', #1255, #3752, #8294 ) ;
#7145=CARTESIAN_POINT ( 'NONE',  ( -0.06692913385815735250, -0.1023622047244094474, -0.5909884645248143498 ) ) ;
#7149=CARTESIAN_POINT ( 'NONE',  ( -0.2939481552201428372, -0.2952755905511811330, 0.2424480883318111957 ) ) ;
#7150=ORIENTED_EDGE ( 'NONE', *, *, #6835, .F. ) ;
#7152=CYLINDRICAL_SURFACE ( 'NONE', #13653, 0.003937007874015749712 ) ;
#7155=CARTESIAN_POINT ( 'NONE',  ( 0.09842519685044817668, -0.2952755905511811330, -0.4584677793364516640 ) ) ;
#7157=AXIS2_PLACEMENT_3D ( 'NONE', #9596, #215, #8732 ) ;
#7164=DIRECTION ( 'NONE',  ( 1.000000000000000000, 0.000000000000000000, 0.000000000000000000 ) ) ;
#7166=DIRECTION ( 'NONE',  ( 0.8660254037844399289, 0.000000000000000000, 0.4999999999999975575 ) ) ;
#7167=CARTESIAN_POINT ( 'NONE',  ( 0.5576140732134206024, -0.4881889763779528324, 0.2082870074805215910 ) ) ;
#7169=DIRECTION ( 'NONE',  ( 0.000000000000000000, 0.000000000000000000, -1.000000000000000000 ) ) ;
#7172=DIRECTION ( 'NONE',  ( 0.000000000000000000, 1.000000000000000000, 0.000000000000000000 ) ) ;
#7179=EDGE_LOOP ( 'NONE', ( #7293, #1829, #471, #11511 ) ) ;
#7182=VERTEX_POINT ( 'NONE', #11244 ) ;
#7183=AXIS2_PLACEMENT_3D ( 'NONE', #7949, #3411, #4496 ) ;
#7189=LINE ( 'NONE', #8512, #3156 ) ;
#7190=DIRECTION ( 'NONE',  ( 0.000000000000000000, 0.000000000000000000, -1.000000000000000000 ) ) ;
#7191=CIRCLE ( 'NONE', #451, 0.003937007874015758385 ) ;
#7193=ORIENTED_EDGE ( 'NONE', *, *, #10480, .F. ) ;
#7194=DIRECTION ( 'NONE',  ( -0.000000000000000000, -0.000000000000000000, 1.000000000000000000 ) ) ;
#7202=DIRECTION ( 'NONE',  ( 0.000000000000000000, 0.000000000000000000, -1.000000000000000000 ) ) ;
#7206=LINE ( 'NONE', #5774, #9128 ) ;
#7208=CARTESIAN_POINT ( 'NONE',  ( -0.4769054117961255002, -0.09842519685039372024, 0.3480785096661502265 ) ) ;
#7210=AXIS2_PLACEMENT_3D ( 'NONE', #5082, #13487, #262 ) ;
#7216=DIRECTION ( 'NONE',  ( 0.000000000000000000, 1.000000000000000000, -0.000000000000000000 ) ) ;
#7217=VERTEX_POINT ( 'NONE', #8743 ) ;
#7219=AXIS2_PLACEMENT_3D ( 'NONE', #6172, #3759, #7508 ) ;
#7223=EDGE_CURVE ( 'NONE', #8290, #9755, #11349, .T. ) ;
#7225=DIRECTION ( 'NONE',  ( -0.8660254037844385966, 0.000000000000000000, -0.5000000000000003331 ) ) ;
#7227=CARTESIAN_POINT ( 'NONE',  ( 0.1062992125984796865, -0.09448818897637796532, -0.5870514566507987197 ) ) ;
#7233=DIRECTION ( 'NONE',  ( -0.000000000000000000, 1.000000000000000000, -0.000000000000000000 ) ) ;
#7235=ORIENTED_EDGE ( 'NONE', *, *, #11997, .T. ) ;
#7237=ORIENTED_EDGE ( 'NONE', *, *, #4982, .F. ) ;
#7238=ORIENTED_EDGE ( 'NONE', *, *, #944, .F. ) ;
#7244=CARTESIAN_POINT ( 'NONE',  ( 0.4769054117961250561, -0.4881889763779528324, 0.3480785096661500599 ) ) ;
#7248=EDGE_CURVE ( 'NONE', #2367, #3987, #7336, .T. ) ;
#7249=DIRECTION ( 'NONE',  ( 1.504632769052528010E-28, -8.673617379884035472E-15, -1.000000000000000000 ) ) ;
#7250=DIRECTION ( 'NONE',  ( 0.000000000000000000, -0.000000000000000000, 1.000000000000000000 ) ) ;
#7252=ORIENTED_EDGE ( 'NONE', *, *, #9638, .T. ) ;
#7253=ADVANCED_FACE ( 'NONE', ( #1531 ), #7640, .F. ) ;
#7254=VERTEX_POINT ( 'NONE', #590 ) ;
#7258=DIRECTION ( 'NONE',  ( -0.4999999999999966693, 0.000000000000000000, 0.8660254037844405950 ) ) ;
#7259=FACE_OUTER_BOUND ( 'NONE', #38, .T. ) ;
#7260=CARTESIAN_POINT ( 'NONE',  ( -0.3569402812043674933, -0.2952755905511811330, 0.1333425256503556200 ) ) ;
#7262=LINE ( 'NONE', #2487, #11135 ) ;
#7263=DIRECTION ( 'NONE',  ( -0.000000000000000000, -1.000000000000000000, -0.000000000000000000 ) ) ;
#7264=FACE_OUTER_BOUND ( 'NONE', #6536, .T. ) ;
#7265=CARTESIAN_POINT ( 'NONE',  ( -0.1463103599444685599, -0.09842519685039370636, -0.08447232569917004219 ) ) ;
#7266=ORIENTED_EDGE ( 'NONE', *, *, #9115, .T. ) ;
#7268=ORIENTED_EDGE ( 'NONE', *, *, #10009, .F. ) ;
#7269=DIRECTION ( 'NONE',  ( -0.8660254037844384856, 0.000000000000000000, -0.5000000000000003331 ) ) ;
#7274=DIRECTION ( 'NONE',  ( 0.000000000000000000, 0.000000000000000000, 1.000000000000000000 ) ) ;
#7281=EDGE_CURVE ( 'NONE', #3157, #897, #7845, .T. ) ;
#7284=VERTEX_POINT ( 'NONE', #5348 ) ;
#7285=DIRECTION ( 'NONE',  ( -1.000000000000000000, -0.000000000000000000, -3.614007241618347785E-16 ) ) ;
#7286=EDGE_CURVE ( 'NONE', #6774, #11698, #6283, .T. ) ;
#7287=CARTESIAN_POINT ( 'NONE',  ( -0.4591888763630547210, -0.4881889763779528324, 0.3787644491703232585 ) ) ;
#7289=DIRECTION ( 'NONE',  ( -0.8660254037844388186, 0.000000000000000000, 0.4999999999999995559 ) ) ;
#7291=DIRECTION ( 'NONE',  ( 0.000000000000000000, -1.000000000000000000, 0.000000000000000000 ) ) ;
#7293=ORIENTED_EDGE ( 'NONE', *, *, #5359, .T. ) ;
#7294=FACE_OUTER_BOUND ( 'NONE', #9362, .T. ) ;
#7295=DIRECTION ( 'NONE',  ( -1.734723475976802677E-14, 0.000000000000000000, -1.000000000000000000 ) ) ;
#7299=ADVANCED_FACE ( 'NONE', ( #14940 ), #10296, .T. ) ;
#7301=ORIENTED_EDGE ( 'NONE', *, *, #7281, .T. ) ;
#7302=ORIENTED_EDGE ( 'NONE', *, *, #7682, .F. ) ;
#7304=ADVANCED_FACE ( 'NONE', ( #5510 ), #4341, .F. ) ;
#7307=DIRECTION ( 'NONE',  ( 0.8660254037844384856, 0.000000000000000000, -0.5000000000000004441 ) ) ;
#7309=CARTESIAN_POINT ( 'NONE',  ( 0.1023622047244639455, -0.09842519685039372024, -0.5870514566507987197 ) ) ;
#7312=DIRECTION ( 'NONE',  ( 0.8660254037844464792, 0.000000000000000000, 0.4999999999999864553 ) ) ;
#7314=DIRECTION ( 'NONE',  ( -0.8660254037844405950, 0.000000000000000000, 0.4999999999999966693 ) ) ;
#7316=EDGE_LOOP ( 'NONE', ( #549, #5788, #9879, #402 ) ) ;
#7317=ORIENTED_EDGE ( 'NONE', *, *, #4733, .T. ) ;
#7321=EDGE_CURVE ( 'NONE', #4029, #11838, #3421, .T. ) ;
#7323=DIRECTION ( 'NONE',  ( -0.000000000000000000, -1.000000000000000000, -0.000000000000000000 ) ) ;
#7324=EDGE_CURVE ( 'NONE', #4499, #1289, #7010, .T. ) ;
#7325=CARTESIAN_POINT ( 'NONE',  ( 0.1552072824047652788, -0.09842519685039370636, -0.5870514566507987197 ) ) ;
#7328=FACE_OUTER_BOUND ( 'NONE', #8491, .T. ) ;
#7329=CARTESIAN_POINT ( 'NONE',  ( 0.06692913385832212347, -0.4881889763779528324, -0.5870514566507987197 ) ) ;
#7330=DIRECTION ( 'NONE',  ( 3.476578583725179813E-16, 0.000000000000000000, -1.000000000000000000 ) ) ;
#7332=EDGE_LOOP ( 'NONE', ( #8687, #5364, #13542 ) ) ;
#7336=CIRCLE ( 'NONE', #9106, 0.007874015748031501158 ) ;
#7338=CIRCLE ( 'NONE', #13110, 0.003937007874015780069 ) ;
#7339=CIRCLE ( 'NONE', #6080, 0.003937007874015724558 ) ;
#7340=CARTESIAN_POINT ( 'NONE',  ( 0.1552072824047652233, -0.003937007874015747977, -0.5870514566507987197 ) ) ;
#7341=EDGE_CURVE ( 'NONE', #12059, #1905, #4850, .T. ) ;
#7344=DIRECTION ( 'NONE',  ( 0.4999999999999922284, -0.000000000000000000, -0.8660254037844431485 ) ) ;
#7347=CARTESIAN_POINT ( 'NONE',  ( -0.6582248459352179060, -0.2952755905511811330, -0.3018834747714004840 ) ) ;
#7348=CARTESIAN_POINT ( 'NONE',  ( 0.2939481552201435588, -0.2952755905511811330, 0.2424480883318115843 ) ) ;
#7352=ORIENTED_EDGE ( 'NONE', *, *, #5284, .T. ) ;
#7354=ORIENTED_EDGE ( 'NONE', *, *, #13235, .F. ) ;
#7355=AXIS2_PLACEMENT_3D ( 'NONE', #12463, #7747, #626 ) ;
#7356=CIRCLE ( 'NONE', #2108, 0.003937007874015724558 ) ;
#7359=LINE ( 'NONE', #6707, #9342 ) ;
#7361=VECTOR ( 'NONE', #13754, 39.37007874015748143 ) ;
#7362=CIRCLE ( 'NONE', #7626, 0.04330708661417331101 ) ;
#7364=LINE ( 'NONE', #12164, #8354 ) ;
#7367=CIRCLE ( 'NONE', #2627, 0.003937007874015750579 ) ;
#7370=DIRECTION ( 'NONE',  ( 0.000000000000000000, 0.000000000000000000, 1.000000000000000000 ) ) ;
#7372=DIRECTION ( 'NONE',  ( 0.000000000000000000, 0.000000000000000000, -1.000000000000000000 ) ) ;
#7374=EDGE_CURVE ( 'NONE', #7659, #6576, #3844, .T. ) ;
#7377=AXIS2_PLACEMENT_3D ( 'NONE', #10321, #2021, #6719 ) ;
#7379=ORIENTED_EDGE ( 'NONE', *, *, #1552, .F. ) ;
#7381=VERTEX_POINT ( 'NONE', #9285 ) ;
#7382=ORIENTED_EDGE ( 'NONE', *, *, #8331, .F. ) ;
#7384=VERTEX_POINT ( 'NONE', #3255 ) ;
#7385=CYLINDRICAL_SURFACE ( 'NONE', #11148, 0.003937007874015759253 ) ;
#7386=CYLINDRICAL_SURFACE ( 'NONE', #8655, 0.003937007874015750579 ) ;
#7388=CARTESIAN_POINT ( 'NONE',  ( 0.1062992125984795755, -0.1023622047244094474, -0.2482618547481154070 ) ) ;
#7391=AXIS2_PLACEMENT_3D ( 'NONE', #14948, #11559, #11315 ) ;
#7395=AXIS2_PLACEMENT_3D ( 'NONE', #4405, #14115, #2284 ) ;
#7396=CARTESIAN_POINT ( 'NONE',  ( 0.1023622047244639177, -0.2952755905511811330, -0.4624047872104674606 ) ) ;
#7397=FACE_OUTER_BOUND ( 'NONE', #15158, .T. ) ;
#7398=DIRECTION ( 'NONE',  ( -6.505213034913065258E-15, 0.000000000000000000, -1.000000000000000000 ) ) ;
#7403=CIRCLE ( 'NONE', #14841, 0.003937007874015754916 ) ;
#7405=AXIS2_PLACEMENT_3D ( 'NONE', #3735, #3877, #11157 ) ;
#7406=VECTOR ( 'NONE', #669, 39.37007874015748143 ) ;
#7409=CARTESIAN_POINT ( 'NONE',  ( -0.5615510810874360104, -0.1023622047244094474, 0.2014679098129269763 ) ) ;
#7416=EDGE_CURVE ( 'NONE', #4753, #3491, #816, .T. ) ;
#7417=DIRECTION ( 'NONE',  ( 0.000000000000000000, 0.000000000000000000, 1.000000000000000000 ) ) ;
#7420=AXIS2_PLACEMENT_3D ( 'NONE', #1974, #788, #13872 ) ;
#7422=ORIENTED_EDGE ( 'NONE', *, *, #14781, .T. ) ;
#7423=EDGE_LOOP ( 'NONE', ( #11184, #1419, #8142, #10736 ) ) ;
#7424=ORIENTED_EDGE ( 'NONE', *, *, #2458, .F. ) ;
#7425=EDGE_CURVE ( 'NONE', #984, #253, #13603, .T. ) ;
#7428=AXIS2_PLACEMENT_3D ( 'NONE', #12131, #155, #10864 ) ;
#7431=CARTESIAN_POINT ( 'NONE',  ( -0.1618514667033796040, -0.4921259842519685179, 0.2122517380126066888 ) ) ;
#7433=CARTESIAN_POINT ( 'NONE',  ( -0.09842519685028337795, -0.2952755905511811330, -0.3757906139821208802 ) ) ;
#7439=AXIS2_PLACEMENT_3D ( 'NONE', #7972, #9069, #5459 ) ;
#7440=CARTESIAN_POINT ( 'NONE',  ( 0.06692913385832212347, -0.1023622047244094474, -0.5870514566507987197 ) ) ;
#7441=EDGE_LOOP ( 'NONE', ( #10563, #9485, #3013, #6343 ) ) ;
#7446=ORIENTED_EDGE ( 'NONE', *, *, #8742, .T. ) ;
#7447=LINE ( 'NONE', #12244, #10634 ) ;
#7448=CIRCLE ( 'NONE', #712, 0.003937007874015749712 ) ;
#7451=CIRCLE ( 'NONE', #3963, 0.003937007874015724558 ) ;
#7452=FACE_OUTER_BOUND ( 'NONE', #13782, .T. ) ;
#7454=EDGE_LOOP ( 'NONE', ( #14178, #8124, #13786, #7820 ) ) ;
#7455=CYLINDRICAL_SURFACE ( 'NONE', #10922, 0.003937007874015724558 ) ;
#7456=CARTESIAN_POINT ( 'NONE',  ( -0.06692913385815735250, -0.4881889763779528324, -0.5909884645248143498 ) ) ;
#7457=DIRECTION ( 'NONE',  ( -1.000000000000000000, 0.000000000000000000, 0.000000000000000000 ) ) ;
#7458=DIRECTION ( 'NONE',  ( 0.000000000000000000, 0.000000000000000000, 1.000000000000000000 ) ) ;
#7459=AXIS2_PLACEMENT_3D ( 'NONE', #3288, #11358, #8059 ) ;
#7462=VERTEX_POINT ( 'NONE', #11727 ) ;
#7463=EDGE_LOOP ( 'NONE', ( #12446, #515, #3032, #4308 ) ) ;
#7467=DIRECTION ( 'NONE',  ( 1.000000000000000000, 0.000000000000000000, 1.445602896647339903E-16 ) ) ;
#7473=DIRECTION ( 'NONE',  ( 0.5000000000000001110, 0.000000000000000000, -0.8660254037844385966 ) ) ;
#7477=DIRECTION ( 'NONE',  ( -1.000000000000000000, -0.000000000000000000, -3.476578583725179813E-16 ) ) ;
#7479=ADVANCED_FACE ( 'NONE', ( #278 ), #1365, .T. ) ;
#7482=VERTEX_POINT ( 'NONE', #2531 ) ;
#7484=CARTESIAN_POINT ( 'NONE',  ( -0.3964138223131424832, -0.2952755905511811330, 0.1515865201236451798 ) ) ;
#7487=CARTESIAN_POINT ( 'NONE',  ( 0.5084014747882494856, -0.4881889763779528324, 0.2935257283254013583 ) ) ;
#7488=DIRECTION ( 'NONE',  ( 0.5000000000000004441, 0.000000000000000000, -0.8660254037844382635 ) ) ;
#7492=LINE ( 'NONE', #297, #2822 ) ;
#7494=ORIENTED_EDGE ( 'NONE', *, *, #13482, .F. ) ;
#7495=EDGE_CURVE ( 'NONE', #315, #12429, #10698, .T. ) ;
#7496=ORIENTED_EDGE ( 'NONE', *, *, #12584, .F. ) ;
#7497=EDGE_LOOP ( 'NONE', ( #6537, #8872, #2687, #5392 ) ) ;
#7501=EDGE_LOOP ( 'NONE', ( #14309, #7193, #9335 ) ) ;
#7502=DIRECTION ( 'NONE',  ( 0.4999999999999979461, -0.000000000000000000, 0.8660254037844398178 ) ) ;
#7503=EDGE_CURVE ( 'NONE', #9212, #13179, #6076, .T. ) ;
#7504=CARTESIAN_POINT ( 'NONE',  ( -0.2393297813659119588, -0.09842519685039370636, 0.06089400679736759608 ) ) ;
#7508=DIRECTION ( 'NONE',  ( 0.000000000000000000, 0.000000000000000000, 1.000000000000000000 ) ) ;
#7514=ORIENTED_EDGE ( 'NONE', *, *, #9712, .F. ) ;
#7520=DIRECTION ( 'NONE',  ( -0.4999999999999996114, -0.000000000000000000, -0.8660254037844389297 ) ) ;
#7525=EDGE_CURVE ( 'NONE', #7766, #10116, #1108, .T. ) ;
#7526=CARTESIAN_POINT ( 'NONE',  ( 0.06299212598430636856, -0.2952755905511811330, -0.4190977005962941426 ) ) ;
#7527=CARTESIAN_POINT ( 'NONE',  ( 0.5413385826771386355, -0.1023622047244094474, 0.2443509997554994817 ) ) ;
#7530=ORIENTED_EDGE ( 'NONE', *, *, #3001, .T. ) ;
#7531=DIRECTION ( 'NONE',  ( 0.000000000000000000, -1.000000000000000000, 0.000000000000000000 ) ) ;
#7538=EDGE_CURVE ( 'NONE', #241, #7384, #2301, .T. ) ;
#7540=DIRECTION ( 'NONE',  ( 0.000000000000000000, -1.000000000000000000, -0.000000000000000000 ) ) ;
#7541=ORIENTED_EDGE ( 'NONE', *, *, #11825, .F. ) ;
#7542=ORIENTED_EDGE ( 'NONE', *, *, #747, .T. ) ;
#7545=CARTESIAN_POINT ( 'NONE',  ( 0.2652685895082805834, -0.4921259842519685179, 0.03495519865525829883 ) ) ;
#7555=DIRECTION ( 'NONE',  ( 0.000000000000000000, 1.000000000000000000, 0.000000000000000000 ) ) ;
#7561=EDGE_LOOP ( 'NONE', ( #8228, #7688, #14012, #8188 ) ) ;
#7564=TOROIDAL_SURFACE ( 'NONE', #9846, 0.007874015748031495954, 0.003937007874015747977 ) ;
#7568=VECTOR ( 'NONE', #4283, 39.37007874015748143 ) ;
#7569=CYLINDRICAL_SURFACE ( 'NONE', #11337, 0.003937007874015749712 ) ;
#7572=ADVANCED_FACE ( 'NONE', ( #10830 ), #3644, .F. ) ;
#7578=EDGE_LOOP ( 'NONE', ( #6230, #2946, #13246, #32 ) ) ;
#7581=CIRCLE ( 'NONE', #7096, 0.03937007874015751446 ) ;
#7582=VECTOR ( 'NONE', #2953, 39.37007874015748143 ) ;
#7583=AXIS2_PLACEMENT_3D ( 'NONE', #6659, #13734, #6805 ) ;
#7585=ORIENTED_EDGE ( 'NONE', *, *, #5790, .T. ) ;
#7588=CARTESIAN_POINT ( 'NONE',  ( -0.1586168312385622392, -0.09448818897637796532, -0.5890199605878065903 ) ) ;
#7589=TOROIDAL_SURFACE ( 'NONE', #852, 0.04330708661417328326, 0.003937007874015747977 ) ;
#7593=ADVANCED_FACE ( 'NONE', ( #8421 ), #2469, .T. ) ;
#7604=CYLINDRICAL_SURFACE ( 'NONE', #9694, 0.1574803149606299191 ) ;
#7607=ORIENTED_EDGE ( 'NONE', *, *, #5506, .T. ) ;
#7610=ORIENTED_EDGE ( 'NONE', *, *, #9137, .F. ) ;
#7612=AXIS2_PLACEMENT_3D ( 'NONE', #1256, #9641, #8150 ) ;
#7616=AXIS2_PLACEMENT_3D ( 'NONE', #9744, #4948, #9969 ) ;
#7623=CARTESIAN_POINT ( 'NONE',  ( -0.1724006475077544398, -0.1023622047244094474, 0.1728816592724491952 ) ) ;
#7626=AXIS2_PLACEMENT_3D ( 'NONE', #7065, #14052, #11714 ) ;
#7627=AXIS2_PLACEMENT_3D ( 'NONE', #2732, #7502, #9950 ) ;
#7629=ADVANCED_FACE ( 'NONE', ( #2836 ), #12558, .F. ) ;
#7630=ORIENTED_EDGE ( 'NONE', *, *, #15456, .F. ) ;
#7631=CIRCLE ( 'NONE', #10649, 0.003937007874015724558 ) ;
#7633=LINE ( 'NONE', #581, #7361 ) ;
#7636=ADVANCED_FACE ( 'NONE', ( #6506 ), #5108, .T. ) ;
#7637=TOROIDAL_SURFACE ( 'NONE', #12401, 0.007874015748031495954, 0.003937007874015747977 ) ;
#7638=VECTOR ( 'NONE', #13228, 39.37007874015748143 ) ;
#7640=PLANE ( 'NONE',  #14613 ) ;
#7642=AXIS2_PLACEMENT_3D ( 'NONE', #5586, #10386, #10540 ) ;
#7644=CARTESIAN_POINT ( 'NONE',  ( 0.4330708661417309036, -0.09448818897637796532, 0.4318761856142889766 ) ) ;
#7646=DIRECTION ( 'NONE',  ( -0.000000000000000000, 1.000000000000000000, 0.000000000000000000 ) ) ;
#7647=CARTESIAN_POINT ( 'NONE',  ( 0.1023622047244639455, -0.4881889763779528324, -0.5870514566507987197 ) ) ;
#7653=AXIS2_PLACEMENT_3D ( 'NONE', #7971, #6708, #15093 ) ;
#7654=ORIENTED_EDGE ( 'NONE', *, *, #7960, .F. ) ;
#7655=ORIENTED_EDGE ( 'NONE', *, *, #7374, .F. ) ;
#7656=ORIENTED_EDGE ( 'NONE', *, *, #15185, .F. ) ;
#7659=VERTEX_POINT ( 'NONE', #10048 ) ;
#7661=FACE_OUTER_BOUND ( 'NONE', #5572, .T. ) ;
#7662=CARTESIAN_POINT ( 'NONE',  ( 0.5418660417173575272, -0.1023622047244094474, 0.2355633981508976349 ) ) ;
#7673=CARTESIAN_POINT ( 'NONE',  ( -0.06299212598414158371, -0.2952755905511811330, -0.4624047872104674606 ) ) ;
#7675=ORIENTED_EDGE ( 'NONE', *, *, #15195, .T. ) ;
#7677=EDGE_CURVE ( 'NONE', #4061, #13962, #10854, .T. ) ;
#7682=EDGE_CURVE ( 'NONE', #12044, #5876, #10101, .T. ) ;
#7683=CARTESIAN_POINT ( 'NONE',  ( 0.000000000000000000, -0.4921259842519685179, -0.1535433070866141780 ) ) ;
#7684=DIRECTION ( 'NONE',  ( 0.000000000000000000, 0.000000000000000000, -1.000000000000000000 ) ) ;
#7688=ORIENTED_EDGE ( 'NONE', *, *, #5653, .F. ) ;
#7693=LINE ( 'NONE', #1896, #9467 ) ;
#7694=DIRECTION ( 'NONE',  ( 0.000000000000000000, 0.000000000000000000, -1.000000000000000000 ) ) ;
#7699=AXIS2_PLACEMENT_3D ( 'NONE', #1616, #2952, #10300 ) ;
#7701=ORIENTED_EDGE ( 'NONE', *, *, #3763, .T. ) ;
#7702=DIRECTION ( 'NONE',  ( -0.4999999999999998335, 0.000000000000000000, -0.8660254037844388186 ) ) ;
#7704=TOROIDAL_SURFACE ( 'NONE', #12468, 0.007874015748031495954, 0.003937007874015747977 ) ;
#7705=EDGE_CURVE ( 'NONE', #13131, #5345, #12866, .T. ) ;
#7707=ADVANCED_FACE ( 'NONE', ( #7848, #10216 ), #2137, .F. ) ;
#7708=LINE ( 'NONE', #5334, #1629 ) ;
#7709=CARTESIAN_POINT ( 'NONE',  ( 0.1062992125984795477, -0.1023622047244094474, -0.2482618547481154347 ) ) ;
#7711=LINE ( 'NONE', #1597, #8382 ) ;
#7712=AXIS2_PLACEMENT_3D ( 'NONE', #7916, #15045, #13869 ) ;
#7718=ORIENTED_EDGE ( 'NONE', *, *, #12800, .F. ) ;
#7719=CARTESIAN_POINT ( 'NONE',  ( -0.5413385826771385245, -0.1023622047244094474, 0.2443509997554989266 ) ) ;
#7721=EDGE_CURVE ( 'NONE', #15201, #9446, #12790, .T. ) ;
#7723=CARTESIAN_POINT ( 'NONE',  ( 0.5398975377803496567, -0.1023622047244094474, 0.2389729469846946508 ) ) ;
#7724=CARTESIAN_POINT ( 'NONE',  ( 0.1586168312385622392, -0.09448818897637796532, -0.5890199605878065903 ) ) ;
#7727=EDGE_CURVE ( 'NONE', #984, #2367, #1846, .T. ) ;
#7731=VERTEX_POINT ( 'NONE', #11613 ) ;
#7737=CARTESIAN_POINT ( 'NONE',  ( 0.06692913385832215123, -0.4881889763779528324, -0.5870514566507987197 ) ) ;
#7738=LINE ( 'NONE', #8832, #14456 ) ;
#7739=DIRECTION ( 'NONE',  ( 0.8660254037844365982, -0.000000000000000000, 0.5000000000000035527 ) ) ;
#7740=DIRECTION ( 'NONE',  ( 1.000000000000000000, -0.000000000000000000, -0.000000000000000000 ) ) ;
#7741=DIRECTION ( 'NONE',  ( -0.000000000000000000, -1.000000000000000000, -0.000000000000000000 ) ) ;
#7744=VERTEX_POINT ( 'NONE', #4248 ) ;
#7747=DIRECTION ( 'NONE',  ( 0.8660254037844365982, -0.000000000000000000, 0.5000000000000035527 ) ) ;
#7749=EDGE_LOOP ( 'NONE', ( #518, #12676 ) ) ;
#7754=DIRECTION ( 'NONE',  ( -1.000000000000000000, -0.000000000000000000, -0.000000000000000000 ) ) ;
#7761=ADVANCED_FACE ( 'NONE', ( #9192 ), #4312, .F. ) ;
#7763=DIRECTION ( 'NONE',  ( 0.000000000000000000, 1.000000000000000000, -0.000000000000000000 ) ) ;
#7766=VERTEX_POINT ( 'NONE', #4484 ) ;
#7767=ORIENTED_EDGE ( 'NONE', *, *, #1543, .T. ) ;
#7768=DIRECTION ( 'NONE',  ( -0.8660254037844385966, 0.000000000000000000, -0.5000000000000001110 ) ) ;
#7773=FACE_OUTER_BOUND ( 'NONE', #8363, .T. ) ;
#7774=VERTEX_POINT ( 'NONE', #7145 ) ;
#7778=CARTESIAN_POINT ( 'NONE',  ( -0.2353927734918962178, -0.09842519685039370636, 0.06771310446496157931 ) ) ;
#7783=EDGE_LOOP ( 'NONE', ( #6387, #8306 ) ) ;
#7784=ORIENTED_EDGE ( 'NONE', *, *, #182, .T. ) ;
#7789=CARTESIAN_POINT ( 'NONE',  ( 0.2325106836984822400, -0.1023622047244094474, 0.06483101467147835140 ) ) ;
#7792=DIRECTION ( 'NONE',  ( 0.8660254037844405950, 0.000000000000000000, 0.4999999999999966693 ) ) ;
#7794=ADVANCED_FACE ( 'NONE', ( #9570 ), #7112, .T. ) ;
#7801=ORIENTED_EDGE ( 'NONE', *, *, #2616, .T. ) ;
#7803=CARTESIAN_POINT ( 'NONE',  ( 1.928577636452524610E-17, -0.4921259842519685179, -0.1574803149606299191 ) ) ;
#7804=EDGE_CURVE ( 'NONE', #9228, #13529, #27, .T. ) ;
#7805=LINE ( 'NONE', #1718, #825 ) ;
#7806=DIRECTION ( 'NONE',  ( 0.000000000000000000, 1.000000000000000000, 0.000000000000000000 ) ) ;
#7807=CARTESIAN_POINT ( 'NONE',  ( -0.4552518684890389800, -0.1023622047244094474, 0.3855835468379172903 ) ) ;
#7810=DIRECTION ( 'NONE',  ( -0.000000000000000000, 1.000000000000000000, 0.000000000000000000 ) ) ;
#7811=CARTESIAN_POINT ( 'NONE',  ( -0.2681506793016945611, -0.4921259842519685179, 0.03207310886158504931 ) ) ;
#7813=FACE_OUTER_BOUND ( 'NONE', #7866, .T. ) ;
#7820=ORIENTED_EDGE ( 'NONE', *, *, #1743, .F. ) ;
#7827=CYLINDRICAL_SURFACE ( 'NONE', #11207, 0.003937007874015737569 ) ;
#7829=VERTEX_POINT ( 'NONE', #11781 ) ;
#7833=VECTOR ( 'NONE', #279, 39.37007874015748143 ) ;
#7837=AXIS2_PLACEMENT_3D ( 'NONE', #5636, #5485, #4394 ) ;
#7838=CYLINDRICAL_SURFACE ( 'NONE', #9438, 0.003937007874015758385 ) ;
#7840=ORIENTED_EDGE ( 'NONE', *, *, #2182, .F. ) ;
#7845=CIRCLE ( 'NONE', #1107, 0.03937007874015751446 ) ;
#7847=AXIS2_PLACEMENT_3D ( 'NONE', #7807, #5982, #9687 ) ;
#7848=FACE_BOUND ( 'NONE', #8703, .T. ) ;
#7850=AXIS2_PLACEMENT_3D ( 'NONE', #11509, #8844, #15038 ) ;
#7851=DIRECTION ( 'NONE',  ( -0.8660254037844388186, 0.000000000000000000, 0.4999999999999995559 ) ) ;
#7852=LINE ( 'NONE', #7940, #11626 ) ;
#7853=ORIENTED_EDGE ( 'NONE', *, *, #145, .T. ) ;
#7854=DIRECTION ( 'NONE',  ( 0.8660254037844389297, 0.000000000000000000, -0.4999999999999994449 ) ) ;
#7856=CARTESIAN_POINT ( 'NONE',  ( -0.1724006475077544398, -0.4921259842519685179, 0.1768186671464649640 ) ) ;
#7860=AXIS2_PLACEMENT_3D ( 'NONE', #6105, #8249, #11849 ) ;
#7861=ORIENTED_EDGE ( 'NONE', *, *, #9047, .F. ) ;
#7864=ORIENTED_EDGE ( 'NONE', *, *, #409, .T. ) ;
#7866=EDGE_LOOP ( 'NONE', ( #3566, #12610, #13052, #4010 ) ) ;
#7868=EDGE_CURVE ( 'NONE', #12353, #6007, #6592, .T. ) ;
#7871=LENGTH_MEASURE_WITH_UNIT ( LENGTH_MEASURE( 0.02539999999999999897 ), #11310 );
#7872=VECTOR ( 'NONE', #5111, 39.37007874015748143 ) ;
#7873=VECTOR ( 'NONE', #10365, 39.37007874015748143 ) ;
#7874=DIRECTION ( 'NONE',  ( -1.000000000000000000, 5.204170427930430118E-14, -0.000000000000000000 ) ) ;
#7876=ADVANCED_FACE ( 'NONE', ( #2305 ), #3563, .T. ) ;
#7883=VERTEX_POINT ( 'NONE', #5673 ) ;
#7887=CIRCLE ( 'NONE', #6131, 0.003937007874015724558 ) ;
#7888=EDGE_LOOP ( 'NONE', ( #11959, #5231, #427, #4599 ) ) ;
#7894=FACE_OUTER_BOUND ( 'NONE', #14523, .T. ) ;
#7896=EDGE_CURVE ( 'NONE', #13132, #1093, #367, .T. ) ;
#7897=CARTESIAN_POINT ( 'NONE',  ( -0.3137366569588388998, -0.2952755905511811330, 0.2947875711430708590 ) ) ;
#7905=DIRECTION ( 'NONE',  ( 0.000000000000000000, 0.000000000000000000, -1.000000000000000000 ) ) ;
#7907=ORIENTED_EDGE ( 'NONE', *, *, #5790, .F. ) ;
#7909=ORIENTED_EDGE ( 'NONE', *, *, #1352, .T. ) ;
#7910=CIRCLE ( 'NONE', #678, 0.003937007874015758385 ) ;
#7912=VECTOR ( 'NONE', #3871, 39.37007874015748143 ) ;
#7913=CYLINDRICAL_SURFACE ( 'NONE', #3860, 0.003937007874015724558 ) ;
#7914=DIRECTION ( 'NONE',  ( -1.060575238724906668E-16, 1.000000000000000000, -6.123233995736768501E-17 ) ) ;
#7915=EDGE_CURVE ( 'NONE', #13903, #14791, #10621, .T. ) ;
#7916=CARTESIAN_POINT ( 'NONE',  ( -0.1062992125983148878, -0.1023622047244094474, -0.5909884645248143498 ) ) ;
#7919=LINE ( 'NONE', #9092, #11949 ) ;
#7920=CARTESIAN_POINT ( 'NONE',  ( 0.5413385826771386355, -0.09448818897637796532, 0.2443509997554994817 ) ) ;
#7921=AXIS2_PLACEMENT_3D ( 'NONE', #10691, #8321, #4417 ) ;
#7925=EDGE_LOOP ( 'NONE', ( #4048, #12270, #4662, #3415 ) ) ;
#7931=ORIENTED_EDGE ( 'NONE', *, *, #8024, .T. ) ;
#7934=CARTESIAN_POINT ( 'NONE',  ( 0.5871416322685650835, 0.000000000000000000, 0.1571437749735215272 ) ) ;
#7939=AXIS2_PLACEMENT_3D ( 'NONE', #4827, #14485, #2415 ) ;
#7940=CARTESIAN_POINT ( 'NONE',  ( -0.5905511811023629321, -0.09448818897637796532, 0.1591122789105256785 ) ) ;
#7948=ORIENTED_EDGE ( 'NONE', *, *, #9830, .F. ) ;
#7949=CARTESIAN_POINT ( 'NONE',  ( -0.6582248459352179060, -0.2952755905511811330, -0.3018834747714004840 ) ) ;
#7952=ORIENTED_EDGE ( 'NONE', *, *, #9530, .F. ) ;
#7955=CIRCLE ( 'NONE', #4459, 0.003937007874015724558 ) ;
#7956=SPHERICAL_SURFACE ( 'NONE', #2705, 0.003937007874015747977 ) ;
#7957=LINE ( 'NONE', #6609, #13577 ) ;
#7960=EDGE_CURVE ( 'NONE', #3213, #9228, #15249, .T. ) ;
#7966=VECTOR ( 'NONE', #11573, 39.37007874015748143 ) ;
#7967=ORIENTED_EDGE ( 'NONE', *, *, #9597, .T. ) ;
#7968=ORIENTED_EDGE ( 'NONE', *, *, #4819, .T. ) ;
#7969=ADVANCED_FACE ( 'NONE', ( #11803 ), #15410, .T. ) ;
#7970=DIRECTION ( 'NONE',  ( -1.000000000000000000, -0.000000000000000000, -3.614007241618347785E-16 ) ) ;
#7971=CARTESIAN_POINT ( 'NONE',  ( -0.06692913385815749128, -0.1023622047244094474, -0.2377126739438355507 ) ) ;
#7972=CARTESIAN_POINT ( 'NONE',  ( 0.5905511811023622659, -0.2952755905511811330, -0.4190977005962939206 ) ) ;
#7976=DIRECTION ( 'NONE',  ( 0.8660254037844383745, 0.000000000000000000, 0.5000000000000004441 ) ) ;
#7978=CARTESIAN_POINT ( 'NONE',  ( 0.1724006475077543565, -0.4921259842519685179, 0.1728816592724491952 ) ) ;
#7980=DIRECTION ( 'NONE',  ( 0.8660254037844395958, 0.000000000000000000, 0.4999999999999982236 ) ) ;
#7986=EDGE_CURVE ( 'NONE', #11452, #8847, #216, .T. ) ;
#7988=ORIENTED_EDGE ( 'NONE', *, *, #1858, .T. ) ;
#7991=LINE ( 'NONE', #10657, #14894 ) ;
#7992=DIRECTION ( 'NONE',  ( 0.000000000000000000, 0.000000000000000000, 1.000000000000000000 ) ) ;
#7993=DIRECTION ( 'NONE',  ( 0.8660254037844385966, -0.000000000000000000, 0.5000000000000001110 ) ) ;
#7995=LINE ( 'NONE', #5633, #14939 ) ;
#7998=FACE_OUTER_BOUND ( 'NONE', #9198, .T. ) ;
#7999=ORIENTED_EDGE ( 'NONE', *, *, #10185, .T. ) ;
#8004=EDGE_LOOP ( 'NONE', ( #10606, #12815 ) ) ;
#8005=EDGE_LOOP ( 'NONE', ( #11744, #9421, #1738, #5637 ) ) ;
#8007=DIRECTION ( 'NONE',  ( 0.000000000000000000, -0.000000000000000000, -1.000000000000000000 ) ) ;
#8008=EDGE_CURVE ( 'NONE', #4713, #2230, #11359, .T. ) ;
#8010=DIRECTION ( 'NONE',  ( 4.336808689942006376E-14, 0.000000000000000000, -1.000000000000000000 ) ) ;
#8012=DIRECTION ( 'NONE',  ( 0.8660254037844388186, -0.000000000000000000, -0.4999999999999995559 ) ) ;
#8013=DIRECTION ( 'NONE',  ( -1.000000000000000000, -0.000000000000000000, -3.614007241618347785E-16 ) ) ;
#8016=LINE ( 'NONE', #8257, #12385 ) ;
#8017=CARTESIAN_POINT ( 'NONE',  ( -0.05314960629918528967, -0.09842519685039370636, -0.09205781851247189784 ) ) ;
#8021=VERTEX_POINT ( 'NONE', #13277 ) ;
#8024=EDGE_CURVE ( 'NONE', #11911, #12552, #133, .T. ) ;
#8025=CARTESIAN_POINT ( 'NONE',  ( -0.5595825771504281398, -0.09842519685039372024, 0.2048774586467239645 ) ) ;
#8028=FACE_OUTER_BOUND ( 'NONE', #10822, .T. ) ;
#8031=LINE ( 'NONE', #9465, #5303 ) ;
#8036=VERTEX_POINT ( 'NONE', #11970 ) ;
#8038=CARTESIAN_POINT ( 'NONE',  ( 0.06692913385832209572, -0.2952755905511811330, -0.4624047872104674606 ) ) ;
#8041=FACE_OUTER_BOUND ( 'NONE', #771, .T. ) ;
#8042=FACE_OUTER_BOUND ( 'NONE', #13412, .T. ) ;
#8045=ORIENTED_EDGE ( 'NONE', *, *, #2458, .T. ) ;
#8046=DIRECTION ( 'NONE',  ( 0.8660254037844383745, 0.000000000000000000, 0.5000000000000004441 ) ) ;
#8047=EDGE_CURVE ( 'NONE', #13962, #13771, #12881, .T. ) ;
#8053=LINE ( 'NONE', #10421, #3876 ) ;
#8054=EDGE_CURVE ( 'NONE', #12616, #5709, #11628, .T. ) ;
#8055=ADVANCED_FACE ( 'NONE', ( #5985 ), #2537, .F. ) ;
#8056=DIRECTION ( 'NONE',  ( 0.000000000000000000, 0.000000000000000000, 1.000000000000000000 ) ) ;
#8058=FACE_OUTER_BOUND ( 'NONE', #1799, .T. ) ;
#8059=DIRECTION ( 'NONE',  ( 1.000000000000000000, 8.673617379884013384E-15, 0.000000000000000000 ) ) ;
#8063=EDGE_CURVE ( 'NONE', #9261, #6775, #13625, .T. ) ;
#8069=AXIS2_PLACEMENT_3D ( 'NONE', #14546, #12277, #1536 ) ;
#8074=ADVANCED_FACE ( 'NONE', ( #9831 ), #10772, .F. ) ;
#8081=DIRECTION ( 'NONE',  ( 0.000000000000000000, 0.000000000000000000, 1.000000000000000000 ) ) ;
#8082=VECTOR ( 'NONE', #14346, 39.37007874015748854 ) ;
#8084=DIRECTION ( 'NONE',  ( -0.000000000000000000, 1.000000000000000000, 0.000000000000000000 ) ) ;
#8086=DIRECTION ( 'NONE',  ( 1.224646799147358384E-16, 0.000000000000000000, -1.000000000000000000 ) ) ;
#8087=AXIS2_PLACEMENT_3D ( 'NONE', #2476, #2539, #1379 ) ;
#8088=ADVANCED_FACE ( 'NONE', ( #14771 ), #10140, .T. ) ;
#8090=CARTESIAN_POINT ( 'NONE',  ( 0.06011003619072806392, -0.1023622047244094474, -0.2337756660697248301 ) ) ;
#8091=DIRECTION ( 'NONE',  ( -0.8660254037844389297, -0.000000000000000000, 0.4999999999999994449 ) ) ;
#8092=DIRECTION ( 'NONE',  ( 0.000000000000000000, 1.000000000000000000, 0.000000000000000000 ) ) ;
#8094=EDGE_LOOP ( 'NONE', ( #5827, #13838, #13280, #3250 ) ) ;
#8096=EDGE_CURVE ( 'NONE', #9504, #3033, #13136, .T. ) ;
#8097=CYLINDRICAL_SURFACE ( 'NONE', #4852, 0.003937007874015758385 ) ;
#8099=ORIENTED_EDGE ( 'NONE', *, *, #11037, .T. ) ;
#8102=AXIS2_PLACEMENT_3D ( 'NONE', #1199, #3464, #14193 ) ;
#8109=DIRECTION ( 'NONE',  ( 1.000000000000000000, 0.000000000000000000, -1.224646799147353207E-16 ) ) ;
#8110=CARTESIAN_POINT ( 'NONE',  ( 0.06299212598430639631, -0.4921259842519685179, -0.5870514566507987197 ) ) ;
#8111=ADVANCED_FACE ( 'NONE', ( #2940, #1759 ), #5502, .T. ) ;
#8115=FACE_OUTER_BOUND ( 'NONE', #1006, .T. ) ;
#8118=AXIS2_PLACEMENT_3D ( 'NONE', #2219, #11782, #14122 ) ;
#8119=EDGE_CURVE ( 'NONE', #556, #8212, #7711, .T. ) ;
#8120=VERTEX_POINT ( 'NONE', #6513 ) ;
#8122=EDGE_CURVE ( 'NONE', #4524, #315, #512, .T. ) ;
#8124=ORIENTED_EDGE ( 'NONE', *, *, #8047, .T. ) ;
#8127=CIRCLE ( 'NONE', #6104, 0.003937007874015724558 ) ;
#8130=AXIS2_PLACEMENT_3D ( 'NONE', #12016, #10810, #99 ) ;
#8133=CARTESIAN_POINT ( 'NONE',  ( -0.1618514667033796040, -0.4921259842519685179, 0.2083147301385909200 ) ) ;
#8134=CARTESIAN_POINT ( 'NONE',  ( -0.5452755905511542656, -0.09842519685039370636, 0.2375319020879049503 ) ) ;
#8137=LINE ( 'NONE', #1017, #2684 ) ;
#8138=CARTESIAN_POINT ( 'NONE',  ( 0.4803149606299220720, -0.4881889763779528324, 0.3500470136031578750 ) ) ;
#8140=AXIS2_PLACEMENT_3D ( 'NONE', #13415, #6032, #14357 ) ;
#8142=ORIENTED_EDGE ( 'NONE', *, *, #3219, .T. ) ;
#8145=VERTEX_POINT ( 'NONE', #4182 ) ;
#8148=AXIS2_PLACEMENT_3D ( 'NONE', #6963, #15268, #9396 ) ;
#8150=DIRECTION ( 'NONE',  ( 0.000000000000000000, 1.734723475976817507E-14, -1.000000000000000000 ) ) ;
#8151=LINE ( 'NONE', #2268, #8628 ) ;
#8153=FACE_OUTER_BOUND ( 'NONE', #2156, .T. ) ;
#8154=VECTOR ( 'NONE', #9531, 39.37007874015748854 ) ;
#8155=CARTESIAN_POINT ( 'NONE',  ( -0.4307978335858689278, -0.09842519685039370636, 0.4318761856142863120 ) ) ;
#8157=DIRECTION ( 'NONE',  ( 0.5000000000000004441, 0.000000000000000000, -0.8660254037844383745 ) ) ;
#8158=CARTESIAN_POINT ( 'NONE',  ( 0.5629921259843070347, -0.1023622047244094474, 0.2068459625837795746 ) ) ;
#8159=DIRECTION ( 'NONE',  ( 0.5000000000000003331, 0.000000000000000000, -0.8660254037844385966 ) ) ;
#8160=FACE_OUTER_BOUND ( 'NONE', #3110, .T. ) ;
#8161=ORIENTED_EDGE ( 'NONE', *, *, #11637, .T. ) ;
#8164=AXIS2_PLACEMENT_3D ( 'NONE', #11379, #5719, #12555 ) ;
#8166=EDGE_CURVE ( 'NONE', #13305, #13509, #6445, .T. ) ;
#8172=ADVANCED_FACE ( 'NONE', ( #4025 ), #8801, .T. ) ;
#8173=CARTESIAN_POINT ( 'NONE',  ( 0.4591888763630541104, -0.4881889763779528324, 0.3787644491703229810 ) ) ;
#8174=DIRECTION ( 'NONE',  ( 0.8660254037844389297, 0.000000000000000000, -0.4999999999999996669 ) ) ;
#8179=VECTOR ( 'NONE', #15233, 39.37007874015748143 ) ;
#8184=AXIS2_PLACEMENT_3D ( 'NONE', #1105, #10269, #6895 ) ;
#8185=DIRECTION ( 'NONE',  ( 0.000000000000000000, 0.000000000000000000, 1.000000000000000000 ) ) ;
#8186=DIRECTION ( 'NONE',  ( 0.5000000000000004441, 0.000000000000000000, 0.8660254037844383745 ) ) ;
#8188=ORIENTED_EDGE ( 'NONE', *, *, #778, .F. ) ;
#8192=ORIENTED_EDGE ( 'NONE', *, *, #5290, .T. ) ;
#8193=AXIS2_PLACEMENT_3D ( 'NONE', #2823, #1901, #10042 ) ;
#8195=EDGE_CURVE ( 'NONE', #556, #5098, #4877, .T. ) ;
#8196=ORIENTED_EDGE ( 'NONE', *, *, #3196, .F. ) ;
#8198=AXIS2_PLACEMENT_3D ( 'NONE', #7347, #12155, #3531 ) ;
#8199=DIRECTION ( 'NONE',  ( 0.000000000000000000, 1.000000000000000000, -0.000000000000000000 ) ) ;
#8202=FACE_OUTER_BOUND ( 'NONE', #299, .T. ) ;
#8203=DIRECTION ( 'NONE',  ( 0.000000000000000000, 0.000000000000000000, -1.000000000000000000 ) ) ;
#8205=DIRECTION ( 'NONE',  ( 1.000000000000000000, -8.673617379884051249E-15, 0.000000000000000000 ) ) ;
#8206=CIRCLE ( 'NONE', #5674, 0.003937007874015735834 ) ;
#8207=CARTESIAN_POINT ( 'NONE',  ( -0.1552072824047652788, 0.000000000000000000, -0.5870514566507987197 ) ) ;
#8210=ORIENTED_EDGE ( 'NONE', *, *, #11828, .T. ) ;
#8211=ORIENTED_EDGE ( 'NONE', *, *, #13916, .F. ) ;
#8212=VERTEX_POINT ( 'NONE', #441 ) ;
#8213=VERTEX_POINT ( 'NONE', #12566 ) ;
#8214=EDGE_CURVE ( 'NONE', #6899, #8756, #1376, .T. ) ;
#8217=AXIS2_PLACEMENT_3D ( 'NONE', #14820, #2993, #12628 ) ;
#8222=CARTESIAN_POINT ( 'NONE',  ( 0.06692913385832215123, -0.4921259842519685179, -0.5870514566507987197 ) ) ;
#8223=ORIENTED_EDGE ( 'NONE', *, *, #10006, .T. ) ;
#8228=ORIENTED_EDGE ( 'NONE', *, *, #5756, .T. ) ;
#8230=ORIENTED_EDGE ( 'NONE', *, *, #10576, .T. ) ;
#8234=DIRECTION ( 'NONE',  ( 0.8660254037844385966, -0.000000000000000000, -0.5000000000000001110 ) ) ;
#8235=DIRECTION ( 'NONE',  ( 0.000000000000000000, -0.000000000000000000, -1.000000000000000000 ) ) ;
#8239=LINE ( 'NONE', #13013, #5089 ) ;
#8240=CARTESIAN_POINT ( 'NONE',  ( 0.4342073824196633347, -0.003937007874015747977, 0.4299076816772810505 ) ) ;
#8245=ORIENTED_EDGE ( 'NONE', *, *, #12054, .T. ) ;
#8246=VERTEX_POINT ( 'NONE', #1827 ) ;
#8248=DIRECTION ( 'NONE',  ( 0.8660254037844405950, 1.502314598737171929E-14, 0.4999999999999967804 ) ) ;
#8249=DIRECTION ( 'NONE',  ( -0.5000000000000000000, 0.000000000000000000, 0.8660254037844385966 ) ) ;
#8257=CARTESIAN_POINT ( 'NONE',  ( 0.000000000000000000, -0.4921259842519685179, 0.1768186671464649640 ) ) ;
#8258=EDGE_CURVE ( 'NONE', #2728, #15156, #12649, .T. ) ;
#8261=DIRECTION ( 'NONE',  ( -1.000000000000000000, 0.000000000000000000, 0.000000000000000000 ) ) ;
#8262=ORIENTED_EDGE ( 'NONE', *, *, #10419, .F. ) ;
#8263=ORIENTED_EDGE ( 'NONE', *, *, #8166, .F. ) ;
#8265=DIRECTION ( 'NONE',  ( 0.4999999999999966693, 0.000000000000000000, -0.8660254037844405950 ) ) ;
#8267=EDGE_CURVE ( 'NONE', #14387, #6881, #11894, .T. ) ;
#8277=ORIENTED_EDGE ( 'NONE', *, *, #4923, .T. ) ;
#8278=ORIENTED_EDGE ( 'NONE', *, *, #15304, .F. ) ;
#8279=CARTESIAN_POINT ( 'NONE',  ( -0.1062992125983150127, -0.09842519685039370636, -0.2482618547482104143 ) ) ;
#8280=EDGE_CURVE ( 'NONE', #11605, #10010, #5352, .T. ) ;
#8284=CARTESIAN_POINT ( 'NONE',  ( 0.3137366569588399545, -0.2952755905511811330, 0.2947875711430715251 ) ) ;
#8287=EDGE_CURVE ( 'NONE', #12429, #7254, #8016, .T. ) ;
#8290=VERTEX_POINT ( 'NONE', #15150 ) ;
#8294=DIRECTION ( 'NONE',  ( -1.000000000000000000, 0.000000000000000000, 0.000000000000000000 ) ) ;
#8298=FACE_OUTER_BOUND ( 'NONE', #3391, .T. ) ;
#8299=CARTESIAN_POINT ( 'NONE',  ( -0.4788739157331332597, -0.1023622047244094474, 0.3446689608323532106 ) ) ;
#8301=VERTEX_POINT ( 'NONE', #10525 ) ;
#8303=DIRECTION ( 'NONE',  ( 0.000000000000000000, -1.000000000000000000, 0.000000000000000000 ) ) ;
#8304=CARTESIAN_POINT ( 'NONE',  ( 0.1028896637646825735, -0.09842519685039372024, -0.2462933508111075642 ) ) ;
#8305=SPHERICAL_SURFACE ( 'NONE', #8102, 0.003937007874015747977 ) ;
#8306=ORIENTED_EDGE ( 'NONE', *, *, #1301, .T. ) ;
#8307=EDGE_CURVE ( 'NONE', #14774, #2262, #3246, .T. ) ;
#8308=ORIENTED_EDGE ( 'NONE', *, *, #10390, .F. ) ;
#8310=VECTOR ( 'NONE', #5575, 39.37007874015748143 ) ;
#8312=CARTESIAN_POINT ( 'NONE',  ( 0.000000000000000000, -0.1023622047244094474, 0.000000000000000000 ) ) ;
#8319=FACE_OUTER_BOUND ( 'NONE', #3051, .T. ) ;
#8320=CARTESIAN_POINT ( 'NONE',  ( 0.1062992125984795477, -0.09842519685039370636, -0.2482618547481155458 ) ) ;
#8321=DIRECTION ( 'NONE',  ( 0.8660254037844384856, 0.000000000000000000, 0.5000000000000004441 ) ) ;
#8328=AXIS2_PLACEMENT_3D ( 'NONE', #7287, #8397, #5879 ) ;
#8331=EDGE_CURVE ( 'NONE', #14773, #8390, #1051, .T. ) ;
#8332=DIRECTION ( 'NONE',  ( -0.000000000000000000, 1.000000000000000000, 0.000000000000000000 ) ) ;
#8340=AXIS2_PLACEMENT_3D ( 'NONE', #12949, #15458, #12074 ) ;
#8342=ORIENTED_EDGE ( 'NONE', *, *, #10282, .F. ) ;
#8343=EDGE_CURVE ( 'NONE', #3491, #7659, #9349, .T. ) ;
#8345=ORIENTED_EDGE ( 'NONE', *, *, #14500, .F. ) ;
#8346=VECTOR ( 'NONE', #8658, 39.37007874015748143 ) ;
#8347=ORIENTED_EDGE ( 'NONE', *, *, #11951, .T. ) ;
#8348=EDGE_CURVE ( 'NONE', #2464, #1302, #3637, .T. ) ;
#8354=VECTOR ( 'NONE', #14810, 39.37007874015748143 ) ;
#8355=DIRECTION ( 'NONE',  ( -0.8660254037844398178, 0.000000000000000000, 0.4999999999999979461 ) ) ;
#8356=VECTOR ( 'NONE', #14029, 39.37007874015748143 ) ;
#8358=DIRECTION ( 'NONE',  ( -3.942553354492736135E-16, 0.000000000000000000, 1.000000000000000000 ) ) ;
#8359=ORIENTED_EDGE ( 'NONE', *, *, #10779, .F. ) ;
#8360=DIRECTION ( 'NONE',  ( -1.000000000000000000, 0.000000000000000000, -3.973232667114494807E-16 ) ) ;
#8361=DIRECTION ( 'NONE',  ( -0.4999999999999966693, 0.000000000000000000, -0.8660254037844405950 ) ) ;
#8362=ADVANCED_BREP_SHAPE_REPRESENTATION ( '', ( #9119, #11481 ), #5701 ) ;
#8363=EDGE_LOOP ( 'NONE', ( #1693, #3265, #14492 ) ) ;
#8366=AXIS2_PLACEMENT_3D ( 'NONE', #7737, #5287, #13533 ) ;
#8367=AXIS2_PLACEMENT_3D ( 'NONE', #4675, #9462, #3500 ) ;
#8381=CARTESIAN_POINT ( 'NONE',  ( 0.4749369078591172411, -0.4881889763779528324, 0.3514880584999470203 ) ) ;
#8382=VECTOR ( 'NONE', #15007, 39.37007874015748854 ) ;
#8387=DIRECTION ( 'NONE',  ( 0.000000000000000000, 0.000000000000000000, -1.000000000000000000 ) ) ;
#8389=CARTESIAN_POINT ( 'NONE',  ( -0.06692913385815749128, -0.4921259842519685179, -0.2377126739438355507 ) ) ;
#8390=VERTEX_POINT ( 'NONE', #6918 ) ;
#8391=AXIS2_PLACEMENT_3D ( 'NONE', #10862, #9392, #8358 ) ;
#8392=ORIENTED_EDGE ( 'NONE', *, *, #4923, .F. ) ;
#8394=CARTESIAN_POINT ( 'NONE',  ( -0.2359202325321149429, -0.4921259842519685179, 0.06286251073437550130 ) ) ;
#8395=VECTOR ( 'NONE', #9490, 39.37007874015748143 ) ;
#8396=EDGE_CURVE ( 'NONE', #517, #11768, #7362, .T. ) ;
#8397=DIRECTION ( 'NONE',  ( -0.8660254037844352659, 0.000000000000000000, 0.5000000000000058842 ) ) ;
#8401=CYLINDRICAL_SURFACE ( 'NONE', #11116, 0.003937007874015750579 ) ;
#8406=CARTESIAN_POINT ( 'NONE',  ( -0.1618514667033796040, -0.1023622047244094474, 0.2122517380126066888 ) ) ;
#8407=EDGE_CURVE ( 'NONE', #5098, #11032, #629, .T. ) ;
#8409=VECTOR ( 'NONE', #1748, 39.37007874015748143 ) ;
#8411=FACE_OUTER_BOUND ( 'NONE', #4685, .T. ) ;
#8413=FACE_OUTER_BOUND ( 'NONE', #10295, .T. ) ;
#8421=FACE_OUTER_BOUND ( 'NONE', #8004, .T. ) ;
#8422=DIRECTION ( 'NONE',  ( -0.8660254037844385966, 0.000000000000000000, -0.5000000000000001110 ) ) ;
#8424=CARTESIAN_POINT ( 'NONE',  ( 0.4307978335858662633, -0.09448818897637796532, 0.4279391777402732910 ) ) ;
#8429=FACE_OUTER_BOUND ( 'NONE', #5005, .T. ) ;
#8430=CARTESIAN_POINT ( 'NONE',  ( -0.06692913385815749128, -0.4921259842519685179, -0.2377126739438355507 ) ) ;
#8433=ORIENTED_EDGE ( 'NONE', *, *, #2596, .T. ) ;
#8434=CIRCLE ( 'NONE', #10697, 0.03937007874015750752 ) ;
#8435=ORIENTED_EDGE ( 'NONE', *, *, #3600, .T. ) ;
#8437=DIRECTION ( 'NONE',  ( -1.000000000000000000, -0.000000000000000000, -0.000000000000000000 ) ) ;
#8442=EDGE_CURVE ( 'NONE', #2963, #10145, #8623, .T. ) ;
#8443=DIRECTION ( 'NONE',  ( 0.000000000000000000, 0.000000000000000000, 1.000000000000000000 ) ) ;
#8444=DIRECTION ( 'NONE',  ( -0.4999999999999986122, 2.168404344971006501E-15, 0.8660254037844395958 ) ) ;
#8445=AXIS2_PLACEMENT_3D ( 'NONE', #7527, #12175, #3783 ) ;
#8448=DIRECTION ( 'NONE',  ( -1.000000000000000000, -6.505213034913066047E-15, -0.000000000000000000 ) ) ;
#8454=ORIENTED_EDGE ( 'NONE', *, *, #11623, .T. ) ;
#8455=CIRCLE ( 'NONE', #8702, 0.007874015748031482076 ) ;
#8461=FACE_OUTER_BOUND ( 'NONE', #15108, .T. ) ;
#8467=ADVANCED_FACE ( 'NONE', ( #5968 ), #14394, .F. ) ;
#8468=ORIENTED_EDGE ( 'NONE', *, *, #10836, .F. ) ;
#8469=CARTESIAN_POINT ( 'NONE',  ( 0.1062992125984795477, -0.1023622047244094474, -0.2472069366676780122 ) ) ;
#8473=EDGE_CURVE ( 'NONE', #10209, #6217, #8486, .T. ) ;
#8474=ORIENTED_EDGE ( 'NONE', *, *, #10832, .T. ) ;
#8476=AXIS2_PLACEMENT_3D ( 'NONE', #4775, #8235, #14097 ) ;
#8477=DIRECTION ( 'NONE',  ( 0.000000000000000000, 1.000000000000000000, 0.000000000000000000 ) ) ;
#8486=LINE ( 'NONE', #8548, #6878 ) ;
#8488=EDGE_CURVE ( 'NONE', #6775, #10534, #1350, .T. ) ;
#8489=DIRECTION ( 'NONE',  ( 0.8660254037844383745, 0.000000000000000000, 0.5000000000000004441 ) ) ;
#8490=EDGE_CURVE ( 'NONE', #11452, #3552, #2872, .T. ) ;
#8491=EDGE_LOOP ( 'NONE', ( #1906, #7607, #5787 ) ) ;
#8492=EDGE_LOOP ( 'NONE', ( #8161, #14137, #1853 ) ) ;
#8494=VERTEX_POINT ( 'NONE', #13191 ) ;
#8498=DIRECTION ( 'NONE',  ( -0.8660254037844385966, 0.000000000000000000, -0.5000000000000000000 ) ) ;
#8503=DIRECTION ( 'NONE',  ( 0.000000000000000000, 1.000000000000000000, -8.673617379884035472E-15 ) ) ;
#8504=PLANE ( 'NONE',  #1835 ) ;
#8506=ORIENTED_EDGE ( 'NONE', *, *, #8267, .T. ) ;
#8508=EDGE_CURVE ( 'NONE', #1093, #13132, #6116, .T. ) ;
#8510=CARTESIAN_POINT ( 'NONE',  ( -1.315994971760645248E-15, -0.09842519685039370636, 0.4279391777402719588 ) ) ;
#8511=DIRECTION ( 'NONE',  ( -0.000000000000000000, -1.000000000000000000, 0.000000000000000000 ) ) ;
#8512=CARTESIAN_POINT ( 'NONE',  ( 0.06299212598430639631, -0.4881889763779528324, -0.5909884645248143498 ) ) ;
#8518=EDGE_LOOP ( 'NONE', ( #9871, #1494, #2025, #12646 ) ) ;
#8524=ADVANCED_FACE ( 'NONE', ( #2456 ), #34, .F. ) ;
#8532=CARTESIAN_POINT ( 'NONE',  ( -0.09842519685028340570, -0.4881889763779528324, -0.5870514566507987197 ) ) ;
#8535=EDGE_CURVE ( 'NONE', #8145, #12044, #10817, .T. ) ;
#8536=EDGE_LOOP ( 'NONE', ( #11978, #6643, #11776, #5214 ) ) ;
#8540=EDGE_CURVE ( 'NONE', #8021, #2098, #1154, .T. ) ;
#8547=PLANE ( 'NONE',  #347 ) ;
#8548=CARTESIAN_POINT ( 'NONE',  ( 0.1023622047244638067, -0.4881889763779528324, -0.2472069366676780122 ) ) ;
#8549=CARTESIAN_POINT ( 'NONE',  ( 0.09948011493088554369, -0.4921259842519685179, -0.2443248468740996937 ) ) ;
#8550=CARTESIAN_POINT ( 'NONE',  ( -0.1574803149606299191, -0.09448818897637796532, -0.5909884645248143498 ) ) ;
#8551=VERTEX_POINT ( 'NONE', #9750 ) ;
#8552=EDGE_CURVE ( 'NONE', #7182, #14789, #11653, .T. ) ;
#8553=EDGE_LOOP ( 'NONE', ( #9283, #10448, #302, #1221 ) ) ;
#8558=ADVANCED_FACE ( 'NONE', ( #8319 ), #7152, .F. ) ;
#8564=CARTESIAN_POINT ( 'NONE',  ( 0.4783464566929142014, -0.09842519685039370636, 0.3534565624369548908 ) ) ;
#8568=ADVANCED_FACE ( 'NONE', ( #4012 ), #11217, .T. ) ;
#8570=CARTESIAN_POINT ( 'NONE',  ( 1.976792077363838002E-17, -0.1023622047244094474, 0.1614173228346456879 ) ) ;
#8574=EDGE_LOOP ( 'NONE', ( #3830, #339, #13333 ) ) ;
#8580=CARTESIAN_POINT ( 'NONE',  ( -0.1028896637645180384, -0.4921259842519685179, -0.2462933508112025438 ) ) ;
#8583=CIRCLE ( 'NONE', #9586, 0.003937007874015724558 ) ;
#8584=AXIS2_PLACEMENT_3D ( 'NONE', #7167, #3325, #15403 ) ;
#8585=LINE ( 'NONE', #3810, #3150 ) ;
#8586=EDGE_CURVE ( 'NONE', #9204, #7731, #3389, .T. ) ;
#8590=CARTESIAN_POINT ( 'NONE',  ( 0.06692913385832209572, -0.4921259842519685179, -0.2377126739437404879 ) ) ;
#8592=AXIS2_PLACEMENT_3D ( 'NONE', #5728, #9576, #10524 ) ;
#8594=EDGE_LOOP ( 'NONE', ( #9427, #487 ) ) ;
#8596=ORIENTED_EDGE ( 'NONE', *, *, #5371, .T. ) ;
#8597=APPLICATION_CONTEXT ( 'automotive_design' ) ;
#8599=CIRCLE ( 'NONE', #3592, 0.003937007874015721089 ) ;
#8600=AXIS2_PLACEMENT_3D ( 'NONE', #9684, #3724, #13270 ) ;
#8601=DIRECTION ( 'NONE',  ( -1.000000000000000000, -0.000000000000000000, -3.973232667114495301E-16 ) ) ;
#8603=CIRCLE ( 'NONE', #8592, 0.003937007874015721089 ) ;
#8604=DIRECTION ( 'NONE',  ( 0.8660254037844387076, 0.000000000000000000, 0.4999999999999996669 ) ) ;
#8613=LINE ( 'NONE', #1497, #8712 ) ;
#8614=ORIENTED_EDGE ( 'NONE', *, *, #8535, .T. ) ;
#8621=CIRCLE ( 'NONE', #2856, 0.003937007874015742773 ) ;
#8622=CIRCLE ( 'NONE', #1375, 0.1574803149606299191 ) ;
#8623=CIRCLE ( 'NONE', #1876, 0.003937007874015724558 ) ;
#8628=VECTOR ( 'NONE', #7041, 39.37007874015748143 ) ;
#8638=AXIS2_PLACEMENT_3D ( 'NONE', #7526, #13941, #332 ) ;
#8640=EDGE_LOOP ( 'NONE', ( #3535, #10292, #531, #794 ) ) ;
#8642=ORIENTED_EDGE ( 'NONE', *, *, #3698, .T. ) ;
#8645=ORIENTED_EDGE ( 'NONE', *, *, #2241, .T. ) ;
#8646=DIRECTION ( 'NONE',  ( 0.8660254037844385966, 0.000000000000000000, -0.5000000000000000000 ) ) ;
#8647=LINE ( 'NONE', #7934, #12908 ) ;
#8652=CARTESIAN_POINT ( 'NONE',  ( -0.4803149606299220720, -0.4921259842519685179, 0.3500470136031578194 ) ) ;
#8655=AXIS2_PLACEMENT_3D ( 'NONE', #341, #2529, #2468 ) ;
#8657=DIRECTION ( 'NONE',  ( 0.000000000000000000, 0.000000000000000000, -1.000000000000000000 ) ) ;
#8658=DIRECTION ( 'NONE',  ( -0.000000000000000000, -1.000000000000000000, -0.000000000000000000 ) ) ;
#8662=ORIENTED_EDGE ( 'NONE', *, *, #6520, .T. ) ;
#8663=EDGE_CURVE ( 'NONE', #5876, #4883, #4890, .T. ) ;
#8664=ADVANCED_FACE ( 'NONE', ( #12764 ), #3935, .F. ) ;
#8665=EDGE_LOOP ( 'NONE', ( #13248, #9032, #2524, #4495 ) ) ;
#8667=VERTEX_POINT ( 'NONE', #14015 ) ;
#8668=AXIS2_PLACEMENT_3D ( 'NONE', #6443, #5426, #13568 ) ;
#8669=CARTESIAN_POINT ( 'NONE',  ( 0.3635801767928728556, -0.2952755905511811330, 0.2871962198427739921 ) ) ;
#8675=VECTOR ( 'NONE', #1284, 39.37007874015748143 ) ;
#8678=CARTESIAN_POINT ( 'NONE',  ( -0.1724006475077544398, -0.4881889763779528324, 0.1768186671464649640 ) ) ;
#8679=DIRECTION ( 'NONE',  ( 0.000000000000000000, 1.000000000000000000, 0.000000000000000000 ) ) ;
#8680=CIRCLE ( 'NONE', #6919, 0.03937007874015752140 ) ;
#8681=ORIENTED_EDGE ( 'NONE', *, *, #4986, .F. ) ;
#8682=EDGE_CURVE ( 'NONE', #13131, #13558, #15407, .T. ) ;
#8686=ORIENTED_EDGE ( 'NONE', *, *, #6520, .F. ) ;
#8687=ORIENTED_EDGE ( 'NONE', *, *, #5257, .T. ) ;
#8688=AXIS2_PLACEMENT_3D ( 'NONE', #12597, #13776, #3040 ) ;
#8690=EDGE_CURVE ( 'NONE', #13179, #11605, #8718, .T. ) ;
#8691=DIRECTION ( 'NONE',  ( -0.8660254037844341557, -0.000000000000000000, -0.5000000000000079936 ) ) ;
#8694=DIRECTION ( 'NONE',  ( -0.000000000000000000, 1.000000000000000000, 0.000000000000000000 ) ) ;
#8700=ORIENTED_EDGE ( 'NONE', *, *, #2530, .F. ) ;
#8702=AXIS2_PLACEMENT_3D ( 'NONE', #459, #1277, #2002 ) ;
#8703=EDGE_LOOP ( 'NONE', ( #3545, #13267 ) ) ;
#8704=ORIENTED_EDGE ( 'NONE', *, *, #77, .T. ) ;
#8707=EDGE_CURVE ( 'NONE', #13646, #2728, #6373, .T. ) ;
#8710=CARTESIAN_POINT ( 'NONE',  ( 0.4769054117961250561, -0.1023622047244094474, 0.3480785096661500599 ) ) ;
#8712=VECTOR ( 'NONE', #7216, 39.37007874015748143 ) ;
#8715=VERTEX_POINT ( 'NONE', #15106 ) ;
#8718=LINE ( 'NONE', #8786, #14149 ) ;
#8721=CIRCLE ( 'NONE', #2962, 0.003937007874015724558 ) ;
#8725=DIRECTION ( 'NONE',  ( -1.000000000000000000, -1.734723475976817507E-14, 0.000000000000000000 ) ) ;
#8732=DIRECTION ( 'NONE',  ( 0.000000000000000000, -0.000000000000000000, -1.000000000000000000 ) ) ;
#8733=EDGE_CURVE ( 'NONE', #5753, #1627, #10398, .T. ) ;
#8734=LINE ( 'NONE', #1757, #8346 ) ;
#8736=DIRECTION ( 'NONE',  ( -0.8660254037844388186, 0.000000000000000000, 0.4999999999999995559 ) ) ;
#8738=ORIENTED_EDGE ( 'NONE', *, *, #10367, .T. ) ;
#8739=VERTEX_POINT ( 'NONE', #12921 ) ;
#8740=EDGE_LOOP ( 'NONE', ( #2039, #2810, #6454, #2248 ) ) ;
#8742=EDGE_CURVE ( 'NONE', #3832, #11872, #7034, .T. ) ;
#8743=CARTESIAN_POINT ( 'NONE',  ( 0.2953892001169327042, -0.2952755905511811330, 0.2478261411026164707 ) ) ;
#8745=DIRECTION ( 'NONE',  ( -0.000000000000000000, 1.000000000000000000, 0.000000000000000000 ) ) ;
#8747=ADVANCED_FACE ( 'NONE', ( #9629 ), #8902, .T. ) ;
#8752=CARTESIAN_POINT ( 'NONE',  ( -0.06692913385815728311, -0.2952755905511811330, -0.4190977005962941426 ) ) ;
#8754=ORIENTED_EDGE ( 'NONE', *, *, #5196, .T. ) ;
#8756=VERTEX_POINT ( 'NONE', #14407 ) ;
#8757=EDGE_LOOP ( 'NONE', ( #11957, #4511, #12590, #14412 ) ) ;
#8761=CARTESIAN_POINT ( 'NONE',  ( 0.5615510810874363434, -0.09448818897637796532, 0.2014679098129276424 ) ) ;
#8762=DIRECTION ( 'NONE',  ( 0.000000000000000000, 0.000000000000000000, 1.000000000000000000 ) ) ;
#8770=CARTESIAN_POINT ( 'NONE',  ( -0.1743691514447623103, -0.4921259842519685179, 0.1734091183126679758 ) ) ;
#8773=DIRECTION ( 'NONE',  ( -0.8660254037844385966, -0.000000000000000000, -0.5000000000000000000 ) ) ;
#8775=EDGE_CURVE ( 'NONE', #7883, #9377, #10558, .T. ) ;
#8776=ORIENTED_EDGE ( 'NONE', *, *, #12488, .F. ) ;
#8785=DIRECTION ( 'NONE',  ( 0.000000000000000000, 0.000000000000000000, -1.000000000000000000 ) ) ;
#8786=CARTESIAN_POINT ( 'NONE',  ( 0.2652685895082805834, -0.1023622047244094474, 0.03495519865525829883 ) ) ;
#8789=FACE_OUTER_BOUND ( 'NONE', #321, .T. ) ;
#8790=ORIENTED_EDGE ( 'NONE', *, *, #9137, .T. ) ;
#8797=DIRECTION ( 'NONE',  ( 1.000000000000000000, -8.673617379884049672E-15, -0.000000000000000000 ) ) ;
#8798=FACE_OUTER_BOUND ( 'NONE', #10906, .T. ) ;
#8799=CARTESIAN_POINT ( 'NONE',  ( -0.4121618538092056139, -0.2952755905511811330, 0.1243101294532692330 ) ) ;
#8800=LINE ( 'NONE', #4968, #2325 ) ;
#8801=CYLINDRICAL_SURFACE ( 'NONE', #9136, 0.003937007874015758385 ) ;
#8805=EDGE_LOOP ( 'NONE', ( #11725, #8984, #15454, #8196 ) ) ;
#8807=ORIENTED_EDGE ( 'NONE', *, *, #13355, .F. ) ;
#8808=DIRECTION ( 'NONE',  ( -1.000000000000000000, 0.000000000000000000, 0.000000000000000000 ) ) ;
#8810=DIRECTION ( 'NONE',  ( 1.000000000000000000, -0.000000000000000000, -0.000000000000000000 ) ) ;
#8811=CARTESIAN_POINT ( 'NONE',  ( 0.1804058482825207921, -0.4881889763779528324, -0.1041573650692961123 ) ) ;
#8812=DIRECTION ( 'NONE',  ( 0.8660254037844390407, 0.000000000000000000, -0.4999999999999994449 ) ) ;
#8813=DIRECTION ( 'NONE',  ( 0.8660254037844385966, 0.000000000000000000, 0.5000000000000000000 ) ) ;
#8816=ADVANCED_FACE ( 'NONE', ( #4603 ), #15342, .T. ) ;
#8817=DIRECTION ( 'NONE',  ( -1.301042606982607687E-14, 0.000000000000000000, 1.000000000000000000 ) ) ;
#8818=DIRECTION ( 'NONE',  ( -0.8660254037844385966, 0.000000000000000000, -0.5000000000000000000 ) ) ;
#8821=ORIENTED_EDGE ( 'NONE', *, *, #13927, .T. ) ;
#8824=ORIENTED_EDGE ( 'NONE', *, *, #256, .T. ) ;
#8825=ADVANCED_FACE ( 'NONE', ( #14253 ), #14654, .T. ) ;
#8827=CARTESIAN_POINT ( 'NONE',  ( -0.03346456692913319514, -0.4881889763779528324, 0.05796233017454789638 ) ) ;
#8829=DIRECTION ( 'NONE',  ( -0.000000000000000000, 1.000000000000000000, -0.000000000000000000 ) ) ;
#8830=AXIS2_PLACEMENT_3D ( 'NONE', #8173, #11847, #9507 ) ;
#8832=CARTESIAN_POINT ( 'NONE',  ( -0.06299212598414161146, -0.4881889763779528324, -0.5909884645248154600 ) ) ;
#8836=AXIS2_PLACEMENT_3D ( 'NONE', #7811, #7741, #621 ) ;
#8837=CARTESIAN_POINT ( 'NONE',  ( -0.1724006475077544398, -0.4921259842519685179, 0.1728816592724491952 ) ) ;
#8841=ORIENTED_EDGE ( 'NONE', *, *, #10832, .F. ) ;
#8843=EDGE_CURVE ( 'NONE', #9186, #10277, #7887, .T. ) ;
#8844=DIRECTION ( 'NONE',  ( -0.000000000000000000, -1.000000000000000000, -0.000000000000000000 ) ) ;
#8845=CARTESIAN_POINT ( 'NONE',  ( -0.02952755905511744716, -0.09842519685039370636, 0.05114323250695388540 ) ) ;
#8846=EDGE_CURVE ( 'NONE', #4047, #13856, #5368, .T. ) ;
#8847=VERTEX_POINT ( 'NONE', #13147 ) ;
#8856=DIRECTION ( 'NONE',  ( -0.000000000000000000, -1.000000000000000000, -0.000000000000000000 ) ) ;
#8861=CARTESIAN_POINT ( 'NONE',  ( -0.6241293575972478580, -0.2952755905511811330, -0.3215685141414794113 ) ) ;
#8864=AXIS2_PLACEMENT_3D ( 'NONE', #8424, #11800, #12035 ) ;
#8866=DIRECTION ( 'NONE',  ( -1.000000000000000000, 0.000000000000000000, 0.000000000000000000 ) ) ;
#8872=ORIENTED_EDGE ( 'NONE', *, *, #235, .T. ) ;
#8874=AXIS2_PLACEMENT_3D ( 'NONE', #8974, #1820, #13747 ) ;
#8875=ORIENTED_EDGE ( 'NONE', *, *, #6594, .F. ) ;
#8876=AXIS2_PLACEMENT_3D ( 'NONE', #6395, #7806, #14733 ) ;
#8878=ORIENTED_EDGE ( 'NONE', *, *, #9246, .F. ) ;
#8880=DIRECTION ( 'NONE',  ( -1.504632769052536979E-28, 8.673617379884035472E-15, 1.000000000000000000 ) ) ;
#8881=FACE_OUTER_BOUND ( 'NONE', #14189, .T. ) ;
#8882=AXIS2_PLACEMENT_3D ( 'NONE', #8950, #7914, #3139 ) ;
#8885=CARTESIAN_POINT ( 'NONE',  ( -0.1062992125983150127, -0.1023622047244094474, -0.2482618547482104143 ) ) ;
#8888=CARTESIAN_POINT ( 'NONE',  ( 0.04921259842516965272, -0.4921259842519685179, -0.08523872084487793543 ) ) ;
#8890=CARTESIAN_POINT ( 'NONE',  ( -0.06692913385815726923, -0.2952755905511811330, -0.4584677793364516640 ) ) ;
#8891=DIRECTION ( 'NONE',  ( -0.5000000000000001110, 0.000000000000000000, 0.8660254037844388186 ) ) ;
#8893=VECTOR ( 'NONE', #8977, 39.37007874015748143 ) ;
#8894=AXIS2_PLACEMENT_3D ( 'NONE', #13038, #11421, #3417 ) ;
#8898=DIRECTION ( 'NONE',  ( -0.000000000000000000, 1.000000000000000000, -0.000000000000000000 ) ) ;
#8899=ORIENTED_EDGE ( 'NONE', *, *, #1959, .F. ) ;
#8902=TOROIDAL_SURFACE ( 'NONE', #8148, 0.1535433070866141780, 0.003937007874015747977 ) ;
#8903=CIRCLE ( 'NONE', #2148, 0.04330708661417330407 ) ;
#8907=CIRCLE ( 'NONE', #400, 0.003937007874015758385 ) ;
#8908=CARTESIAN_POINT ( 'NONE',  ( -0.5610236220472173407, -0.1023622047244094474, 0.2102555114175287954 ) ) ;
#8915=TOROIDAL_SURFACE ( 'NONE', #10163, 0.1535433070866141780, 0.003937007874015747977 ) ;
#8917=AXIS2_PLACEMENT_3D ( 'NONE', #537, #11329, #14874 ) ;
#8921=AXIS2_PLACEMENT_3D ( 'NONE', #10449, #10523, #11621 ) ;
#8922=EDGE_LOOP ( 'NONE', ( #11181, #10631, #13628, #10037 ) ) ;
#8923=EDGE_LOOP ( 'NONE', ( #8878, #14619, #5844, #610 ) ) ;
#8930=EDGE_CURVE ( 'NONE', #5518, #10807, #6633, .T. ) ;
#8931=DIRECTION ( 'NONE',  ( -1.734723475976802677E-14, 0.000000000000000000, -1.000000000000000000 ) ) ;
#8935=AXIS2_PLACEMENT_3D ( 'NONE', #4541, #14100, #10503 ) ;
#8937=ORIENTED_EDGE ( 'NONE', *, *, #6166, .T. ) ;
#8938=CARTESIAN_POINT ( 'NONE',  ( -0.4121618538092055584, -0.2952755905511811330, 0.1243101294532693024 ) ) ;
#8941=ORIENTED_EDGE ( 'NONE', *, *, #13596, .T. ) ;
#8943=AXIS2_PLACEMENT_3D ( 'NONE', #13031, #2293, #7068 ) ;
#8944=ORIENTED_EDGE ( 'NONE', *, *, #5272, .F. ) ;
#8950=CARTESIAN_POINT ( 'NONE',  ( 0.4339188594849086034, -0.2952755905511811330, 0.1732400634307316167 ) ) ;
#8951=DIRECTION ( 'NONE',  ( 0.000000000000000000, 1.000000000000000000, 0.000000000000000000 ) ) ;
#8953=VECTOR ( 'NONE', #6397, 39.37007874015748143 ) ;
#8956=CARTESIAN_POINT ( 'NONE',  ( 0.3964138223131414840, -0.2952755905511811330, 0.1515865201236449578 ) ) ;
#8959=AXIS2_PLACEMENT_3D ( 'NONE', #14585, #3851, #7458 ) ;
#8961=DIRECTION ( 'NONE',  ( 0.8660254037844390407, 0.000000000000000000, -0.4999999999999995004 ) ) ;
#8962=ORIENTED_EDGE ( 'NONE', *, *, #3769, .F. ) ;
#8963=ORIENTED_EDGE ( 'NONE', *, *, #1999, .F. ) ;
#8968=AXIS2_PLACEMENT_3D ( 'NONE', #3229, #8159, #5712 ) ;
#8974=CARTESIAN_POINT ( 'NONE',  ( -0.09842519685028335019, -0.2952755905511811330, -0.4190977005962941981 ) ) ;
#8977=DIRECTION ( 'NONE',  ( 1.000000000000000000, -0.000000000000000000, -0.000000000000000000 ) ) ;
#8982=EDGE_CURVE ( 'NONE', #13984, #4499, #2784, .T. ) ;
#8983=ORIENTED_EDGE ( 'NONE', *, *, #8733, .T. ) ;
#8984=ORIENTED_EDGE ( 'NONE', *, *, #10746, .T. ) ;
#8989=CARTESIAN_POINT ( 'NONE',  ( -0.1724006475077544953, -0.4881889763779528324, 0.1768186671464649640 ) ) ;
#8992=FACE_OUTER_BOUND ( 'NONE', #14526, .T. ) ;
#8993=ORIENTED_EDGE ( 'NONE', *, *, #3290, .T. ) ;
#9007=DIRECTION ( 'NONE',  ( 1.445602896647339903E-16, 0.000000000000000000, -1.000000000000000000 ) ) ;
#9013=EDGE_LOOP ( 'NONE', ( #3801, #1691, #5120, #9680 ) ) ;
#9016=EDGE_CURVE ( 'NONE', #11032, #5098, #10653, .T. ) ;
#9018=CARTESIAN_POINT ( 'NONE',  ( 0.5860051159906326523, -0.09448818897637796532, 0.1591122789105293422 ) ) ;
#9019=DIRECTION ( 'NONE',  ( -0.8660254037844397068, -0.000000000000000000, -0.4999999999999980571 ) ) ;
#9028=EDGE_CURVE ( 'NONE', #14809, #3677, #6069, .T. ) ;
#9032=ORIENTED_EDGE ( 'NONE', *, *, #8682, .T. ) ;
#9036=DIRECTION ( 'NONE',  ( 0.000000000000000000, 0.000000000000000000, -1.000000000000000000 ) ) ;
#9038=PRODUCT_CONTEXT ( 'NONE', #8597, 'mechanical' ) ;
#9039=DIRECTION ( 'NONE',  ( -1.000000000000000000, 0.000000000000000000, 0.000000000000000000 ) ) ;
#9041=CARTESIAN_POINT ( 'NONE',  ( -0.06299212598414161146, -0.1023622047244094474, -0.5870514566507987197 ) ) ;
#9043=DIRECTION ( 'NONE',  ( 0.000000000000000000, 0.000000000000000000, -1.000000000000000000 ) ) ;
#9045=ADVANCED_FACE ( 'NONE', ( #8992 ), #824, .F. ) ;
#9047=EDGE_CURVE ( 'NONE', #14387, #15025, #5449, .T. ) ;
#9056=CARTESIAN_POINT ( 'NONE',  ( 0.000000000000000000, 5.629100846319917971E-17, -0.1614173228346456879 ) ) ;
#9059=CARTESIAN_POINT ( 'NONE',  ( -0.09842519685028340570, -0.09842519685039370636, -0.5909884645248143498 ) ) ;
#9061=VERTEX_POINT ( 'NONE', #13830 ) ;
#9063=ORIENTED_EDGE ( 'NONE', *, *, #13355, .T. ) ;
#9066=CARTESIAN_POINT ( 'NONE',  ( -0.1629063847838169987, -0.1023622047244094474, 0.2161887458866224576 ) ) ;
#9069=DIRECTION ( 'NONE',  ( -1.000000000000000000, -0.000000000000000000, -3.476578583725179813E-16 ) ) ;
#9072=CARTESIAN_POINT ( 'NONE',  ( -0.5860051159906336515, 0.000000000000000000, 0.1591122789105256508 ) ) ;
#9075=ORIENTED_EDGE ( 'NONE', *, *, #750, .F. ) ;
#9077=ORIENTED_EDGE ( 'NONE', *, *, #5318, .F. ) ;
#9079=ORIENTED_EDGE ( 'NONE', *, *, #6701, .T. ) ;
#9080=UNCERTAINTY_MEASURE_WITH_UNIT (LENGTH_MEASURE( 1.000000000000000082E-05 ), #10155, 'distance_accuracy_value', 'NONE');
#9083=DIRECTION ( 'NONE',  ( -3.476578583725179813E-16, -0.000000000000000000, 1.000000000000000000 ) ) ;
#9084=AXIS2_PLACEMENT_3D ( 'NONE', #14486, #13292, #7417 ) ;
#9086=CARTESIAN_POINT ( 'NONE',  ( -0.4121618538092056139, -0.2952755905511811330, 0.1243101294532692330 ) ) ;
#9089=DIRECTION ( 'NONE',  ( 0.000000000000000000, 0.000000000000000000, -1.000000000000000000 ) ) ;
#9090=CARTESIAN_POINT ( 'NONE',  ( 0.000000000000000000, -0.4921259842519685179, 0.000000000000000000 ) ) ;
#9091=EDGE_LOOP ( 'NONE', ( #111, #635 ) ) ;
#9092=CARTESIAN_POINT ( 'NONE',  ( 0.06692913385832206796, -0.4921259842519685179, 9.675294977568793108E-18 ) ) ;
#9096=DIRECTION ( 'NONE',  ( 0.5000000000000134337, 0.000000000000000000, -0.8660254037844308250 ) ) ;
#9099=CARTESIAN_POINT ( 'NONE',  ( -0.5418660417173573052, -0.1023622047244094474, 0.2355633981508970798 ) ) ;
#9101=ORIENTED_EDGE ( 'NONE', *, *, #13171, .F. ) ;
#9102=ORIENTED_EDGE ( 'NONE', *, *, #8442, .T. ) ;
#9103=ORIENTED_EDGE ( 'NONE', *, *, #8119, .F. ) ;
#9104=DIRECTION ( 'NONE',  ( -0.8660254037844385966, 0.000000000000000000, -0.5000000000000001110 ) ) ;
#9106=AXIS2_PLACEMENT_3D ( 'NONE', #7719, #2775, #11308 ) ;
#9109=AXIS2_PLACEMENT_3D ( 'NONE', #6355, #8797, #12263 ) ;
#9110=CARTESIAN_POINT ( 'NONE',  ( -0.1618514667033796040, -0.4921259842519685179, 0.2161887458866224576 ) ) ;
#9111=DIRECTION ( 'NONE',  ( -0.8660254037844398178, 0.000000000000000000, 0.4999999999999979461 ) ) ;
#9112=CIRCLE ( 'NONE', #7850, 0.1574803149606299191 ) ;
#9115=EDGE_CURVE ( 'NONE', #1223, #7284, #13692, .T. ) ;
#9119=MANIFOLD_SOLID_BREP ( 'Fillet1', #3375 ) ;
#9120=CARTESIAN_POINT ( 'NONE',  ( 0.3944453183761336135, -0.2952755905511811330, 0.1549960689574419737 ) ) ;
#9124=AXIS2_PLACEMENT_3D ( 'NONE', #767, #3121, #12758 ) ;
#9128=VECTOR ( 'NONE', #7120, 39.37007874015748143 ) ;
#9130=ORIENTED_EDGE ( 'NONE', *, *, #708, .F. ) ;
#9132=EDGE_LOOP ( 'NONE', ( #9063, #10058, #4924, #9994, #10227 ) ) ;
#9133=ADVANCED_FACE ( 'NONE', ( #2307 ), #6852, .T. ) ;
#9135=FACE_OUTER_BOUND ( 'NONE', #7925, .T. ) ;
#9136=AXIS2_PLACEMENT_3D ( 'NONE', #7856, #3080, #5429 ) ;
#9137=EDGE_CURVE ( 'NONE', #12044, #10896, #4903, .T. ) ;
#9138=DIRECTION ( 'NONE',  ( 0.000000000000000000, 0.000000000000000000, -1.000000000000000000 ) ) ;
#9139=CIRCLE ( 'NONE', #2375, 0.003937007874015750579 ) ;
#9141=AXIS2_PLACEMENT_3D ( 'NONE', #4821, #12211, #8443 ) ;
#9144=DIRECTION ( 'NONE',  ( 0.000000000000000000, -1.000000000000000000, -0.000000000000000000 ) ) ;
#9146=EDGE_LOOP ( 'NONE', ( #12540, #7092 ) ) ;
#9147=ORIENTED_EDGE ( 'NONE', *, *, #10888, .T. ) ;
#9148=ORIENTED_EDGE ( 'NONE', *, *, #2177, .T. ) ;
#9150=ORIENTED_EDGE ( 'NONE', *, *, #79, .F. ) ;
#9151=CIRCLE ( 'NONE', #658, 0.03937007874015750752 ) ;
#9154=DIRECTION ( 'NONE',  ( -0.8660254037844383745, 0.000000000000000000, -0.5000000000000002220 ) ) ;
#9156=AXIS2_PLACEMENT_3D ( 'NONE', #13337, #5025, #6436 ) ;
#9161=VERTEX_POINT ( 'NONE', #4584 ) ;
#9163=ADVANCED_FACE ( 'NONE', ( #14156 ), #4677, .T. ) ;
#9164=DIRECTION ( 'NONE',  ( 1.000000000000000000, 0.000000000000000000, 3.614007241618343347E-16 ) ) ;
#9169=EDGE_CURVE ( 'NONE', #13646, #2681, #5383, .T. ) ;
#9176=PLANE ( 'NONE',  #2632 ) ;
#9178=CARTESIAN_POINT ( 'NONE',  ( 0.1618514667033794374, -0.4881889763779528324, 0.2083147301385909200 ) ) ;
#9179=DIRECTION ( 'NONE',  ( 0.000000000000000000, 0.000000000000000000, -1.000000000000000000 ) ) ;
#9181=CARTESIAN_POINT ( 'NONE',  ( 0.06351958502452506594, -0.4881889763779528324, -0.2357441700067326729 ) ) ;
#9183=ORIENTED_EDGE ( 'NONE', *, *, #14959, .F. ) ;
#9186=VERTEX_POINT ( 'NONE', #3503 ) ;
#9188=ORIENTED_EDGE ( 'NONE', *, *, #3366, .T. ) ;
#9189=ORIENTED_EDGE ( 'NONE', *, *, #1367, .T. ) ;
#9190=DIRECTION ( 'NONE',  ( -0.8660254037844398178, 0.000000000000000000, 0.4999999999999979461 ) ) ;
#9192=FACE_OUTER_BOUND ( 'NONE', #6181, .T. ) ;
#9193=CARTESIAN_POINT ( 'NONE',  ( -0.4749369078591176851, -0.4881889763779528324, 0.3514880584999471314 ) ) ;
#9195=FACE_OUTER_BOUND ( 'NONE', #12768, .T. ) ;
#9198=EDGE_LOOP ( 'NONE', ( #2290, #13861, #2064, #4718 ) ) ;
#9204=VERTEX_POINT ( 'NONE', #10706 ) ;
#9205=AXIS2_PLACEMENT_3D ( 'NONE', #12390, #14752, #13549 ) ;
#9208=DIRECTION ( 'NONE',  ( -0.8660254037844385966, 0.000000000000000000, -0.5000000000000001110 ) ) ;
#9209=EDGE_LOOP ( 'NONE', ( #10869, #2708, #3554, #6341 ) ) ;
#9210=AXIS2_PLACEMENT_3D ( 'NONE', #4563, #9350, #8185 ) ;
#9212=VERTEX_POINT ( 'NONE', #9536 ) ;
#9220=AXIS2_PLACEMENT_3D ( 'NONE', #14622, #2483, #14477 ) ;
#9221=DIRECTION ( 'NONE',  ( 1.000000000000000000, 0.000000000000000000, -1.224646799147353207E-16 ) ) ;
#9222=DIRECTION ( 'NONE',  ( -1.000000000000000000, 0.000000000000000000, -0.000000000000000000 ) ) ;
#9227=VECTOR ( 'NONE', #12459, 39.37007874015748143 ) ;
#9228=VERTEX_POINT ( 'NONE', #9832 ) ;
#9229=ADVANCED_FACE ( 'NONE', ( #136 ), #9601, .T. ) ;
#9233=CARTESIAN_POINT ( 'NONE',  ( -0.1023622047242991467, -0.4881889763779528324, -0.5909884645248143498 ) ) ;
#9235=DIRECTION ( 'NONE',  ( 0.000000000000000000, 0.000000000000000000, -1.000000000000000000 ) ) ;
#9237=CARTESIAN_POINT ( 'NONE',  ( -0.4822834645669303311, -0.09448818897637796532, 0.3466374647693610811 ) ) ;
#9241=ORIENTED_EDGE ( 'NONE', *, *, #13719, .F. ) ;
#9242=ORIENTED_EDGE ( 'NONE', *, *, #4575, .T. ) ;
#9244=ORIENTED_EDGE ( 'NONE', *, *, #7804, .T. ) ;
#9245=DIRECTION ( 'NONE',  ( 0.4999999999999998335, -0.000000000000000000, 0.8660254037844388186 ) ) ;
#9246=EDGE_CURVE ( 'NONE', #14775, #11240, #3656, .T. ) ;
#9247=CARTESIAN_POINT ( 'NONE',  ( -0.1531294576120625639, -0.4881889763779528324, -0.08840933357318579711 ) ) ;
#9252=ORIENTED_EDGE ( 'NONE', *, *, #5257, .F. ) ;
#9254=EDGE_CURVE ( 'NONE', #3213, #13283, #7910, .T. ) ;
#9255=LINE ( 'NONE', #6656, #14110 ) ;
#9256=DIRECTION ( 'NONE',  ( 0.8660254037844491437, 0.000000000000000000, 0.4999999999999815148 ) ) ;
#9257=DIRECTION ( 'NONE',  ( -0.000000000000000000, 1.000000000000000000, 0.000000000000000000 ) ) ;
#9258=EDGE_LOOP ( 'NONE', ( #3908, #13401, #12223, #14316 ) ) ;
#9261=VERTEX_POINT ( 'NONE', #1460 ) ;
#9263=EDGE_CURVE ( 'NONE', #6899, #4570, #4410, .T. ) ;
#9264=DIRECTION ( 'NONE',  ( -0.8660254037844395958, 0.000000000000000000, 0.4999999999999986122 ) ) ;
#9268=CARTESIAN_POINT ( 'NONE',  ( -0.09842519685028340570, -0.4881889763779528324, -0.5870514566507987197 ) ) ;
#9269=DIRECTION ( 'NONE',  ( -3.942553354492736135E-16, 0.000000000000000000, 1.000000000000000000 ) ) ;
#9270=EDGE_CURVE ( 'NONE', #10323, #3491, #2917, .T. ) ;
#9271=VERTEX_POINT ( 'NONE', #12267 ) ;
#9272=CARTESIAN_POINT ( 'NONE',  ( -0.1618514667033796040, -0.4881889763779528324, 0.2161887458866224576 ) ) ;
#9278=ORIENTED_EDGE ( 'NONE', *, *, #10742, .F. ) ;
#9283=ORIENTED_EDGE ( 'NONE', *, *, #9520, .T. ) ;
#9285=CARTESIAN_POINT ( 'NONE',  ( 0.2359202325322792559, -0.1023622047244094474, 0.06286251073447048088 ) ) ;
#9292=( CONVERSION_BASED_UNIT ( 'INCH', #12984 ) LENGTH_UNIT ( ) NAMED_UNIT ( #72 ) );
#9293=EDGE_LOOP ( 'NONE', ( #4940, #4291, #15179, #13422 ) ) ;
#9301=ADVANCED_FACE ( 'NONE', ( #14700 ), #10928, .T. ) ;
#9303=PLANE ( 'NONE',  #3395 ) ;
#9305=CYLINDRICAL_SURFACE ( 'NONE', #637, 0.003937007874015721089 ) ;
#9307=EDGE_LOOP ( 'NONE', ( #13820, #8821, #10397, #8045 ) ) ;
#9308=DIRECTION ( 'NONE',  ( 0.000000000000000000, 0.000000000000000000, -1.000000000000000000 ) ) ;
#9309=CARTESIAN_POINT ( 'NONE',  ( 0.1540707661268329032, 0.000000000000000000, -0.5890199605878065903 ) ) ;
#9313=EDGE_LOOP ( 'NONE', ( #9102, #3208, #5199, #11024 ) ) ;
#9314=ORIENTED_EDGE ( 'NONE', *, *, #14807, .F. ) ;
#9316=EDGE_CURVE ( 'NONE', #11599, #13144, #10670, .T. ) ;
#9317=CARTESIAN_POINT ( 'NONE',  ( 1.976792077363838002E-17, -0.09842519685039370636, 0.1614173228346456879 ) ) ;
#9319=CARTESIAN_POINT ( 'NONE',  ( 0.1062992125984796032, -0.4881889763779528324, -0.2482618547481154347 ) ) ;
#9324=CARTESIAN_POINT ( 'NONE',  ( 0.4552518684890383138, -0.1023622047244094474, 0.3855835468379170128 ) ) ;
#9326=DIRECTION ( 'NONE',  ( 0.000000000000000000, -8.673617379884032317E-15, 1.000000000000000000 ) ) ;
#9329=CYLINDRICAL_SURFACE ( 'NONE', #1690, 0.1574803149606299191 ) ;
#9330=VECTOR ( 'NONE', #9706, 39.37007874015748143 ) ;
#9333=ORIENTED_EDGE ( 'NONE', *, *, #277, .F. ) ;
#9335=ORIENTED_EDGE ( 'NONE', *, *, #2623, .T. ) ;
#9336=CARTESIAN_POINT ( 'NONE',  ( 0.1552072824047652788, 0.000000000000000000, -0.5870514566507987197 ) ) ;
#9337=DIRECTION ( 'NONE',  ( 4.336808689942014285E-16, 0.000000000000000000, -1.000000000000000000 ) ) ;
#9338=DIRECTION ( 'NONE',  ( 1.000000000000000000, -0.000000000000000000, -0.000000000000000000 ) ) ;
#9342=VECTOR ( 'NONE', #14509, 39.37007874015748143 ) ;
#9343=AXIS2_PLACEMENT_3D ( 'NONE', #14715, #6463, #8812 ) ;
#9344=CARTESIAN_POINT ( 'NONE',  ( -0.4330708661417336236, -0.09842519685039370636, 0.4318761856142863120 ) ) ;
#9345=ORIENTED_EDGE ( 'NONE', *, *, #8407, .T. ) ;
#9349=LINE ( 'NONE', #11622, #7873 ) ;
#9350=DIRECTION ( 'NONE',  ( -1.000000000000000000, -0.000000000000000000, -0.000000000000000000 ) ) ;
#9351=DIRECTION ( 'NONE',  ( -0.8660254037844387076, 0.000000000000000000, -0.4999999999999998890 ) ) ;
#9352=EDGE_CURVE ( 'NONE', #13856, #12057, #1380, .T. ) ;
#9353=ORIENTED_EDGE ( 'NONE', *, *, #15367, .T. ) ;
#9362=EDGE_LOOP ( 'NONE', ( #9609, #5972, #10794, #7514 ) ) ;
#9365=DIRECTION ( 'NONE',  ( -0.5000000000000035527, -0.000000000000000000, 0.8660254037844365982 ) ) ;
#9366=DIRECTION ( 'NONE',  ( 0.8660254037844384856, 0.000000000000000000, 0.5000000000000003331 ) ) ;
#9368=DIRECTION ( 'NONE',  ( 0.000000000000000000, -1.000000000000000000, 0.000000000000000000 ) ) ;
#9369=CARTESIAN_POINT ( 'NONE',  ( -0.2393297813659119588, -0.1023622047244094474, 0.06089400679736759608 ) ) ;
#9371=CIRCLE ( 'NONE', #4102, 0.003937007874015721089 ) ;
#9372=VECTOR ( 'NONE', #2475, 39.37007874015748143 ) ;
#9373=DIRECTION ( 'NONE',  ( -1.000000000000000000, 0.000000000000000000, 0.000000000000000000 ) ) ;
#9374=CARTESIAN_POINT ( 'NONE',  ( 0.000000000000000000, -0.09842519685039370636, 0.000000000000000000 ) ) ;
#9375=AXIS2_PLACEMENT_3D ( 'NONE', #14267, #5782, #8387 ) ;
#9376=AXIS2_PLACEMENT_3D ( 'NONE', #5109, #6043, #8498 ) ;
#9377=VERTEX_POINT ( 'NONE', #5260 ) ;
#9381=ORIENTED_EDGE ( 'NONE', *, *, #3001, .F. ) ;
#9384=AXIS2_PLACEMENT_3D ( 'NONE', #3038, #12361, #6540 ) ;
#9388=CIRCLE ( 'NONE', #13632, 0.003937007874015750579 ) ;
#9391=DIRECTION ( 'NONE',  ( -0.8660254037844389297, 0.000000000000000000, 0.4999999999999996114 ) ) ;
#9392=DIRECTION ( 'NONE',  ( -1.000000000000000000, -0.000000000000000000, -3.973232667114495301E-16 ) ) ;
#9393=VERTEX_POINT ( 'NONE', #7778 ) ;
#9394=CARTESIAN_POINT ( 'NONE',  ( 0.09842519685044820443, -0.1023622047244094474, -0.5870514566507987197 ) ) ;
#9395=PLANE ( 'NONE',  #5057 ) ;
#9396=DIRECTION ( 'NONE',  ( 0.000000000000000000, 0.000000000000000000, -1.000000000000000000 ) ) ;
#9397=TOROIDAL_SURFACE ( 'NONE', #15151, 0.04330708661417328326, 0.003937007874015747977 ) ;
#9398=AXIS2_PLACEMENT_3D ( 'NONE', #4765, #9548, #8361 ) ;
#9399=VECTOR ( 'NONE', #6008, 39.37007874015748143 ) ;
#9400=ORIENTED_EDGE ( 'NONE', *, *, #14062, .F. ) ;
#9409=ADVANCED_FACE ( 'NONE', ( #13751 ), #12737, .T. ) ;
#9410=DIRECTION ( 'NONE',  ( 1.000000000000000000, 0.000000000000000000, 3.075191616504340279E-15 ) ) ;
#9413=AXIS2_PLACEMENT_3D ( 'NONE', #2485, #14545, #14401 ) ;
#9415=VERTEX_POINT ( 'NONE', #12422 ) ;
#9418=CARTESIAN_POINT ( 'NONE',  ( -0.3137366569588388998, -0.2952755905511811330, 0.2947875711430708590 ) ) ;
#9419=CARTESIAN_POINT ( 'NONE',  ( -0.2681506793016945611, -0.4881889763779528324, 0.03207310886158504931 ) ) ;
#9420=CARTESIAN_POINT ( 'NONE',  ( -0.2373612774289040883, -0.4881889763779528324, 0.06430355563116459117 ) ) ;
#9421=ORIENTED_EDGE ( 'NONE', *, *, #256, .F. ) ;
#9424=VECTOR ( 'NONE', #577, 39.37007874015748854 ) ;
#9427=ORIENTED_EDGE ( 'NONE', *, *, #2802, .T. ) ;
#9429=EDGE_CURVE ( 'NONE', #9678, #5876, #1921, .T. ) ;
#9430=PRODUCT_DEFINITION_SHAPE ( 'NONE', 'NONE',  #9773 ) ;
#9437=DIRECTION ( 'NONE',  ( -0.5000000000000008882, 0.000000000000000000, 0.8660254037844380415 ) ) ;
#9438=AXIS2_PLACEMENT_3D ( 'NONE', #13557, #6340, #5245 ) ;
#9439=CARTESIAN_POINT ( 'NONE',  ( -0.06299212598414166697, -0.2952755905511811330, -0.4190977005962941426 ) ) ;
#9441=CARTESIAN_POINT ( 'NONE',  ( -0.06299212598414161146, -0.4881889763779528324, -0.5870514566507987197 ) ) ;
#9444=CARTESIAN_POINT ( 'NONE',  ( -0.4552518684890389244, -0.1023622047244094474, 0.3855835468379172903 ) ) ;
#9446=VERTEX_POINT ( 'NONE', #6755 ) ;
#9447=DIRECTION ( 'NONE',  ( 0.000000000000000000, 0.000000000000000000, -1.000000000000000000 ) ) ;
#9448=VERTEX_POINT ( 'NONE', #674 ) ;
#9449=VECTOR ( 'NONE', #13329, 39.37007874015748143 ) ;
#9450=EDGE_CURVE ( 'NONE', #5709, #11465, #11394, .T. ) ;
#9452=EDGE_LOOP ( 'NONE', ( #11178, #9697, #15274, #6552 ) ) ;
#9453=CARTESIAN_POINT ( 'NONE',  ( 0.06692913385832215123, -0.4881889763779528324, -0.5870514566507987197 ) ) ;
#9455=EDGE_CURVE ( 'NONE', #15013, #4047, #6515, .T. ) ;
#9462=DIRECTION ( 'NONE',  ( 0.000000000000000000, -1.000000000000000000, 0.000000000000000000 ) ) ;
#9465=CARTESIAN_POINT ( 'NONE',  ( -0.5084014747882513729, -0.09842519685039370636, 0.2935257283253980276 ) ) ;
#9466=CARTESIAN_POINT ( 'NONE',  ( 0.3706061991976989933, -0.003937007874015747977, -0.2139695888701345361 ) ) ;
#9467=VECTOR ( 'NONE', #650, 39.37007874015748143 ) ;
#9474=CIRCLE ( 'NONE', #5446, 0.003937007874015724558 ) ;
#9476=CARTESIAN_POINT ( 'NONE',  ( -0.4606299212598433113, -0.4881889763779528324, 0.3841425019411278674 ) ) ;
#9478=DIRECTION ( 'NONE',  ( -0.8660254037844385966, 0.000000000000000000, -0.5000000000000001110 ) ) ;
#9479=ORIENTED_EDGE ( 'NONE', *, *, #8348, .T. ) ;
#9482=DIRECTION ( 'NONE',  ( 0.000000000000000000, -1.000000000000000000, 0.000000000000000000 ) ) ;
#9484=CIRCLE ( 'NONE', #7712, 0.007874015748031499423 ) ;
#9485=ORIENTED_EDGE ( 'NONE', *, *, #5266, .T. ) ;
#9488=ORIENTED_EDGE ( 'NONE', *, *, #923, .F. ) ;
#9490=DIRECTION ( 'NONE',  ( -0.8660254037844385966, -0.000000000000000000, -0.5000000000000001110 ) ) ;
#9498=DIRECTION ( 'NONE',  ( -0.4999999999999998335, -0.000000000000000000, -0.8660254037844388186 ) ) ;
#9500=CARTESIAN_POINT ( 'NONE',  ( 0.2742631158500650201, -0.2952755905511811330, 0.2765435766697818543 ) ) ;
#9502=ORIENTED_EDGE ( 'NONE', *, *, #714, .T. ) ;
#9504=VERTEX_POINT ( 'NONE', #14772 ) ;
#9505=ORIENTED_EDGE ( 'NONE', *, *, #7324, .F. ) ;
#9506=CARTESIAN_POINT ( 'NONE',  ( 0.1552072824047652788, -0.09448818897637796532, -0.5870514566507987197 ) ) ;
#9507=DIRECTION ( 'NONE',  ( 0.8660254037844427044, 0.000000000000000000, 0.4999999999999928946 ) ) ;
#9511=DIRECTION ( 'NONE',  ( -0.000000000000000000, -1.000000000000000000, -0.000000000000000000 ) ) ;
#9512=CARTESIAN_POINT ( 'NONE',  ( 0.1062992125984795477, -0.1023622047244094474, -0.2482618547481155458 ) ) ;
#9514=DIRECTION ( 'NONE',  ( 0.000000000000000000, 0.000000000000000000, 1.000000000000000000 ) ) ;
#9516=CARTESIAN_POINT ( 'NONE',  ( -0.04921259842516954863, -0.4921259842519685179, -0.08523872084487790768 ) ) ;
#9519=EDGE_LOOP ( 'NONE', ( #4906, #3254, #11323, #2688 ) ) ;
#9520=EDGE_CURVE ( 'NONE', #13891, #1499, #4163, .T. ) ;
#9527=CARTESIAN_POINT ( 'NONE',  ( 0.4307978335858662633, -0.09842519685039370636, 0.4279391777402732910 ) ) ;
#9529=CARTESIAN_POINT ( 'NONE',  ( -0.2647411304678976007, -0.1023622047244094474, 0.03404161279859290595 ) ) ;
#9530=EDGE_CURVE ( 'NONE', #9415, #5934, #12927, .T. ) ;
#9531=DIRECTION ( 'NONE',  ( -0.8660254037844388186, 0.000000000000000000, 0.4999999999999995559 ) ) ;
#9534=EDGE_CURVE ( 'NONE', #10930, #2979, #6828, .T. ) ;
#9536=CARTESIAN_POINT ( 'NONE',  ( 0.1023622047244638067, -0.1023622047244094474, -0.2482618547481154347 ) ) ;
#9537=EDGE_LOOP ( 'NONE', ( #2007, #7861, #248, #1090 ) ) ;
#9538=EDGE_CURVE ( 'NONE', #9186, #12219, #15426, .T. ) ;
#9539=EDGE_LOOP ( 'NONE', ( #8645, #7968, #140, #12801 ) ) ;
#9540=VERTEX_POINT ( 'NONE', #5893 ) ;
#9548=DIRECTION ( 'NONE',  ( 0.8660254037844400399, -2.152835902228474590E-14, -0.4999999999999977240 ) ) ;
#9552=ORIENTED_EDGE ( 'NONE', *, *, #9254, .F. ) ;
#9553=EDGE_CURVE ( 'NONE', #11698, #2979, #11934, .T. ) ;
#9554=CARTESIAN_POINT ( 'NONE',  ( 0.3964138223131414840, -0.2952755905511811330, 0.1515865201236449578 ) ) ;
#9555=ADVANCED_FACE ( 'NONE', ( #2372 ), #12962, .T. ) ;
#9562=ORIENTED_EDGE ( 'NONE', *, *, #5981, .F. ) ;
#9564=FACE_OUTER_BOUND ( 'NONE', #10510, .T. ) ;
#9565=DIRECTION ( 'NONE',  ( 0.000000000000000000, 1.000000000000000000, 0.000000000000000000 ) ) ;
#9567=ORIENTED_EDGE ( 'NONE', *, *, #11420, .F. ) ;
#9569=DIRECTION ( 'NONE',  ( 0.000000000000000000, 0.000000000000000000, -1.000000000000000000 ) ) ;
#9570=FACE_OUTER_BOUND ( 'NONE', #3066, .T. ) ;
#9571=DIRECTION ( 'NONE',  ( -0.000000000000000000, -0.000000000000000000, 1.000000000000000000 ) ) ;
#9576=DIRECTION ( 'NONE',  ( 0.5000000000000004441, 8.673617379884095425E-15, -0.8660254037844384856 ) ) ;
#9580=ORIENTED_EDGE ( 'NONE', *, *, #5506, .F. ) ;
#9584=EDGE_CURVE ( 'NONE', #12009, #12255, #2228, .T. ) ;
#9585=DIRECTION ( 'NONE',  ( -1.000000000000000000, -0.000000000000000000, -0.000000000000000000 ) ) ;
#9586=AXIS2_PLACEMENT_3D ( 'NONE', #10747, #26, #9569 ) ;
#9592=CIRCLE ( 'NONE', #13086, 0.003937007874015741038 ) ;
#9594=CARTESIAN_POINT ( 'NONE',  ( -0.2642136714276788201, -0.4881889763779528324, 0.03889220652917903254 ) ) ;
#9595=DIRECTION ( 'NONE',  ( 0.4999999999999979461, 0.000000000000000000, 0.8660254037844398178 ) ) ;
#9596=CARTESIAN_POINT ( 'NONE',  ( 0.000000000000000000, -0.09842519685039370636, 0.000000000000000000 ) ) ;
#9597=EDGE_CURVE ( 'NONE', #11994, #7766, #5157, .T. ) ;
#9599=DIRECTION ( 'NONE',  ( 0.5000000000000172085, 0.000000000000000000, -0.8660254037844286046 ) ) ;
#9601=CYLINDRICAL_SURFACE ( 'NONE', #12672, 0.003937007874015740171 ) ;
#9604=ORIENTED_EDGE ( 'NONE', *, *, #12386, .F. ) ;
#9605=CIRCLE ( 'NONE', #12853, 0.003937007874015758385 ) ;
#9609=ORIENTED_EDGE ( 'NONE', *, *, #79, .T. ) ;
#9611=EDGE_CURVE ( 'NONE', #4717, #15072, #431, .T. ) ;
#9617=CARTESIAN_POINT ( 'NONE',  ( 0.06692913385832209572, -0.4881889763779528324, -0.2377126739437405434 ) ) ;
#9620=DIRECTION ( 'NONE',  ( -0.4999999999999981681, 0.000000000000000000, -0.8660254037844397068 ) ) ;
#9621=CIRCLE ( 'NONE', #14873, 0.003937007874015741038 ) ;
#9622=EDGE_CURVE ( 'NONE', #3832, #15072, #3175, .T. ) ;
#9625=ORIENTED_EDGE ( 'NONE', *, *, #991, .T. ) ;
#9629=FACE_OUTER_BOUND ( 'NONE', #10972, .T. ) ;
#9630=ORIENTED_EDGE ( 'NONE', *, *, #5038, .F. ) ;
#9632=AXIS2_PLACEMENT_3D ( 'NONE', #3242, #8084, #3164 ) ;
#9633=AXIS2_PLACEMENT_3D ( 'NONE', #1458, #9599, #12266 ) ;
#9634=AXIS2_PLACEMENT_3D ( 'NONE', #4612, #5704, #4293 ) ;
#9638=EDGE_CURVE ( 'NONE', #2526, #9061, #4875, .T. ) ;
#9641=DIRECTION ( 'NONE',  ( 1.000000000000000000, -1.734723475976817507E-14, -3.009265538105091894E-28 ) ) ;
#9644=EDGE_CURVE ( 'NONE', #10586, #8739, #1217, .T. ) ;
#9645=CARTESIAN_POINT ( 'NONE',  ( 0.1062992125984796865, -0.1023622047244094474, -0.5870514566507987197 ) ) ;
#9648=AXIS2_PLACEMENT_3D ( 'NONE', #10056, #6359, #10223 ) ;
#9651=EDGE_LOOP ( 'NONE', ( #425, #6309, #10777, #7036 ) ) ;
#9655=ORIENTED_EDGE ( 'NONE', *, *, #5974, .T. ) ;
#9657=ORIENTED_EDGE ( 'NONE', *, *, #13589, .T. ) ;
#9658=CIRCLE ( 'NONE', #10882, 0.003937007874015724558 ) ;
#9659=ORIENTED_EDGE ( 'NONE', *, *, #14448, .F. ) ;
#9660=AXIS2_PLACEMENT_3D ( 'NONE', #4830, #12998, #2190 ) ;
#9663=VECTOR ( 'NONE', #5909, 39.37007874015748143 ) ;
#9667=DIRECTION ( 'NONE',  ( 0.000000000000000000, 0.000000000000000000, -1.000000000000000000 ) ) ;
#9669=ORIENTED_EDGE ( 'NONE', *, *, #8287, .T. ) ;
#9672=AXIS2_PLACEMENT_3D ( 'NONE', #464, #13588, #9939 ) ;
#9675=ADVANCED_FACE ( 'NONE', ( #14452 ), #1353, .F. ) ;
#9676=DIRECTION ( 'NONE',  ( 1.445602896647339903E-16, 0.000000000000000000, -1.000000000000000000 ) ) ;
#9677=VECTOR ( 'NONE', #13892, 39.37007874015748143 ) ;
#9678=VERTEX_POINT ( 'NONE', #335 ) ;
#9679=ORIENTED_EDGE ( 'NONE', *, *, #7009, .F. ) ;
#9680=ORIENTED_EDGE ( 'NONE', *, *, #3481, .T. ) ;
#9681=ORIENTED_EDGE ( 'NONE', *, *, #7986, .T. ) ;
#9683=VECTOR ( 'NONE', #7477, 39.37007874015748143 ) ;
#9684=CARTESIAN_POINT ( 'NONE',  ( 0.000000000000000000, 2.165354330708661568, 0.000000000000000000 ) ) ;
#9687=DIRECTION ( 'NONE',  ( 0.4999999999999979461, 0.000000000000000000, 0.8660254037844398178 ) ) ;
#9693=CARTESIAN_POINT ( 'NONE',  ( 0.5905511811023622659, -0.2952755905511811330, -0.4584677793364514420 ) ) ;
#9694=AXIS2_PLACEMENT_3D ( 'NONE', #652, #12400, #1670 ) ;
#9697=ORIENTED_EDGE ( 'NONE', *, *, #7416, .F. ) ;
#9699=ORIENTED_EDGE ( 'NONE', *, *, #13311, .T. ) ;
#9700=ADVANCED_FACE ( 'NONE', ( #14682 ), #11690, .T. ) ;
#9702=DIRECTION ( 'NONE',  ( -1.000000000000000000, -0.000000000000000000, -3.075191616504340279E-15 ) ) ;
#9704=CARTESIAN_POINT ( 'NONE',  ( 0.03346456692910666081, -0.4881889763779528324, -0.05796233017450189845 ) ) ;
#9705=CARTESIAN_POINT ( 'NONE',  ( 0.2373612774290684013, -0.4921259842519685179, 0.06430355563125962626 ) ) ;
#9706=DIRECTION ( 'NONE',  ( -0.5000000000000035527, -0.000000000000000000, 0.8660254037844365982 ) ) ;
#9709=DIRECTION ( 'NONE',  ( 0.000000000000000000, -1.000000000000000000, 0.000000000000000000 ) ) ;
#9710=CARTESIAN_POINT ( 'NONE',  ( 0.1023622047244638067, -0.1023622047244094474, -0.2472069366676780122 ) ) ;
#9712=EDGE_CURVE ( 'NONE', #10775, #1163, #14522, .T. ) ;
#9714=VERTEX_POINT ( 'NONE', #3635 ) ;
#9715=ORIENTED_EDGE ( 'NONE', *, *, #8663, .F. ) ;
#9716=VECTOR ( 'NONE', #1700, 39.37007874015748143 ) ;
#9719=ADVANCED_FACE ( 'NONE', ( #8413 ), #7838, .F. ) ;
#9727=AXIS2_PLACEMENT_3D ( 'NONE', #11449, #5542, #7992 ) ;
#9732=CARTESIAN_POINT ( 'NONE',  ( -0.3294846884549020305, -0.2952755905511811330, 0.2675111804726948983 ) ) ;
#9733=TOROIDAL_SURFACE ( 'NONE', #4211, 0.007874015748031495954, 0.003937007874015747977 ) ;
#9734=FACE_OUTER_BOUND ( 'NONE', #10372, .T. ) ;
#9735=ADVANCED_FACE ( 'NONE', ( #10274, #9978 ), #14991, .F. ) ;
#9736=EDGE_LOOP ( 'NONE', ( #11320, #9965, #5155, #2519 ) ) ;
#9738=ADVANCED_FACE ( 'NONE', ( #4014 ), #4167, .T. ) ;
#9741=DIRECTION ( 'NONE',  ( 0.8660254037844365982, -0.000000000000000000, 0.5000000000000035527 ) ) ;
#9742=ADVANCED_FACE ( 'NONE', ( #8789 ), #7604, .T. ) ;
#9744=CARTESIAN_POINT ( 'NONE',  ( 0.09842519685044820443, -0.4881889763779528324, -0.5870514566507987197 ) ) ;
#9746=DIRECTION ( 'NONE',  ( 0.000000000000000000, -1.000000000000000000, 1.734723475976817507E-14 ) ) ;
#9750=CARTESIAN_POINT ( 'NONE',  ( 0.1743691514447621993, -0.1023622047244094474, 0.1734091183126679481 ) ) ;
#9755=VERTEX_POINT ( 'NONE', #13800 ) ;
#9757=ORIENTED_EDGE ( 'NONE', *, *, #8488, .F. ) ;
#9759=DIRECTION ( 'NONE',  ( 0.5000000000000008882, -0.000000000000000000, -0.8660254037844380415 ) ) ;
#9760=ADVANCED_FACE ( 'NONE', ( #2995 ), #11459, .T. ) ;
#9761=EDGE_CURVE ( 'NONE', #3987, #253, #12937, .T. ) ;
#9763=LINE ( 'NONE', #3725, #7833 ) ;
#9771=ORIENTED_EDGE ( 'NONE', *, *, #1986, .T. ) ;
#9772=ORIENTED_EDGE ( 'NONE', *, *, #7009, .T. ) ;
#9773=PRODUCT_DEFINITION ( 'UNKNOWN', '', #15384, #6723 ) ;
#9774=CARTESIAN_POINT ( 'NONE',  ( 0.4822834645669299980, -0.1023622047244094474, 0.3466374647693608591 ) ) ;
#9779=SPHERICAL_SURFACE ( 'NONE', #5140, 0.003937007874015747977 ) ;
#9784=ORIENTED_EDGE ( 'NONE', *, *, #1868, .T. ) ;
#9792=LINE ( 'NONE', #14497, #6825 ) ;
#9795=ORIENTED_EDGE ( 'NONE', *, *, #4793, .T. ) ;
#9799=ORIENTED_EDGE ( 'NONE', *, *, #4659, .T. ) ;
#9803=FACE_OUTER_BOUND ( 'NONE', #7561, .T. ) ;
#9809=DIRECTION ( 'NONE',  ( -1.301042606982607687E-14, 0.000000000000000000, 1.000000000000000000 ) ) ;
#9813=DIRECTION ( 'NONE',  ( -0.5000000000000001110, 0.000000000000000000, -0.8660254037844385966 ) ) ;
#9816=DIRECTION ( 'NONE',  ( 0.5000000000000035527, -0.000000000000000000, -0.8660254037844365982 ) ) ;
#9819=ORIENTED_EDGE ( 'NONE', *, *, #308, .F. ) ;
#9823=CARTESIAN_POINT ( 'NONE',  ( 0.1724006475077543565, -0.09842519685039370636, 0.1689446513984334541 ) ) ;
#9826=DIRECTION ( 'NONE',  ( -0.8660254037844385966, -0.000000000000000000, 0.4999999999999998890 ) ) ;
#9828=CARTESIAN_POINT ( 'NONE',  ( 0.4462573421471743851, -0.2952755905511811330, 0.1439951688233476745 ) ) ;
#9829=FACE_OUTER_BOUND ( 'NONE', #7463, .T. ) ;
#9830=EDGE_CURVE ( 'NONE', #13377, #241, #13700, .T. ) ;
#9831=FACE_OUTER_BOUND ( 'NONE', #1404, .T. ) ;
#9832=CARTESIAN_POINT ( 'NONE',  ( 0.5595825771504284729, -0.4881889763779528324, 0.2048774586467246028 ) ) ;
#9833=ORIENTED_EDGE ( 'NONE', *, *, #8280, .T. ) ;
#9834=ADVANCED_FACE ( 'NONE', ( #3383 ), #793, .T. ) ;
#9838=CIRCLE ( 'NONE', #4320, 0.003937007874015750579 ) ;
#9840=DIRECTION ( 'NONE',  ( 0.8660254037844383745, 0.000000000000000000, -0.5000000000000004441 ) ) ;
#9846=AXIS2_PLACEMENT_3D ( 'NONE', #11328, #9741, #4051 ) ;
#9854=EDGE_CURVE ( 'NONE', #6744, #9415, #8206, .T. ) ;
#9858=ORIENTED_EDGE ( 'NONE', *, *, #11604, .F. ) ;
#9860=AXIS2_PLACEMENT_3D ( 'NONE', #12098, #44, #1149 ) ;
#9864=DIRECTION ( 'NONE',  ( 0.000000000000000000, 0.000000000000000000, 1.000000000000000000 ) ) ;
#9865=AXIS2_PLACEMENT_3D ( 'NONE', #885, #9571, #974 ) ;
#9866=CARTESIAN_POINT ( 'NONE',  ( -0.1028896637645180384, -0.1023622047244094474, -0.2462933508112025438 ) ) ;
#9869=CYLINDRICAL_SURFACE ( 'NONE', #7219, 0.003937007874015749712 ) ;
#9871=ORIENTED_EDGE ( 'NONE', *, *, #923, .T. ) ;
#9879=ORIENTED_EDGE ( 'NONE', *, *, #11500, .F. ) ;
#9880=AXIS2_PLACEMENT_3D ( 'NONE', #14923, #3161, #6748 ) ;
#9881=ADVANCED_FACE ( 'NONE', ( #4547 ), #9329, .T. ) ;
#9885=ADVANCED_FACE ( 'NONE', ( #6984 ), #6941, .T. ) ;
#9886=VECTOR ( 'NONE', #4559, 39.37007874015748143 ) ;
#9887=VECTOR ( 'NONE', #10289, 39.37007874015748143 ) ;
#9891=AXIS2_PLACEMENT_3D ( 'NONE', #13317, #13409, #6106 ) ;
#9894=CARTESIAN_POINT ( 'NONE',  ( -0.2393297813659120143, -0.4921259842519685179, 0.06089400679736763772 ) ) ;
#9896=DIRECTION ( 'NONE',  ( 0.000000000000000000, -8.673617379884013384E-15, 1.000000000000000000 ) ) ;
#9899=CIRCLE ( 'NONE', #5366, 0.03937007874015751446 ) ;
#9900=AXIS2_PLACEMENT_3D ( 'NONE', #12252, #10908, #13325 ) ;
#9904=ORIENTED_EDGE ( 'NONE', *, *, #3103, .F. ) ;
#9906=ADVANCED_FACE ( 'NONE', ( #13611 ), #10174, .F. ) ;
#9907=LINE ( 'NONE', #274, #8409 ) ;
#9908=PLANE ( 'NONE',  #11910 ) ;
#9909=DIRECTION ( 'NONE',  ( -0.5000000000000001110, -0.000000000000000000, 0.8660254037844385966 ) ) ;
#9916=AXIS2_PLACEMENT_3D ( 'NONE', #9984, #14762, #504 ) ;
#9919=AXIS2_PLACEMENT_3D ( 'NONE', #9369, #15248, #14300 ) ;
#9925=DIRECTION ( 'NONE',  ( 0.000000000000000000, 0.000000000000000000, 1.000000000000000000 ) ) ;
#9926=ORIENTED_EDGE ( 'NONE', *, *, #3154, .T. ) ;
#9929=ADVANCED_FACE ( 'NONE', ( #7894 ), #3203, .T. ) ;
#9933=DIRECTION ( 'NONE',  ( 0.4999999999999979461, 0.000000000000000000, 0.8660254037844398178 ) ) ;
#9939=DIRECTION ( 'NONE',  ( -4.336808689942014285E-16, 0.000000000000000000, 1.000000000000000000 ) ) ;
#9942=VECTOR ( 'NONE', #5086, 39.37007874015748143 ) ;
#9944=ORIENTED_EDGE ( 'NONE', *, *, #13531, .T. ) ;
#9945=EDGE_LOOP ( 'NONE', ( #7864, #2875 ) ) ;
#9947=AXIS2_PLACEMENT_3D ( 'NONE', #4219, #843, #6484 ) ;
#9950=DIRECTION ( 'NONE',  ( 0.8660254037844383745, 0.000000000000000000, -0.5000000000000004441 ) ) ;
#9953=EDGE_CURVE ( 'NONE', #12689, #13646, #7738, .T. ) ;
#9954=DIRECTION ( 'NONE',  ( -1.000000000000000000, 0.000000000000000000, 0.000000000000000000 ) ) ;
#9955=AXIS2_PLACEMENT_3D ( 'NONE', #13641, #14904, #3055 ) ;
#9956=DIRECTION ( 'NONE',  ( 0.000000000000000000, 0.000000000000000000, -1.000000000000000000 ) ) ;
#9965=ORIENTED_EDGE ( 'NONE', *, *, #8775, .F. ) ;
#9969=DIRECTION ( 'NONE',  ( -1.000000000000000000, 0.000000000000000000, 0.000000000000000000 ) ) ;
#9970=CIRCLE ( 'NONE', #1461, 0.003937007874015750579 ) ;
#9973=EDGE_LOOP ( 'NONE', ( #15313, #10630, #2419, #9183 ) ) ;
#9978=FACE_OUTER_BOUND ( 'NONE', #1710, .T. ) ;
#9981=ORIENTED_EDGE ( 'NONE', *, *, #9534, .T. ) ;
#9982=ORIENTED_EDGE ( 'NONE', *, *, #7525, .T. ) ;
#9983=FACE_OUTER_BOUND ( 'NONE', #8757, .T. ) ;
#9984=CARTESIAN_POINT ( 'NONE',  ( 0.05905511811029064834, -0.1023622047244094474, -0.5870514566507987197 ) ) ;
#9988=ADVANCED_FACE ( 'NONE', ( #13845 ), #5921, .T. ) ;
#9989=CARTESIAN_POINT ( 'NONE',  ( -0.06692913385815749128, -0.4881889763779528324, -0.2377126739438355507 ) ) ;
#9992=EDGE_CURVE ( 'NONE', #11698, #14663, #12454, .T. ) ;
#9994=ORIENTED_EDGE ( 'NONE', *, *, #11199, .F. ) ;
#10000=EDGE_CURVE ( 'NONE', #3536, #7254, #10443, .T. ) ;
#10003=LINE ( 'NONE', #687, #5562 ) ;
#10006=EDGE_CURVE ( 'NONE', #14974, #10309, #10312, .T. ) ;
#10009=EDGE_CURVE ( 'NONE', #11649, #4524, #15030, .T. ) ;
#10010=VERTEX_POINT ( 'NONE', #4280 ) ;
#10019=DIRECTION ( 'NONE',  ( -1.000000000000000000, -0.000000000000000000, -3.476578583725179813E-16 ) ) ;
#10022=ORIENTED_EDGE ( 'NONE', *, *, #3600, .F. ) ;
#10027=EDGE_LOOP ( 'NONE', ( #9833, #11005, #14323, #8700 ) ) ;
#10033=CARTESIAN_POINT ( 'NONE',  ( -0.09948011493072102251, -0.4881889763779528324, -0.2443248468741946733 ) ) ;
#10035=CARTESIAN_POINT ( 'NONE',  ( 0.000000000000000000, 0.003937007874015860734, 0.000000000000000000 ) ) ;
#10037=ORIENTED_EDGE ( 'NONE', *, *, #4172, .F. ) ;
#10038=LINE ( 'NONE', #11130, #12190 ) ;
#10039=FACE_OUTER_BOUND ( 'NONE', #1939, .T. ) ;
#10040=SPHERICAL_SURFACE ( 'NONE', #8217, 0.003937007874015747977 ) ;
#10041=CARTESIAN_POINT ( 'NONE',  ( -0.1552072824047652233, -0.003937007874015747977, -0.5870514566507987197 ) ) ;
#10042=DIRECTION ( 'NONE',  ( 0.8660254037844389297, 0.000000000000000000, -0.4999999999999994449 ) ) ;
#10043=ORIENTED_EDGE ( 'NONE', *, *, #11469, .T. ) ;
#10045=ORIENTED_EDGE ( 'NONE', *, *, #1026, .F. ) ;
#10047=CARTESIAN_POINT ( 'NONE',  ( -0.2393297813659119588, -0.1023622047244094474, 0.06089400679736759608 ) ) ;
#10048=CARTESIAN_POINT ( 'NONE',  ( -0.2661821753646866906, -0.1023622047244094474, 0.03548265769538203052 ) ) ;
#10049=DIRECTION ( 'NONE',  ( -0.8660254037844309360, 0.000000000000000000, 0.5000000000000134337 ) ) ;
#10053=DIRECTION ( 'NONE',  ( 0.5000000000000004441, -1.502314598737161516E-14, 0.8660254037844384856 ) ) ;
#10054=CARTESIAN_POINT ( 'NONE',  ( -0.1062992125983150127, -0.4881889763779528324, -0.2482618547482104143 ) ) ;
#10056=CARTESIAN_POINT ( 'NONE',  ( 0.000000000000000000, -0.1023622047244094474, 0.000000000000000000 ) ) ;
#10058=ORIENTED_EDGE ( 'NONE', *, *, #6388, .T. ) ;
#10060=ORIENTED_EDGE ( 'NONE', *, *, #778, .T. ) ;
#10063=ADVANCED_FACE ( 'NONE', ( #12757 ), #11814, .T. ) ;
#10071=CARTESIAN_POINT ( 'NONE',  ( 0.4342073824196633347, -0.09448818897637796532, 0.4299076816772810505 ) ) ;
#10085=CARTESIAN_POINT ( 'NONE',  ( -0.4788739157331333707, -0.09842519685039370636, 0.3446689608323532106 ) ) ;
#10088=DIRECTION ( 'NONE',  ( 0.000000000000000000, 0.000000000000000000, 1.000000000000000000 ) ) ;
#10089=CIRCLE ( 'NONE', #10343, 0.003937007874015724558 ) ;
#10090=DIRECTION ( 'NONE',  ( -0.8660254037844385966, 0.000000000000000000, -0.5000000000000002220 ) ) ;
#10091=DIRECTION ( 'NONE',  ( 0.000000000000000000, 1.000000000000000000, 0.000000000000000000 ) ) ;
#10092=CIRCLE ( 'NONE', #6305, 0.003937007874015754916 ) ;
#10096=ORIENTED_EDGE ( 'NONE', *, *, #6715, .F. ) ;
#10101=CIRCLE ( 'NONE', #12356, 0.03937007874015753528 ) ;
#10107=ADVANCED_FACE ( 'NONE', ( #150 ), #1473, .T. ) ;
#10109=DIRECTION ( 'NONE',  ( 0.4999999999999922284, -0.000000000000000000, -0.8660254037844431485 ) ) ;
#10110=DIRECTION ( 'NONE',  ( 1.000000000000000000, 0.000000000000000000, 3.476578583725179813E-16 ) ) ;
#10112=VECTOR ( 'NONE', #12455, 39.37007874015748143 ) ;
#10113=DIRECTION ( 'NONE',  ( 0.000000000000000000, 0.000000000000000000, 1.000000000000000000 ) ) ;
#10115=LINE ( 'NONE', #8861, #3135 ) ;
#10116=VERTEX_POINT ( 'NONE', #1534 ) ;
#10124=CYLINDRICAL_SURFACE ( 'NONE', #7583, 0.003937007874015724558 ) ;
#10130=AXIS2_PLACEMENT_3D ( 'NONE', #1831, #8898, #9925 ) ;
#10133=DIRECTION ( 'NONE',  ( -0.8660254037844385966, 0.000000000000000000, -0.5000000000000000000 ) ) ;
#10137=DIRECTION ( 'NONE',  ( -1.000000000000000000, 0.000000000000000000, 0.000000000000000000 ) ) ;
#10140=CYLINDRICAL_SURFACE ( 'NONE', #12636, 0.003937007874015749712 ) ;
#10141=VECTOR ( 'NONE', #5402, 39.37007874015748143 ) ;
#10143=AXIS2_PLACEMENT_3D ( 'NONE', #12890, #2160, #1224 ) ;
#10145=VERTEX_POINT ( 'NONE', #4911 ) ;
#10146=CIRCLE ( 'NONE', #13643, 0.003937007874015721089 ) ;
#10149=EDGE_LOOP ( 'NONE', ( #1777, #3281, #10776, #3750 ) ) ;
#10151=AXIS2_PLACEMENT_3D ( 'NONE', #3188, #12258, #8646 ) ;
#10155=( CONVERSION_BASED_UNIT ( 'INCH', #7871 ) LENGTH_UNIT ( ) NAMED_UNIT ( #11555 ) );
#10160=FACE_OUTER_BOUND ( 'NONE', #3569, .T. ) ;
#10161=CARTESIAN_POINT ( 'NONE',  ( 0.1754240695251997051, -0.1023622047244094474, 0.1694721104386522070 ) ) ;
#10163=AXIS2_PLACEMENT_3D ( 'NONE', #3304, #4245, #6666 ) ;
#10165=ORIENTED_EDGE ( 'NONE', *, *, #10937, .T. ) ;
#10169=AXIS2_PLACEMENT_3D ( 'NONE', #7064, #13978, #3244 ) ;
#10174=CYLINDRICAL_SURFACE ( 'NONE', #7439, 0.03937007874015751446 ) ;
#10175=DIRECTION ( 'NONE',  ( 0.000000000000000000, -1.734723475976806463E-14, -1.000000000000000000 ) ) ;
#10176=DIRECTION ( 'NONE',  ( 0.000000000000000000, 0.000000000000000000, 1.000000000000000000 ) ) ;
#10177=DIRECTION ( 'NONE',  ( -0.000000000000000000, -1.000000000000000000, 0.000000000000000000 ) ) ;
#10178=FACE_OUTER_BOUND ( 'NONE', #7332, .T. ) ;
#10180=CARTESIAN_POINT ( 'NONE',  ( -0.5615510810874360104, -0.09842519685039370636, 0.2014679098129269208 ) ) ;
#10183=DIRECTION ( 'NONE',  ( 0.8660254037844388186, 0.000000000000000000, -0.4999999999999996669 ) ) ;
#10184=ORIENTED_EDGE ( 'NONE', *, *, #10009, .T. ) ;
#10185=EDGE_CURVE ( 'NONE', #4812, #11006, #10783, .T. ) ;
#10187=ORIENTED_EDGE ( 'NONE', *, *, #4032, .T. ) ;
#10188=AXIS2_PLACEMENT_3D ( 'NONE', #15306, #4565, #9351 ) ;
#10190=ORIENTED_EDGE ( 'NONE', *, *, #9854, .T. ) ;
#10193=DIRECTION ( 'NONE',  ( 0.8660254037844374864, 0.000000000000000000, 0.5000000000000017764 ) ) ;
#10196=CARTESIAN_POINT ( 'NONE',  ( 0.1552072824047652233, -0.09448818897637796532, -0.5909884645248143498 ) ) ;
#10198=CARTESIAN_POINT ( 'NONE',  ( 0.4307978335858663188, -0.003937007874015747977, 0.4279391777402731800 ) ) ;
#10199=EDGE_CURVE ( 'NONE', #7217, #3033, #15448, .T. ) ;
#10200=VERTEX_POINT ( 'NONE', #229 ) ;
#10201=DIRECTION ( 'NONE',  ( 0.8660254037844385966, 0.000000000000000000, 0.5000000000000000000 ) ) ;
#10204=CYLINDRICAL_SURFACE ( 'NONE', #3090, 0.003937007874015747109 ) ;
#10205=ORIENTED_EDGE ( 'NONE', *, *, #12678, .F. ) ;
#10206=ADVANCED_FACE ( 'NONE', ( #7259 ), #1309, .T. ) ;
#10207=DIRECTION ( 'NONE',  ( 0.5000000000000001110, 0.000000000000000000, 0.8660254037844384856 ) ) ;
#10208=ADVANCED_FACE ( 'NONE', ( #13287 ), #1244, .T. ) ;
#10209=VERTEX_POINT ( 'NONE', #12048 ) ;
#10211=AXIS2_PLACEMENT_3D ( 'NONE', #12209, #11079, #64 ) ;
#10214=DIRECTION ( 'NONE',  ( -0.000000000000000000, 1.000000000000000000, -0.000000000000000000 ) ) ;
#10215=CIRCLE ( 'NONE', #13221, 0.003937007874015721089 ) ;
#10216=FACE_OUTER_BOUND ( 'NONE', #6496, .T. ) ;
#10220=SPHERICAL_SURFACE ( 'NONE', #7122, 0.003937007874015747977 ) ;
#10221=EDGE_LOOP ( 'NONE', ( #3588, #4750, #4648 ) ) ;
#10223=DIRECTION ( 'NONE',  ( 0.000000000000000000, 0.000000000000000000, -1.000000000000000000 ) ) ;
#10225=ADVANCED_FACE ( 'NONE', ( #6222 ), #10856, .T. ) ;
#10227=ORIENTED_EDGE ( 'NONE', *, *, #10006, .F. ) ;
#10229=ORIENTED_EDGE ( 'NONE', *, *, #8552, .T. ) ;
#10231=ORIENTED_EDGE ( 'NONE', *, *, #2238, .F. ) ;
#10233=DIRECTION ( 'NONE',  ( 0.4999999999999998335, 0.000000000000000000, 0.8660254037844388186 ) ) ;
#10237=DIRECTION ( 'NONE',  ( 0.000000000000000000, -1.000000000000000000, 0.000000000000000000 ) ) ;
#10238=DIRECTION ( 'NONE',  ( 0.000000000000000000, 0.000000000000000000, 1.000000000000000000 ) ) ;
#10242=VERTEX_POINT ( 'NONE', #5131 ) ;
#10244=ORIENTED_EDGE ( 'NONE', *, *, #10888, .F. ) ;
#10247=CARTESIAN_POINT ( 'NONE',  ( -0.5894146648244306119, -0.09842519685039370636, 0.1610807828475335490 ) ) ;
#10249=FACE_OUTER_BOUND ( 'NONE', #5824, .T. ) ;
#10253=VERTEX_POINT ( 'NONE', #5353 ) ;
#10254=DIRECTION ( 'NONE',  ( -1.000000000000000000, 0.000000000000000000, 0.000000000000000000 ) ) ;
#10255=CARTESIAN_POINT ( 'NONE',  ( -0.4305093106511125312, -0.2952755905511811330, 0.1712715594937239405 ) ) ;
#10256=VERTEX_POINT ( 'NONE', #5206 ) ;
#10258=ADVANCED_FACE ( 'NONE', ( #6461 ), #6606, .T. ) ;
#10261=CARTESIAN_POINT ( 'NONE',  ( -0.1062992125983150959, -0.09842519685039370636, -3.695575659861521121E-17 ) ) ;
#10262=EDGE_CURVE ( 'NONE', #3552, #9161, #13583, .T. ) ;
#10263=FACE_OUTER_BOUND ( 'NONE', #2922, .T. ) ;
#10266=DIRECTION ( 'NONE',  ( 0.8660254037844388186, 0.000000000000000000, -0.4999999999999998335 ) ) ;
#10267=DIRECTION ( 'NONE',  ( 0.8660254037844383745, 9.486769009248228879E-16, 0.5000000000000004441 ) ) ;
#10269=DIRECTION ( 'NONE',  ( 1.000000000000000000, 0.000000000000000000, 3.614007241618347785E-16 ) ) ;
#10271=CYLINDRICAL_SURFACE ( 'NONE', #6189, 0.03937007874015754916 ) ;
#10274=FACE_BOUND ( 'NONE', #10489, .T. ) ;
#10277=VERTEX_POINT ( 'NONE', #5271 ) ;
#10279=ORIENTED_EDGE ( 'NONE', *, *, #9622, .T. ) ;
#10280=CARTESIAN_POINT ( 'NONE',  ( 0.1638199706403873079, -0.4921259842519685179, 0.2127791970528254417 ) ) ;
#10282=EDGE_CURVE ( 'NONE', #11838, #11452, #13212, .T. ) ;
#10289=DIRECTION ( 'NONE',  ( -3.614007241618347785E-16, 0.000000000000000000, 1.000000000000000000 ) ) ;
#10291=ORIENTED_EDGE ( 'NONE', *, *, #13260, .F. ) ;
#10292=ORIENTED_EDGE ( 'NONE', *, *, #5773, .F. ) ;
#10294=ORIENTED_EDGE ( 'NONE', *, *, #2629, .T. ) ;
#10295=EDGE_LOOP ( 'NONE', ( #12070, #1782, #13711, #12780 ) ) ;
#10296=CYLINDRICAL_SURFACE ( 'NONE', #13106, 0.1574803149606299191 ) ;
#10298=( NAMED_UNIT ( * ) PLANE_ANGLE_UNIT ( ) SI_UNIT ( $, .RADIAN. ) );
#10300=DIRECTION ( 'NONE',  ( 0.000000000000000000, 0.000000000000000000, -1.000000000000000000 ) ) ;
#10301=DIRECTION ( 'NONE',  ( 0.000000000000000000, 1.000000000000000000, -0.000000000000000000 ) ) ;
#10304=LINE ( 'NONE', #12438, #1084 ) ;
#10307=ORIENTED_EDGE ( 'NONE', *, *, #13036, .F. ) ;
#10309=VERTEX_POINT ( 'NONE', #12666 ) ;
#10310=CARTESIAN_POINT ( 'NONE',  ( -0.4769054117961255002, -0.4881889763779528324, 0.3480785096661502265 ) ) ;
#10312=LINE ( 'NONE', #10247, #13201 ) ;
#10317=EDGE_LOOP ( 'NONE', ( #6702, #4126, #2041, #9981, #10578, #10529, #5454, #6367, #1607, #7317, #10454, #3986, #14917, #13189, #14674, #1359, #5522, #14111 ) ) ;
#10319=EDGE_CURVE ( 'NONE', #14035, #11638, #11464, .T. ) ;
#10321=CARTESIAN_POINT ( 'NONE',  ( -0.06692913385815735250, -0.4881889763779528324, -0.5870514566507987197 ) ) ;
#10323=VERTEX_POINT ( 'NONE', #8908 ) ;
#10326=AXIS2_PLACEMENT_3D ( 'NONE', #3670, #8444, #7792 ) ;
#10330=FACE_OUTER_BOUND ( 'NONE', #9519, .T. ) ;
#10333=DIRECTION ( 'NONE',  ( 0.000000000000000000, 1.000000000000000000, 0.000000000000000000 ) ) ;
#10334=ORIENTED_EDGE ( 'NONE', *, *, #4271, .F. ) ;
#10338=TOROIDAL_SURFACE ( 'NONE', #13844, 0.1614173228346456879, 0.003937007874015747977 ) ;
#10339=CARTESIAN_POINT ( 'NONE',  ( 0.4552518684890383138, -0.09448818897637796532, 0.3855835468379170128 ) ) ;
#10343=AXIS2_PLACEMENT_3D ( 'NONE', #12748, #10472, #7084 ) ;
#10344=DIRECTION ( 'NONE',  ( -0.5000000000000004441, 0.000000000000000000, -0.8660254037844383745 ) ) ;
#10352=VECTOR ( 'NONE', #1133, 39.37007874015748143 ) ;
#10353=AXIS2_PLACEMENT_3D ( 'NONE', #4093, #9909, #10133 ) ;
#10355=DIRECTION ( 'NONE',  ( -0.5000000000000004441, -0.000000000000000000, -0.8660254037844384856 ) ) ;
#10358=CARTESIAN_POINT ( 'NONE',  ( 0.05905511811029059283, -0.09842519685039370636, -0.2377126739437405434 ) ) ;
#10359=CIRCLE ( 'NONE', #9865, 0.003937007874015749712 ) ;
#10363=DIRECTION ( 'NONE',  ( -1.000000000000000000, 8.673617379884013384E-15, 0.000000000000000000 ) ) ;
#10365=DIRECTION ( 'NONE',  ( 0.8660254037844389297, 0.000000000000000000, -0.4999999999999994449 ) ) ;
#10367=EDGE_CURVE ( 'NONE', #7381, #4497, #1459, .T. ) ;
#10369=CIRCLE ( 'NONE', #12121, 0.003937007874015724558 ) ;
#10371=AXIS2_PLACEMENT_3D ( 'NONE', #10651, #2494, #7202 ) ;
#10372=EDGE_LOOP ( 'NONE', ( #5936, #14241, #9188, #4073, #10060, #3859 ) ) ;
#10374=LINE ( 'NONE', #11549, #13605 ) ;
#10382=AXIS2_PLACEMENT_3D ( 'NONE', #12562, #572, #13811 ) ;
#10386=DIRECTION ( 'NONE',  ( -0.5000000000000004441, 3.120833636094142350E-14, -0.8660254037844383745 ) ) ;
#10388=CIRCLE ( 'NONE', #6882, 0.003937007874015724558 ) ;
#10389=DIRECTION ( 'NONE',  ( 0.000000000000000000, 0.000000000000000000, 1.000000000000000000 ) ) ;
#10390=EDGE_CURVE ( 'NONE', #14789, #986, #8455, .T. ) ;
#10397=ORIENTED_EDGE ( 'NONE', *, *, #8119, .T. ) ;
#10398=CIRCLE ( 'NONE', #9660, 0.003937007874015749712 ) ;
#10404=CARTESIAN_POINT ( 'NONE',  ( -0.06692913385815731087, -0.2952755905511811330, -0.3797276218561366212 ) ) ;
#10407=VECTOR ( 'NONE', #10555, 39.37007874015748143 ) ;
#10410=DIRECTION ( 'NONE',  ( 1.000000000000000000, 0.000000000000000000, 0.000000000000000000 ) ) ;
#10411=CIRCLE ( 'NONE', #7653, 0.003937007874015758385 ) ;
#10414=DIRECTION ( 'NONE',  ( 0.000000000000000000, 0.000000000000000000, -1.000000000000000000 ) ) ;
#10419=EDGE_CURVE ( 'NONE', #11634, #8036, #13915, .T. ) ;
#10420=EDGE_LOOP ( 'NONE', ( #10916, #845, #3522, #12925 ) ) ;
#10421=CARTESIAN_POINT ( 'NONE',  ( 0.5905511811023620439, -0.003937007874015747977, 0.1591122789105293978 ) ) ;
#10424=FACE_OUTER_BOUND ( 'NONE', #8740, .T. ) ;
#10427=DIRECTION ( 'NONE',  ( -0.4999999999999998890, -5.810221930991196648E-16, 0.8660254037844387076 ) ) ;
#10428=DIRECTION ( 'NONE',  ( -0.000000000000000000, -1.000000000000000000, 0.000000000000000000 ) ) ;
#10429=ORIENTED_EDGE ( 'NONE', *, *, #10486, .T. ) ;
#10430=DIRECTION ( 'NONE',  ( -0.000000000000000000, 1.000000000000000000, 0.000000000000000000 ) ) ;
#10431=DIRECTION ( 'NONE',  ( 0.000000000000000000, 1.000000000000000000, 0.000000000000000000 ) ) ;
#10433=CARTESIAN_POINT ( 'NONE',  ( 0.4591888763630541104, -0.4921259842519685179, 0.3787644491703230365 ) ) ;
#10434=CARTESIAN_POINT ( 'NONE',  ( -0.03346456692910660530, -0.4881889763779528324, -0.05796233017450189845 ) ) ;
#10437=VECTOR ( 'NONE', #10254, 39.37007874015748143 ) ;
#10440=AXIS2_PLACEMENT_3D ( 'NONE', #14424, #3528, #10659 ) ;
#10441=CARTESIAN_POINT ( 'NONE',  ( -0.09842519685028340570, -0.4921259842519685179, -0.5870514566507987197 ) ) ;
#10443=CIRCLE ( 'NONE', #1931, 0.003937007874015758385 ) ;
#10444=CARTESIAN_POINT ( 'NONE',  ( -0.4552518684890389244, -0.09842519685039370636, 0.3855835468379172903 ) ) ;
#10447=DIRECTION ( 'NONE',  ( 0.8660254037844387076, 0.000000000000000000, 0.4999999999999996669 ) ) ;
#10448=ORIENTED_EDGE ( 'NONE', *, *, #4, .F. ) ;
#10449=CARTESIAN_POINT ( 'NONE',  ( 0.000000000000000000, -0.4881889763779528324, 0.000000000000000000 ) ) ;
#10450=CARTESIAN_POINT ( 'NONE',  ( 0.2647411304680618027, -0.4921259842519685179, 0.03404161279868787859 ) ) ;
#10451=CIRCLE ( 'NONE', #12457, 0.003937007874015724558 ) ;
#10452=DIRECTION ( 'NONE',  ( 0.4999999999999976130, -0.000000000000000000, 0.8660254037844400399 ) ) ;
#10454=ORIENTED_EDGE ( 'NONE', *, *, #4601, .T. ) ;
#10460=EDGE_CURVE ( 'NONE', #7381, #14663, #7448, .T. ) ;
#10461=ORIENTED_EDGE ( 'NONE', *, *, #7915, .T. ) ;
#10465=DIRECTION ( 'NONE',  ( 0.5000000000000001110, -0.000000000000000000, -0.8660254037844385966 ) ) ;
#10466=AXIS2_PLACEMENT_3D ( 'NONE', #10035, #6253, #2586 ) ;
#10467=CARTESIAN_POINT ( 'NONE',  ( 0.4330708661417309036, -0.09448818897637796532, 0.4318761856142889766 ) ) ;
#10468=LINE ( 'NONE', #4580, #8154 ) ;
#10472=DIRECTION ( 'NONE',  ( 0.000000000000000000, -1.000000000000000000, 0.000000000000000000 ) ) ;
#10475=ORIENTED_EDGE ( 'NONE', *, *, #10262, .T. ) ;
#10479=ADVANCED_FACE ( 'NONE', ( #4504 ), #7956, .T. ) ;
#10480=EDGE_CURVE ( 'NONE', #11872, #5535, #13461, .T. ) ;
#10484=EDGE_CURVE ( 'NONE', #1810, #3677, #3944, .T. ) ;
#10486=EDGE_CURVE ( 'NONE', #8145, #5520, #14713, .T. ) ;
#10488=DIRECTION ( 'NONE',  ( 0.000000000000000000, 0.000000000000000000, -1.000000000000000000 ) ) ;
#10489=EDGE_LOOP ( 'NONE', ( #6087, #12427 ) ) ;
#10490=DIRECTION ( 'NONE',  ( -0.000000000000000000, 1.000000000000000000, -0.000000000000000000 ) ) ;
#10492=ORIENTED_EDGE ( 'NONE', *, *, #14541, .F. ) ;
#10494=ORIENTED_EDGE ( 'NONE', *, *, #7425, .T. ) ;
#10496=CARTESIAN_POINT ( 'NONE',  ( 0.4296613173079339432, -0.09448818897637796532, 0.4299076816772811060 ) ) ;
#10498=EDGE_CURVE ( 'NONE', #10242, #4029, #14150, .T. ) ;
#10503=DIRECTION ( 'NONE',  ( 0.8660254037844383745, 0.000000000000000000, -0.5000000000000004441 ) ) ;
#10506=LINE ( 'NONE', #5784, #6571 ) ;
#10507=ORIENTED_EDGE ( 'NONE', *, *, #14722, .T. ) ;
#10509=DIRECTION ( 'NONE',  ( -0.8660254037844405950, 0.000000000000000000, 0.4999999999999966693 ) ) ;
#10510=EDGE_LOOP ( 'NONE', ( #7302, #8790, #7541, #9715 ) ) ;
#10512=ORIENTED_EDGE ( 'NONE', *, *, #7321, .T. ) ;
#10516=DIRECTION ( 'NONE',  ( -0.8660254037844383745, 0.000000000000000000, 0.5000000000000004441 ) ) ;
#10521=ORIENTED_EDGE ( 'NONE', *, *, #1301, .F. ) ;
#10523=DIRECTION ( 'NONE',  ( -0.000000000000000000, 1.000000000000000000, -0.000000000000000000 ) ) ;
#10524=DIRECTION ( 'NONE',  ( -0.8660254037844383745, 0.000000000000000000, -0.5000000000000004441 ) ) ;
#10525=CARTESIAN_POINT ( 'NONE',  ( -0.5452755905511542656, -0.4881889763779528324, 0.2375319020879049503 ) ) ;
#10529=ORIENTED_EDGE ( 'NONE', *, *, #15243, .T. ) ;
#10530=ORIENTED_EDGE ( 'NONE', *, *, #7705, .F. ) ;
#10533=ORIENTED_EDGE ( 'NONE', *, *, #15461, .F. ) ;
#10534=VERTEX_POINT ( 'NONE', #13992 ) ;
#10536=DIRECTION ( 'NONE',  ( -0.8660254037844400399, -5.421010862427505407E-16, 0.4999999999999976130 ) ) ;
#10539=CARTESIAN_POINT ( 'NONE',  ( 0.4307978335858662633, -0.09448818897637796532, 0.4279391777402732910 ) ) ;
#10540=DIRECTION ( 'NONE',  ( 0.8660254037844383745, -9.486769009248228879E-16, -0.5000000000000004441 ) ) ;
#10541=CARTESIAN_POINT ( 'NONE',  ( -0.1618514667033796040, -0.4881889763779528324, 0.2083147301385909200 ) ) ;
#10543=ADVANCED_FACE ( 'NONE', ( #8028 ), #413, .T. ) ;
#10544=DIRECTION ( 'NONE',  ( 0.000000000000000000, -0.000000000000000000, 1.000000000000000000 ) ) ;
#10547=ORIENTED_EDGE ( 'NONE', *, *, #5653, .T. ) ;
#10551=DIRECTION ( 'NONE',  ( 0.8660254037844365982, -0.000000000000000000, 0.5000000000000035527 ) ) ;
#10554=CARTESIAN_POINT ( 'NONE',  ( -0.04921259842516954863, -0.4881889763779528324, -0.08523872084487790768 ) ) ;
#10555=DIRECTION ( 'NONE',  ( -0.000000000000000000, -1.000000000000000000, -0.000000000000000000 ) ) ;
#10558=LINE ( 'NONE', #11820, #7638 ) ;
#10563=ORIENTED_EDGE ( 'NONE', *, *, #13057, .T. ) ;
#10566=DIRECTION ( 'NONE',  ( -1.000000000000000000, 0.000000000000000000, 0.000000000000000000 ) ) ;
#10569=CYLINDRICAL_SURFACE ( 'NONE', #5428, 0.003937007874015721089 ) ;
#10570=CYLINDRICAL_SURFACE ( 'NONE', #10440, 0.003937007874015741038 ) ;
#10572=ORIENTED_EDGE ( 'NONE', *, *, #8096, .F. ) ;
#10573=LINE ( 'NONE', #2034, #5160 ) ;
#10574=FACE_OUTER_BOUND ( 'NONE', #6720, .T. ) ;
#10575=PLANE ( 'NONE',  #4202 ) ;
#10576=EDGE_CURVE ( 'NONE', #3335, #11465, #5191, .T. ) ;
#10577=CARTESIAN_POINT ( 'NONE',  ( 0.4552518684890383138, -0.09842519685039370636, 0.3855835468379170128 ) ) ;
#10578=ORIENTED_EDGE ( 'NONE', *, *, #1538, .T. ) ;
#10580=VECTOR ( 'NONE', #13059, 39.37007874015748143 ) ;
#10583=EDGE_CURVE ( 'NONE', #5216, #8739, #13218, .T. ) ;
#10586=VERTEX_POINT ( 'NONE', #14513 ) ;
#10588=CARTESIAN_POINT ( 'NONE',  ( -0.4625984251968516259, -0.09842519685039370636, 0.3807329531073311846 ) ) ;
#10589=DIRECTION ( 'NONE',  ( 0.4999999999999966693, 0.000000000000000000, 0.8660254037844405950 ) ) ;
#10595=CIRCLE ( 'NONE', #9343, 0.04330708661417329020 ) ;
#10597=ORIENTED_EDGE ( 'NONE', *, *, #1426, .T. ) ;
#10598=CARTESIAN_POINT ( 'NONE',  ( 0.06767366483286080259, -0.2952755905511811330, 0.7209811753676967916 ) ) ;
#10599=CIRCLE ( 'NONE', #1334, 0.007874015748031499423 ) ;
#10601=DIRECTION ( 'NONE',  ( -0.8660254037844385966, 0.000000000000000000, -0.5000000000000000000 ) ) ;
#10602=CARTESIAN_POINT ( 'NONE',  ( 0.5379290338433416752, -0.1023622047244094474, 0.2423824958184916112 ) ) ;
#10606=ORIENTED_EDGE ( 'NONE', *, *, #8930, .T. ) ;
#10607=AXIS2_PLACEMENT_3D ( 'NONE', #4556, #10355, #10516 ) ;
#10611=CARTESIAN_POINT ( 'NONE',  ( 0.5418660417173575272, -0.4881889763779528324, 0.2355633981508976349 ) ) ;
#10612=EDGE_CURVE ( 'NONE', #4737, #11240, #12472, .T. ) ;
#10613=CARTESIAN_POINT ( 'NONE',  ( 0.000000000000000000, 2.165354330708661568, 0.000000000000000000 ) ) ;
#10617=DIRECTION ( 'NONE',  ( -0.4999999999999995004, -0.000000000000000000, -0.8660254037844390407 ) ) ;
#10618=DIRECTION ( 'NONE',  ( -0.5000000000000000000, 0.000000000000000000, 0.8660254037844385966 ) ) ;
#10619=DIRECTION ( 'NONE',  ( -0.000000000000000000, -1.000000000000000000, -0.000000000000000000 ) ) ;
#10620=AXIS2_PLACEMENT_3D ( 'NONE', #3820, #2883, #1639 ) ;
#10621=CIRCLE ( 'NONE', #11110, 0.003937007874015741038 ) ;
#10622=VECTOR ( 'NONE', #1322, 39.37007874015748143 ) ;
#10624=DIRECTION ( 'NONE',  ( 0.4999999999999981681, 0.000000000000000000, 0.8660254037844397068 ) ) ;
#10625=CIRCLE ( 'NONE', #7100, 0.003937007874015737569 ) ;
#10630=ORIENTED_EDGE ( 'NONE', *, *, #14807, .T. ) ;
#10631=ORIENTED_EDGE ( 'NONE', *, *, #12054, .F. ) ;
#10634=VECTOR ( 'NONE', #4720, 39.37007874015748143 ) ;
#10636=CIRCLE ( 'NONE', #9891, 0.003937007874015758385 ) ;
#10644=CIRCLE ( 'NONE', #14408, 0.003937007874015754916 ) ;
#10645=VECTOR ( 'NONE', #3632, 39.37007874015748143 ) ;
#10649=AXIS2_PLACEMENT_3D ( 'NONE', #3122, #391, #9954 ) ;
#10651=CARTESIAN_POINT ( 'NONE',  ( 0.000000000000000000, -0.4881889763779528324, 0.000000000000000000 ) ) ;
#10653=CIRCLE ( 'NONE', #5640, 0.04330708661417331101 ) ;
#10655=CIRCLE ( 'NONE', #4892, 0.003937007874015750579 ) ;
#10656=LINE ( 'NONE', #4616, #2359 ) ;
#10657=CARTESIAN_POINT ( 'NONE',  ( 0.1629063847838169432, -0.1023622047244094474, 0.2122517380126066888 ) ) ;
#10659=DIRECTION ( 'NONE',  ( -1.000000000000000000, 0.000000000000000000, -3.476578583725183758E-16 ) ) ;
#10660=AXIS2_PLACEMENT_3D ( 'NONE', #4912, #10857, #293 ) ;
#10666=CARTESIAN_POINT ( 'NONE',  ( 0.3964138223131414840, -0.2952755905511811330, 0.1515865201236449578 ) ) ;
#10668=DIRECTION ( 'NONE',  ( 1.000000000000000000, -8.673617379884051249E-15, -7.523163845262650140E-29 ) ) ;
#10670=CIRCLE ( 'NONE', #2411, 0.003937007874015750579 ) ;
#10672=ORIENTED_EDGE ( 'NONE', *, *, #12573, .T. ) ;
#10677=LINE ( 'NONE', #10808, #8082 ) ;
#10678=CYLINDRICAL_SURFACE ( 'NONE', #1904, 0.003937007874015724558 ) ;
#10679=ADVANCED_FACE ( 'NONE', ( #7452 ), #6446, .F. ) ;
#10686=DIRECTION ( 'NONE',  ( 0.000000000000000000, -0.000000000000000000, 1.000000000000000000 ) ) ;
#10688=EDGE_CURVE ( 'NONE', #2574, #105, #6964, .T. ) ;
#10691=CARTESIAN_POINT ( 'NONE',  ( 0.4591888763630541104, -0.4881889763779528324, 0.3787644491703230365 ) ) ;
#10697=AXIS2_PLACEMENT_3D ( 'NONE', #8938, #1795, #10183 ) ;
#10698=LINE ( 'NONE', #14371, #11869 ) ;
#10699=CARTESIAN_POINT ( 'NONE',  ( 0.1609378808468091004, -0.1023622047244094474, 0.2156612868464037047 ) ) ;
#10701=CARTESIAN_POINT ( 'NONE',  ( 0.4121618538092042261, -0.2952755905511811330, 0.1243101294532688583 ) ) ;
#10702=DIRECTION ( 'NONE',  ( 0.000000000000000000, 0.000000000000000000, 1.000000000000000000 ) ) ;
#10703=ADVANCED_FACE ( 'NONE', ( #14982 ), #3056, .T. ) ;
#10704=AXIS2_PLACEMENT_3D ( 'NONE', #13365, #6151, #10941 ) ;
#10706=CARTESIAN_POINT ( 'NONE',  ( 0.06299212598430634080, -0.2952755905511811885, -0.3757906139821208247 ) ) ;
#10708=ORIENTED_EDGE ( 'NONE', *, *, #3219, .F. ) ;
#10709=ADVANCED_FACE ( 'NONE', ( #14905 ), #7827, .T. ) ;
#10713=AXIS2_PLACEMENT_3D ( 'NONE', #8381, #1101, #5857 ) ;
#10715=CIRCLE ( 'NONE', #961, 0.003937007874015750579 ) ;
#10717=LINE ( 'NONE', #9705, #10889 ) ;
#10718=FACE_OUTER_BOUND ( 'NONE', #3855, .T. ) ;
#10719=DIRECTION ( 'NONE',  ( 0.5000000000000001110, 0.000000000000000000, -0.8660254037844385966 ) ) ;
#10720=EDGE_LOOP ( 'NONE', ( #1141, #11260, #3333, #14165 ) ) ;
#10722=FACE_BOUND ( 'NONE', #9091, .T. ) ;
#10725=VERTEX_POINT ( 'NONE', #1891 ) ;
#10727=ORIENTED_EDGE ( 'NONE', *, *, #5371, .F. ) ;
#10736=ORIENTED_EDGE ( 'NONE', *, *, #6875, .F. ) ;
#10740=CARTESIAN_POINT ( 'NONE',  ( 0.2681506793018588741, -0.1023622047244094474, 0.03207310886168002889 ) ) ;
#10742=EDGE_CURVE ( 'NONE', #6761, #7284, #9484, .T. ) ;
#10743=EDGE_CURVE ( 'NONE', #11638, #8739, #11981, .T. ) ;
#10746=EDGE_CURVE ( 'NONE', #897, #13132, #7955, .T. ) ;
#10747=CARTESIAN_POINT ( 'NONE',  ( -0.06692913385815735250, -0.4881889763779528324, -0.5870514566507987197 ) ) ;
#10749=DIRECTION ( 'NONE',  ( 0.000000000000000000, 0.000000000000000000, 1.000000000000000000 ) ) ;
#10754=DIRECTION ( 'NONE',  ( 0.8660254037844385966, 0.000000000000000000, 0.5000000000000000000 ) ) ;
#10755=DIRECTION ( 'NONE',  ( 3.973232667114494807E-16, -0.000000000000000000, -1.000000000000000000 ) ) ;
#10757=EDGE_CURVE ( 'NONE', #9271, #13131, #8721, .T. ) ;
#10758=DIRECTION ( 'NONE',  ( 1.000000000000000000, 0.000000000000000000, 1.445602896647339903E-16 ) ) ;
#10759=EDGE_CURVE ( 'NONE', #897, #3157, #2712, .T. ) ;
#10760=ORIENTED_EDGE ( 'NONE', *, *, #6196, .T. ) ;
#10764=EDGE_CURVE ( 'NONE', #14809, #1289, #3211, .T. ) ;
#10766=CARTESIAN_POINT ( 'NONE',  ( -0.1023622047242991884, -0.2952755905511811885, -0.3757906139821208802 ) ) ;
#10769=DIRECTION ( 'NONE',  ( 0.000000000000000000, 1.000000000000000000, 0.000000000000000000 ) ) ;
#10771=FACE_OUTER_BOUND ( 'NONE', #9973, .T. ) ;
#10772=PLANE ( 'NONE',  #14889 ) ;
#10773=CARTESIAN_POINT ( 'NONE',  ( 0.4625984251968510708, -0.4881889763779528324, 0.3807329531073309070 ) ) ;
#10775=VERTEX_POINT ( 'NONE', #10196 ) ;
#10776=ORIENTED_EDGE ( 'NONE', *, *, #11015, .T. ) ;
#10777=ORIENTED_EDGE ( 'NONE', *, *, #13532, .F. ) ;
#10778=ORIENTED_EDGE ( 'NONE', *, *, #2261, .T. ) ;
#10779=EDGE_CURVE ( 'NONE', #13855, #2421, #2214, .T. ) ;
#10780=ADVANCED_FACE ( 'NONE', ( #5478 ), #15207, .F. ) ;
#10783=LINE ( 'NONE', #8580, #6668 ) ;
#10788=ORIENTED_EDGE ( 'NONE', *, *, #8214, .T. ) ;
#10790=DIRECTION ( 'NONE',  ( -3.973232667114494807E-16, 0.000000000000000000, 1.000000000000000000 ) ) ;
#10794=ORIENTED_EDGE ( 'NONE', *, *, #1868, .F. ) ;
#10796=CARTESIAN_POINT ( 'NONE',  ( 0.000000000000000000, -0.4921259842519685179, 0.000000000000000000 ) ) ;
#10800=DIRECTION ( 'NONE',  ( 0.000000000000000000, 1.000000000000000000, 0.000000000000000000 ) ) ;
#10807=VERTEX_POINT ( 'NONE', #2269 ) ;
#10808=CARTESIAN_POINT ( 'NONE',  ( 0.1017691531708310448, -0.2952755905511811330, 0.7406662147377752747 ) ) ;
#10810=DIRECTION ( 'NONE',  ( -0.000000000000000000, 1.000000000000000000, -0.000000000000000000 ) ) ;
#10811=CARTESIAN_POINT ( 'NONE',  ( -0.06299212598414161146, -0.4921259842519685179, -0.5870514566507987197 ) ) ;
#10812=DIRECTION ( 'NONE',  ( 0.000000000000000000, 0.000000000000000000, -1.000000000000000000 ) ) ;
#10815=ORIENTED_EDGE ( 'NONE', *, *, #8490, .F. ) ;
#10817=LINE ( 'NONE', #266, #10645 ) ;
#10821=DIRECTION ( 'NONE',  ( 0.5000000000000004441, -0.000000000000000000, -0.8660254037844384856 ) ) ;
#10822=EDGE_LOOP ( 'NONE', ( #10187, #162, #15014 ) ) ;
#10826=FACE_OUTER_BOUND ( 'NONE', #4660, .T. ) ;
#10828=CIRCLE ( 'NONE', #5313, 0.003937007874015750579 ) ;
#10829=AXIS2_PLACEMENT_3D ( 'NONE', #1002, #9221, #2306 ) ;
#10830=FACE_OUTER_BOUND ( 'NONE', #11303, .T. ) ;
#10832=EDGE_CURVE ( 'NONE', #11006, #12201, #7044, .T. ) ;
#10833=VECTOR ( 'NONE', #4933, 39.37007874015748143 ) ;
#10835=DIRECTION ( 'NONE',  ( -0.5000000000000001110, 0.000000000000000000, 0.8660254037844385966 ) ) ;
#10836=EDGE_CURVE ( 'NONE', #2901, #8551, #955, .T. ) ;
#10837=CARTESIAN_POINT ( 'NONE',  ( -0.06299212598414173636, -0.1023622047244094474, -0.2377126739438355507 ) ) ;
#10838=CARTESIAN_POINT ( 'NONE',  ( -0.4307978335858689278, -0.09448818897637796532, 0.4318761856142863120 ) ) ;
#10839=DIRECTION ( 'NONE',  ( -1.000000000000000000, 0.000000000000000000, 0.000000000000000000 ) ) ;
#10842=DIRECTION ( 'NONE',  ( 0.000000000000000000, 0.000000000000000000, 1.000000000000000000 ) ) ;
#10845=ORIENTED_EDGE ( 'NONE', *, *, #11709, .T. ) ;
#10847=VECTOR ( 'NONE', #5567, 39.37007874015748143 ) ;
#10850=ADVANCED_FACE ( 'NONE', ( #8153 ), #14263, .T. ) ;
#10851=CARTESIAN_POINT ( 'NONE',  ( 0.000000000000000000, -0.4881889763779528324, -0.1535433070866141780 ) ) ;
#10853=VECTOR ( 'NONE', #14560, 39.37007874015748143 ) ;
#10854=CIRCLE ( 'NONE', #10353, 0.03937007874015751446 ) ;
#10856=CYLINDRICAL_SURFACE ( 'NONE', #13714, 0.003937007874015749712 ) ;
#10857=DIRECTION ( 'NONE',  ( 0.8660254037844365982, -0.000000000000000000, 0.5000000000000035527 ) ) ;
#10862=CARTESIAN_POINT ( 'NONE',  ( 0.1023622047244638761, -0.2952755905511811330, -0.4190977005962941426 ) ) ;
#10864=DIRECTION ( 'NONE',  ( -0.8660254037844428154, 0.000000000000000000, -0.4999999999999926725 ) ) ;
#10866=CYLINDRICAL_SURFACE ( 'NONE', #9084, 0.03937007874015751446 ) ;
#10868=ORIENTED_EDGE ( 'NONE', *, *, #9538, .T. ) ;
#10869=ORIENTED_EDGE ( 'NONE', *, *, #11860, .T. ) ;
#10871=AXIS2_PLACEMENT_3D ( 'NONE', #6779, #765, #11569 ) ;
#10872=AXIS2_PLACEMENT_3D ( 'NONE', #2170, #13120, #3259 ) ;
#10873=CIRCLE ( 'NONE', #1377, 0.003937007874015721089 ) ;
#10875=EDGE_LOOP ( 'NONE', ( #6056, #4494 ) ) ;
#10876=AXIS2_PLACEMENT_3D ( 'NONE', #9018, #4006, #1888 ) ;
#10879=CARTESIAN_POINT ( 'NONE',  ( 0.06692913385832208184, -0.2952755905511811330, -0.3797276218561366212 ) ) ;
#10881=DIRECTION ( 'NONE',  ( -0.5000000000000000000, -0.000000000000000000, -0.8660254037844388186 ) ) ;
#10882=AXIS2_PLACEMENT_3D ( 'NONE', #14967, #3123, #10488 ) ;
#10884=AXIS2_PLACEMENT_3D ( 'NONE', #14837, #1687, #9043 ) ;
#10888=EDGE_CURVE ( 'NONE', #1202, #12059, #1229, .T. ) ;
#10889=VECTOR ( 'NONE', #13223, 39.37007874015748143 ) ;
#10893=EDGE_CURVE ( 'NONE', #12689, #15156, #445, .T. ) ;
#10894=ADVANCED_FACE ( 'NONE', ( #5777 ), #10570, .T. ) ;
#10896=VERTEX_POINT ( 'NONE', #15 ) ;
#10899=TOROIDAL_SURFACE ( 'NONE', #9916, 0.007874015748031495954, 0.003937007874015747977 ) ;
#10900=DIRECTION ( 'NONE',  ( 1.000000000000000000, 0.000000000000000000, -0.000000000000000000 ) ) ;
#10901=AXIS2_PLACEMENT_3D ( 'NONE', #12811, #3428, #10702 ) ;
#10903=CARTESIAN_POINT ( 'NONE',  ( -0.3964138223131424277, -0.2952755905511811330, 0.1515865201236452631 ) ) ;
#10904=CARTESIAN_POINT ( 'NONE',  ( 0.1618514667033794374, -0.1023622047244094474, 0.2161887458866224576 ) ) ;
#10906=EDGE_LOOP ( 'NONE', ( #14824, #379, #5713, #11213 ) ) ;
#10907=DIRECTION ( 'NONE',  ( 0.000000000000000000, 0.000000000000000000, 1.000000000000000000 ) ) ;
#10908=DIRECTION ( 'NONE',  ( -0.4999999999999967804, -0.000000000000000000, -0.8660254037844405950 ) ) ;
#10912=VECTOR ( 'NONE', #15149, 39.37007874015748143 ) ;
#10913=ORIENTED_EDGE ( 'NONE', *, *, #12678, .T. ) ;
#10916=ORIENTED_EDGE ( 'NONE', *, *, #1778, .T. ) ;
#10922=AXIS2_PLACEMENT_3D ( 'NONE', #4953, #12081, #10907 ) ;
#10924=FACE_OUTER_BOUND ( 'NONE', #3465, .T. ) ;
#10925=LINE ( 'NONE', #15409, #11586 ) ;
#10928=CYLINDRICAL_SURFACE ( 'NONE', #1172, 0.003937007874015758385 ) ;
#10930=VERTEX_POINT ( 'NONE', #15355 ) ;
#10937=EDGE_CURVE ( 'NONE', #6761, #15201, #4620, .T. ) ;
#10938=DIRECTION ( 'NONE',  ( 0.5000000000000069944, 0.000000000000000000, -0.8660254037844347108 ) ) ;
#10941=DIRECTION ( 'NONE',  ( -1.000000000000000000, 0.000000000000000000, 0.000000000000000000 ) ) ;
#10944=CIRCLE ( 'NONE', #1694, 0.04330708661417329020 ) ;
#10947=CARTESIAN_POINT ( 'NONE',  ( -0.06351958502436047538, -0.4921259842519685179, -0.2357441700068276802 ) ) ;
#10948=VERTEX_POINT ( 'NONE', #5707 ) ;
#10955=ORIENTED_EDGE ( 'NONE', *, *, #14997, .T. ) ;
#10957=CARTESIAN_POINT ( 'NONE',  ( -0.3314531923919099565, -0.2952755905511811330, 0.2641016316388978824 ) ) ;
#10960=DIRECTION ( 'NONE',  ( 0.000000000000000000, -1.000000000000000000, -0.000000000000000000 ) ) ;
#10964=AXIS2_PLACEMENT_3D ( 'NONE', #4296, #785, #9089 ) ;
#10968=CARTESIAN_POINT ( 'NONE',  ( -0.3746568166374384945, -0.2952755905511811330, 0.1026565861461826018 ) ) ;
#10972=EDGE_LOOP ( 'NONE', ( #4481, #8435, #5453, #9679 ) ) ;
#10976=DIRECTION ( 'NONE',  ( 0.000000000000000000, 0.000000000000000000, 1.000000000000000000 ) ) ;
#10977=FACE_OUTER_BOUND ( 'NONE', #12305, .T. ) ;
#10988=CARTESIAN_POINT ( 'NONE',  ( 0.4516353949179792160, -0.2952755905511811330, 0.1425541239265584736 ) ) ;
#10992=ORIENTED_EDGE ( 'NONE', *, *, #8063, .F. ) ;
#10996=DIRECTION ( 'NONE',  ( 1.000000000000000000, 0.000000000000000000, 3.075191616504340279E-15 ) ) ;
#10999=DIRECTION ( 'NONE',  ( -0.8660254037844398178, 0.000000000000000000, 0.4999999999999979461 ) ) ;
#11000=CYLINDRICAL_SURFACE ( 'NONE', #1356, 0.003937007874015721089 ) ;
#11003=DIRECTION ( 'NONE',  ( 0.8660254037844390407, 0.000000000000000000, -0.4999999999999990008 ) ) ;
#11005=ORIENTED_EDGE ( 'NONE', *, *, #2020, .F. ) ;
#11006=VERTEX_POINT ( 'NONE', #5149 ) ;
#11011=DIRECTION ( 'NONE',  ( -0.5000000000000000000, 0.000000000000000000, 0.8660254037844385966 ) ) ;
#11015=EDGE_CURVE ( 'NONE', #4061, #7217, #2660, .T. ) ;
#11017=DIRECTION ( 'NONE',  ( -0.8660254037844389297, -0.000000000000000000, 0.4999999999999994449 ) ) ;
#11020=ADVANCED_FACE ( 'NONE', ( #13239 ), #13471, .T. ) ;
#11021=ORIENTED_EDGE ( 'NONE', *, *, #14113, .F. ) ;
#11022=ORIENTED_EDGE ( 'NONE', *, *, #948, .T. ) ;
#11023=EDGE_LOOP ( 'NONE', ( #14589, #12352, #548, #13674 ) ) ;
#11024=ORIENTED_EDGE ( 'NONE', *, *, #3011, .F. ) ;
#11029=DIRECTION ( 'NONE',  ( 4.257580834543280144E-32, 1.000000000000000000, -1.224646799147353207E-16 ) ) ;
#11031=EDGE_CURVE ( 'NONE', #7482, #517, #14737, .T. ) ;
#11032=VERTEX_POINT ( 'NONE', #1492 ) ;
#11035=DIRECTION ( 'NONE',  ( -0.8660254037844388186, 0.000000000000000000, 0.4999999999999995559 ) ) ;
#11036=ORIENTED_EDGE ( 'NONE', *, *, #580, .F. ) ;
#11037=EDGE_CURVE ( 'NONE', #8021, #5345, #1967, .T. ) ;
#11039=ORIENTED_EDGE ( 'NONE', *, *, #1175, .F. ) ;
#11040=LINE ( 'NONE', #2748, #14366 ) ;
#11041=LINE ( 'NONE', #2583, #633 ) ;
#11042=DIRECTION ( 'NONE',  ( 0.000000000000000000, 0.000000000000000000, -1.000000000000000000 ) ) ;
#11044=ADVANCED_FACE ( 'NONE', ( #14498 ), #9869, .T. ) ;
#11049=DIRECTION ( 'NONE',  ( 0.8660254037844390407, 0.000000000000000000, -0.4999999999999994449 ) ) ;
#11051=DIRECTION ( 'NONE',  ( 0.4999999999999922284, -0.000000000000000000, -0.8660254037844430375 ) ) ;
#11052=ADVANCED_FACE ( 'NONE', ( #10178 ), #1724, .T. ) ;
#11053=ORIENTED_EDGE ( 'NONE', *, *, #11335, .F. ) ;
#11057=CARTESIAN_POINT ( 'NONE',  ( 0.1724006475077543565, -0.09842519685039370636, 0.1768186671464649640 ) ) ;
#11058=CARTESIAN_POINT ( 'NONE',  ( -0.1574803149606299191, -0.003937007874015747977, -0.5909884645248143498 ) ) ;
#11059=DIRECTION ( 'NONE',  ( 1.000000000000000000, 0.000000000000000000, 0.000000000000000000 ) ) ;
#11064=CARTESIAN_POINT ( 'NONE',  ( -0.4307978335858689278, -0.003937007874015747977, 0.4318761856142863120 ) ) ;
#11065=LINE ( 'NONE', #10450, #13358 ) ;
#11066=CARTESIAN_POINT ( 'NONE',  ( 0.2686781383420775993, -0.1023622047244094474, 0.03298669471825042832 ) ) ;
#11074=CIRCLE ( 'NONE', #3596, 0.007874015748031482076 ) ;
#11076=DIRECTION ( 'NONE',  ( -0.000000000000000000, 1.000000000000000000, 0.000000000000000000 ) ) ;
#11078=DIRECTION ( 'NONE',  ( 0.000000000000000000, -1.000000000000000000, -0.000000000000000000 ) ) ;
#11079=DIRECTION ( 'NONE',  ( 0.000000000000000000, -1.000000000000000000, 0.000000000000000000 ) ) ;
#11080=DIRECTION ( 'NONE',  ( 0.000000000000000000, 0.000000000000000000, 1.000000000000000000 ) ) ;
#11081=LINE ( 'NONE', #6063, #12825 ) ;
#11082=CIRCLE ( 'NONE', #15348, 0.007874015748031504627 ) ;
#11083=DIRECTION ( 'NONE',  ( 0.000000000000000000, 1.734723475976802677E-14, 1.000000000000000000 ) ) ;
#11087=AXIS2_PLACEMENT_3D ( 'NONE', #10054, #1686, #3872 ) ;
#11088=ORIENTED_EDGE ( 'NONE', *, *, #2538, .T. ) ;
#11095=CIRCLE ( 'NONE', #12359, 0.007874015748031501158 ) ;
#11096=AXIS2_PLACEMENT_3D ( 'NONE', #11435, #7905, #4369 ) ;
#11101=DIRECTION ( 'NONE',  ( -0.8660254037844385966, 0.000000000000000000, 0.5000000000000001110 ) ) ;
#11107=DIRECTION ( 'NONE',  ( 0.8660254037844385966, 0.000000000000000000, -0.4999999999999998890 ) ) ;
#11109=CIRCLE ( 'NONE', #15162, 0.003937007874015746242 ) ;
#11110=AXIS2_PLACEMENT_3D ( 'NONE', #3430, #8205, #5587 ) ;
#11112=VECTOR ( 'NONE', #9083, 39.37007874015748143 ) ;
#11115=ORIENTED_EDGE ( 'NONE', *, *, #142, .T. ) ;
#11116=AXIS2_PLACEMENT_3D ( 'NONE', #2449, #7225, #6025 ) ;
#11118=ORIENTED_EDGE ( 'NONE', *, *, #11623, .F. ) ;
#11120=CIRCLE ( 'NONE', #12384, 0.04330708661417330407 ) ;
#11130=CARTESIAN_POINT ( 'NONE',  ( -0.3706061991976995484, -0.09842519685039370636, -0.2139695888701363957 ) ) ;
#11132=DIRECTION ( 'NONE',  ( 0.000000000000000000, 0.000000000000000000, -1.000000000000000000 ) ) ;
#11134=CARTESIAN_POINT ( 'NONE',  ( 0.04921259842519617317, -0.4881889763779528324, 0.08523872084492387091 ) ) ;
#11135=VECTOR ( 'NONE', #4692, 39.37007874015748143 ) ;
#11141=EDGE_LOOP ( 'NONE', ( #13821, #7136, #12906, #10533 ) ) ;
#11144=ADVANCED_FACE ( 'NONE', ( #5528 ), #12532, .T. ) ;
#11145=CARTESIAN_POINT ( 'NONE',  ( -0.04921259842519618705, -0.4881889763779528324, 0.08523872084492388479 ) ) ;
#11146=CARTESIAN_POINT ( 'NONE',  ( -0.1552072824047653066, -0.09842519685039370636, -0.5870514566507987197 ) ) ;
#11148=AXIS2_PLACEMENT_3D ( 'NONE', #14761, #7702, #340 ) ;
#11151=CARTESIAN_POINT ( 'NONE',  ( -0.1062992125983148878, -0.1023622047244094474, -0.5870514566507987197 ) ) ;
#11152=VECTOR ( 'NONE', #9759, 39.37007874015748143 ) ;
#11153=CARTESIAN_POINT ( 'NONE',  ( 0.2661821753648509481, -0.4881889763779528324, 0.03548265769547701703 ) ) ;
#11154=FACE_BOUND ( 'NONE', #12656, .T. ) ;
#11155=CARTESIAN_POINT ( 'NONE',  ( 0.000000000000000000, -0.09842519685039370636, 0.000000000000000000 ) ) ;
#11156=VECTOR ( 'NONE', #14517, 39.37007874015748143 ) ;
#11157=DIRECTION ( 'NONE',  ( 0.000000000000000000, 0.000000000000000000, 1.000000000000000000 ) ) ;
#11158=EDGE_LOOP ( 'NONE', ( #5228, #9604, #13716, #11326 ) ) ;
#11159=ORIENTED_EDGE ( 'NONE', *, *, #1538, .F. ) ;
#11162=ORIENTED_EDGE ( 'NONE', *, *, #10199, .T. ) ;
#11163=AXIS2_PLACEMENT_3D ( 'NONE', #13731, #6654, #6497 ) ;
#11171=DIRECTION ( 'NONE',  ( 0.000000000000000000, 0.000000000000000000, 1.000000000000000000 ) ) ;
#11173=EDGE_CURVE ( 'NONE', #6881, #4497, #11269, .T. ) ;
#11176=DIRECTION ( 'NONE',  ( -0.4999999999999979461, 0.000000000000000000, -0.8660254037844398178 ) ) ;
#11178=ORIENTED_EDGE ( 'NONE', *, *, #9270, .T. ) ;
#11179=ORIENTED_EDGE ( 'NONE', *, *, #15185, .T. ) ;
#11180=VECTOR ( 'NONE', #8012, 39.37007874015748854 ) ;
#11181=ORIENTED_EDGE ( 'NONE', *, *, #15301, .T. ) ;
#11184=ORIENTED_EDGE ( 'NONE', *, *, #3831, .F. ) ;
#11186=DIRECTION ( 'NONE',  ( 0.8660254037844387076, 0.000000000000000000, 0.5000000000000001110 ) ) ;
#11191=CARTESIAN_POINT ( 'NONE',  ( -0.06692913385815735250, -0.4921259842519685179, -0.5909884645248143498 ) ) ;
#11193=VECTOR ( 'NONE', #14279, 39.37007874015748143 ) ;
#11194=CARTESIAN_POINT ( 'NONE',  ( -0.4307978335858689833, -0.003937007874015747977, 0.4279391777402706265 ) ) ;
#11197=ORIENTED_EDGE ( 'NONE', *, *, #10779, .T. ) ;
#11198=DIRECTION ( 'NONE',  ( 0.000000000000000000, 1.000000000000000000, 0.000000000000000000 ) ) ;
#11199=EDGE_CURVE ( 'NONE', #10309, #10256, #5956, .T. ) ;
#11204=ORIENTED_EDGE ( 'NONE', *, *, #8008, .T. ) ;
#11207=AXIS2_PLACEMENT_3D ( 'NONE', #12843, #6494, #12620 ) ;
#11210=AXIS2_PLACEMENT_3D ( 'NONE', #6285, #13220, #7258 ) ;
#11211=CARTESIAN_POINT ( 'NONE',  ( 0.06692913385832209572, -0.4881889763779528324, -0.2377126739437405434 ) ) ;
#11212=CARTESIAN_POINT ( 'NONE',  ( 0.06299212598430639631, -0.4881889763779528324, -0.5870514566507987197 ) ) ;
#11213=ORIENTED_EDGE ( 'NONE', *, *, #5192, .T. ) ;
#11214=EDGE_CURVE ( 'NONE', #777, #2454, #4284, .T. ) ;
#11215=FACE_OUTER_BOUND ( 'NONE', #7316, .T. ) ;
#11216=CARTESIAN_POINT ( 'NONE',  ( -0.5905511811023629321, -0.09448818897637796532, 0.1591122789105256785 ) ) ;
#11217=CYLINDRICAL_SURFACE ( 'NONE', #2146, 0.003937007874015749712 ) ;
#11225=EDGE_LOOP ( 'NONE', ( #7037, #13085, #1628, #10708 ) ) ;
#11228=CARTESIAN_POINT ( 'NONE',  ( -0.3623183339751723242, -0.2952755905511811330, 0.1319014807535664191 ) ) ;
#11237=EDGE_CURVE ( 'NONE', #8301, #3987, #14077, .T. ) ;
#11240=VERTEX_POINT ( 'NONE', #5836 ) ;
#11244=CARTESIAN_POINT ( 'NONE',  ( 0.1028896637646825596, -0.4881889763779528324, -0.2462933508111075365 ) ) ;
#11249=DIRECTION ( 'NONE',  ( 0.000000000000000000, 0.000000000000000000, -1.000000000000000000 ) ) ;
#11251=ADVANCED_FACE ( 'NONE', ( #10718 ), #11751, .F. ) ;
#11255=ORIENTED_EDGE ( 'NONE', *, *, #14195, .T. ) ;
#11258=ORIENTED_EDGE ( 'NONE', *, *, #9429, .F. ) ;
#11260=ORIENTED_EDGE ( 'NONE', *, *, #13152, .F. ) ;
#11264=DIRECTION ( 'NONE',  ( -0.5000000000000059952, 0.000000000000000000, 0.8660254037844351549 ) ) ;
#11267=FACE_OUTER_BOUND ( 'NONE', #6118, .T. ) ;
#11269=LINE ( 'NONE', #12759, #9227 ) ;
#11271=EDGE_LOOP ( 'NONE', ( #1346, #3243, #7630, #4170 ) ) ;
#11273=LINE ( 'NONE', #8845, #5950 ) ;
#11274=ORIENTED_EDGE ( 'NONE', *, *, #4229, .T. ) ;
#11275=ORIENTED_EDGE ( 'NONE', *, *, #1501, .T. ) ;
#11278=EDGE_CURVE ( 'NONE', #7659, #4124, #4316, .T. ) ;
#11280=LINE ( 'NONE', #14813, #13209 ) ;
#11286=DIRECTION ( 'NONE',  ( 0.000000000000000000, -1.000000000000000000, 0.000000000000000000 ) ) ;
#11287=CARTESIAN_POINT ( 'NONE',  ( -0.1552072824047652788, -0.003937007874015747977, -0.5870514566507987197 ) ) ;
#11288=ORIENTED_EDGE ( 'NONE', *, *, #5315, .F. ) ;
#11291=APPLICATION_CONTEXT ( 'automotive_design' ) ;
#11294=CARTESIAN_POINT ( 'NONE',  ( -0.06299212598414161146, -0.1023622047244094474, -0.5909884645248154600 ) ) ;
#11297=CARTESIAN_POINT ( 'NONE',  ( -0.1062992125983148878, -0.1023622047244094474, -0.5870514566507987197 ) ) ;
#11298=DIRECTION ( 'NONE',  ( 0.4999999999999798495, 0.000000000000000000, -0.8660254037844501429 ) ) ;
#11303=EDGE_LOOP ( 'NONE', ( #4853, #9505, #11979, #11547 ) ) ;
#11305=VERTEX_POINT ( 'NONE', #9237 ) ;
#11308=DIRECTION ( 'NONE',  ( 0.4999999999999966693, 0.000000000000000000, 0.8660254037844405950 ) ) ;
#11310=( LENGTH_UNIT ( ) NAMED_UNIT ( * ) SI_UNIT ( $, .METRE. ) );
#11312=EDGE_CURVE ( 'NONE', #4031, #13771, #1819, .T. ) ;
#11315=DIRECTION ( 'NONE',  ( 0.000000000000000000, -0.000000000000000000, 1.000000000000000000 ) ) ;
#11319=AXIS2_PLACEMENT_3D ( 'NONE', #1312, #153, #4913 ) ;
#11320=ORIENTED_EDGE ( 'NONE', *, *, #11434, .T. ) ;
#11321=AXIS2_PLACEMENT_3D ( 'NONE', #2416, #7194, #2783 ) ;
#11323=ORIENTED_EDGE ( 'NONE', *, *, #3019, .T. ) ;
#11324=VERTEX_POINT ( 'NONE', #14010 ) ;
#11326=ORIENTED_EDGE ( 'NONE', *, *, #8473, .F. ) ;
#11327=ADVANCED_FACE ( 'NONE', ( #12994 ), #5760, .T. ) ;
#11328=CARTESIAN_POINT ( 'NONE',  ( 0.5615510810874363434, -0.1023622047244094474, 0.2014679098129276147 ) ) ;
#11329=DIRECTION ( 'NONE',  ( 0.4999999999999979461, 0.000000000000000000, 0.8660254037844398178 ) ) ;
#11330=TOROIDAL_SURFACE ( 'NONE', #11853, 0.1614173228346456879, 0.003937007874015747977 ) ;
#11332=CARTESIAN_POINT ( 'NONE',  ( 0.04921259842519613847, -0.4921259842519685179, 0.08523872084492380152 ) ) ;
#11333=AXIS2_PLACEMENT_3D ( 'NONE', #15129, #9257, #9096 ) ;
#11335=EDGE_CURVE ( 'NONE', #10948, #9186, #11081, .T. ) ;
#11336=CARTESIAN_POINT ( 'NONE',  ( 0.4749369078591172411, -0.1023622047244094474, 0.3514880584999470203 ) ) ;
#11337=AXIS2_PLACEMENT_3D ( 'NONE', #14965, #9007, #12368 ) ;
#11339=DIRECTION ( 'NONE',  ( 0.000000000000000000, 0.000000000000000000, 1.000000000000000000 ) ) ;
#11340=DIRECTION ( 'NONE',  ( -0.000000000000000000, -1.000000000000000000, 0.000000000000000000 ) ) ;
#11346=ORIENTED_EDGE ( 'NONE', *, *, #2182, .T. ) ;
#11348=ORIENTED_EDGE ( 'NONE', *, *, #3447, .F. ) ;
#11349=CIRCLE ( 'NONE', #14103, 0.003937007874015724558 ) ;
#11350=VECTOR ( 'NONE', #9338, 39.37007874015748143 ) ;
#11351=CIRCLE ( 'NONE', #6332, 0.1535433070866141780 ) ;
#11352=VECTOR ( 'NONE', #2992, 39.37007874015748143 ) ;
#11354=CARTESIAN_POINT ( 'NONE',  ( -0.5084014747882513729, -0.09842519685039370636, 0.2935257283253980831 ) ) ;
#11356=CARTESIAN_POINT ( 'NONE',  ( -0.5905511811023629321, -0.003937007874015747977, 0.1591122789105256785 ) ) ;
#11358=DIRECTION ( 'NONE',  ( -0.000000000000000000, 0.000000000000000000, 1.000000000000000000 ) ) ;
#11359=CIRCLE ( 'NONE', #12621, 0.003937007874015747977 ) ;
#11360=LINE ( 'NONE', #12546, #10141 ) ;
#11362=DIRECTION ( 'NONE',  ( 0.5000000000000008882, -0.000000000000000000, -0.8660254037844380415 ) ) ;
#11375=ORIENTED_EDGE ( 'NONE', *, *, #39, .T. ) ;
#11378=VECTOR ( 'NONE', #13181, 39.37007874015748143 ) ;
#11379=CARTESIAN_POINT ( 'NONE',  ( -0.1618514667033795484, -0.1023622047244094474, 0.2161887458866224576 ) ) ;
#11386=DIRECTION ( 'NONE',  ( 0.000000000000000000, 0.000000000000000000, -1.000000000000000000 ) ) ;
#11389=CARTESIAN_POINT ( 'NONE',  ( 0.1763376553817700698, -0.1023622047244094474, 0.1699995694788709322 ) ) ;
#11393=AXIS2_PLACEMENT_3D ( 'NONE', #8827, #11186, #1717 ) ;
#11394=LINE ( 'NONE', #1828, #6154 ) ;
#11395=TOROIDAL_SURFACE ( 'NONE', #2379, 0.04330708661417328326, 0.003937007874015747977 ) ;
#11398=ORIENTED_EDGE ( 'NONE', *, *, #8287, .F. ) ;
#11411=CARTESIAN_POINT ( 'NONE',  ( -0.5595825771504281398, -0.1023622047244094474, 0.2048774586467239645 ) ) ;
#11412=DIRECTION ( 'NONE',  ( -0.000000000000000000, 1.000000000000000000, 0.000000000000000000 ) ) ;
#11416=ORIENTED_EDGE ( 'NONE', *, *, #5038, .T. ) ;
#11420=EDGE_CURVE ( 'NONE', #1499, #8246, #2549, .T. ) ;
#11421=DIRECTION ( 'NONE',  ( 0.5000000000000014433, -0.000000000000000000, -0.8660254037844378194 ) ) ;
#11427=DIRECTION ( 'NONE',  ( 0.000000000000000000, 0.000000000000000000, -1.000000000000000000 ) ) ;
#11428=DIRECTION ( 'NONE',  ( -0.000000000000000000, -1.000000000000000000, -0.000000000000000000 ) ) ;
#11429=DIRECTION ( 'NONE',  ( 0.000000000000000000, 0.000000000000000000, -1.000000000000000000 ) ) ;
#11430=CIRCLE ( 'NONE', #12687, 0.003937007874015743640 ) ;
#11434=EDGE_CURVE ( 'NONE', #4524, #9377, #2820, .T. ) ;
#11435=CARTESIAN_POINT ( 'NONE',  ( 0.1062992125984796865, -0.1023622047244094474, -0.5909884645248143498 ) ) ;
#11436=AXIS2_PLACEMENT_3D ( 'NONE', #4178, #1753, #3006 ) ;
#11437=EDGE_CURVE ( 'NONE', #10323, #12947, #6555, .T. ) ;
#11444=VECTOR ( 'NONE', #846, 39.37007874015748143 ) ;
#11446=AXIS2_PLACEMENT_3D ( 'NONE', #976, #4646, #9437 ) ;
#11449=CARTESIAN_POINT ( 'NONE',  ( 0.000000000000000000, 0.003937007874015860734, -0.1614173228346456879 ) ) ;
#11452=VERTEX_POINT ( 'NONE', #13289 ) ;
#11455=CIRCLE ( 'NONE', #2196, 0.04330708661417329020 ) ;
#11458=ORIENTED_EDGE ( 'NONE', *, *, #1125, .T. ) ;
#11459=CYLINDRICAL_SURFACE ( 'NONE', #6165, 0.003937007874015721089 ) ;
#11460=ORIENTED_EDGE ( 'NONE', *, *, #8442, .F. ) ;
#11464=CIRCLE ( 'NONE', #7699, 0.1614173228346456879 ) ;
#11465=VERTEX_POINT ( 'NONE', #14402 ) ;
#11466=CARTESIAN_POINT ( 'NONE',  ( 0.1629063847838169432, -0.4921259842519685179, 0.2122517380126066888 ) ) ;
#11467=CARTESIAN_POINT ( 'NONE',  ( 0.000000000000000000, -0.4881889763779528324, 0.1768186671464649640 ) ) ;
#11469=EDGE_CURVE ( 'NONE', #15156, #13856, #3976, .T. ) ;
#11477=DIRECTION ( 'NONE',  ( -0.5000000000000001110, 0.000000000000000000, 0.8660254037844388186 ) ) ;
#11478=CARTESIAN_POINT ( 'NONE',  ( -0.4769054117961255002, -0.4921259842519685179, 0.3480785096661502265 ) ) ;
#11479=AXIS2_PLACEMENT_3D ( 'NONE', #554, #10266, #4157 ) ;
#11481=AXIS2_PLACEMENT_3D ( 'NONE', #12576, #4264, #5441 ) ;
#11482=ORIENTED_EDGE ( 'NONE', *, *, #15461, .T. ) ;
#11483=FACE_OUTER_BOUND ( 'NONE', #6808, .T. ) ;
#11487=DIRECTION ( 'NONE',  ( -0.000000000000000000, -1.000000000000000000, -0.000000000000000000 ) ) ;
#11490=CYLINDRICAL_SURFACE ( 'NONE', #5072, 0.003937007874015724558 ) ;
#11492=LINE ( 'NONE', #2957, #6556 ) ;
#11494=ORIENTED_EDGE ( 'NONE', *, *, #6921, .F. ) ;
#11500=EDGE_CURVE ( 'NONE', #4812, #6947, #1575, .T. ) ;
#11506=ORIENTED_EDGE ( 'NONE', *, *, #3679, .T. ) ;
#11508=EDGE_CURVE ( 'NONE', #13903, #10948, #3580, .T. ) ;
#11509=CARTESIAN_POINT ( 'NONE',  ( 0.000000000000000000, 2.161417322834645827, 0.000000000000000000 ) ) ;
#11511=ORIENTED_EDGE ( 'NONE', *, *, #14413, .F. ) ;
#11514=CARTESIAN_POINT ( 'NONE',  ( 0.2364476915724980366, -0.4881889763779528324, 0.06377609659104091500 ) ) ;
#11515=EDGE_CURVE ( 'NONE', #6947, #6576, #10003, .T. ) ;
#11516=EDGE_CURVE ( 'NONE', #12255, #13377, #14341, .T. ) ;
#11517=LINE ( 'NONE', #2985, #5847 ) ;
#11518=CARTESIAN_POINT ( 'NONE',  ( 0.4749369078591172966, -0.4921259842519685179, 0.3514880584999470203 ) ) ;
#11519=DIRECTION ( 'NONE',  ( -1.000000000000000000, 0.000000000000000000, 0.000000000000000000 ) ) ;
#11520=CARTESIAN_POINT ( 'NONE',  ( 0.2393297813660762718, -0.1023622047244094474, 0.06089400679746260342 ) ) ;
#11521=EDGE_LOOP ( 'NONE', ( #13880, #403, #8681 ) ) ;
#11523=EDGE_CURVE ( 'NONE', #7254, #12443, #7957, .T. ) ;
#11525=DIRECTION ( 'NONE',  ( 0.000000000000000000, 1.000000000000000000, 0.000000000000000000 ) ) ;
#11529=VERTEX_POINT ( 'NONE', #12513 ) ;
#11530=ORIENTED_EDGE ( 'NONE', *, *, #5675, .T. ) ;
#11534=CARTESIAN_POINT ( 'NONE',  ( -0.1023622047242992716, -0.09842519685039372024, -0.2482618547482104143 ) ) ;
#11535=EDGE_CURVE ( 'NONE', #6985, #12201, #6820, .T. ) ;
#11541=CARTESIAN_POINT ( 'NONE',  ( -0.1618514667033796040, -0.1023622047244094474, 0.2161887458866224576 ) ) ;
#11547=ORIENTED_EDGE ( 'NONE', *, *, #9028, .F. ) ;
#11549=CARTESIAN_POINT ( 'NONE',  ( -0.5610236220472173407, -0.4921259842519685179, 0.2102555114175287954 ) ) ;
#11553=DIRECTION ( 'NONE',  ( 0.000000000000000000, 0.000000000000000000, -1.000000000000000000 ) ) ;
#11555=DIMENSIONAL_EXPONENTS ( 1.000000000000000000, 0.000000000000000000, 0.000000000000000000, 0.000000000000000000, 0.000000000000000000, 0.000000000000000000, 0.000000000000000000 ) ;
#11559=DIRECTION ( 'NONE',  ( 0.000000000000000000, 1.000000000000000000, 0.000000000000000000 ) ) ;
#11562=ORIENTED_EDGE ( 'NONE', *, *, #15076, .T. ) ;
#11566=ORIENTED_EDGE ( 'NONE', *, *, #14082, .F. ) ;
#11569=DIRECTION ( 'NONE',  ( 0.000000000000000000, 0.000000000000000000, -1.000000000000000000 ) ) ;
#11571=DIRECTION ( 'NONE',  ( 1.000000000000000000, 0.000000000000000000, 0.000000000000000000 ) ) ;
#11572=LINE ( 'NONE', #9476, #2136 ) ;
#11573=DIRECTION ( 'NONE',  ( -1.000000000000000000, -0.000000000000000000, -0.000000000000000000 ) ) ;
#11578=DIRECTION ( 'NONE',  ( 0.000000000000000000, -1.000000000000000000, 0.000000000000000000 ) ) ;
#11582=CIRCLE ( 'NONE', #6064, 0.003937007874015743640 ) ;
#11586=VECTOR ( 'NONE', #14301, 39.37007874015748143 ) ;
#11587=DIRECTION ( 'NONE',  ( 0.5000000000000035527, 0.000000000000000000, -0.8660254037844365982 ) ) ;
#11595=AXIS2_PLACEMENT_3D ( 'NONE', #2635, #62, #13219 ) ;
#11597=PLANE ( 'NONE',  #8968 ) ;
#11598=SPHERICAL_SURFACE ( 'NONE', #11333, 0.003937007874015747977 ) ;
#11599=VERTEX_POINT ( 'NONE', #7724 ) ;
#11604=EDGE_CURVE ( 'NONE', #6660, #12429, #10828, .T. ) ;
#11605=VERTEX_POINT ( 'NONE', #1771 ) ;
#11612=CIRCLE ( 'NONE', #9109, 0.003937007874015741038 ) ;
#11613=CARTESIAN_POINT ( 'NONE',  ( 0.06299212598430636856, -0.2952755905511811330, -0.4624047872104674606 ) ) ;
#11615=CIRCLE ( 'NONE', #13369, 0.003937007874015754916 ) ;
#11618=DIRECTION ( 'NONE',  ( -3.075191616504340279E-15, 0.000000000000000000, 1.000000000000000000 ) ) ;
#11620=ORIENTED_EDGE ( 'NONE', *, *, #9992, .F. ) ;
#11621=DIRECTION ( 'NONE',  ( 0.000000000000000000, 0.000000000000000000, -1.000000000000000000 ) ) ;
#11622=CARTESIAN_POINT ( 'NONE',  ( -0.2652685895081163259, -0.1023622047244094474, 0.03495519865516327068 ) ) ;
#11623=EDGE_CURVE ( 'NONE', #3451, #10948, #14946, .T. ) ;
#11626=VECTOR ( 'NONE', #806, 39.37007874015748143 ) ;
#11627=VECTOR ( 'NONE', #9208, 39.37007874015748143 ) ;
#11628=CIRCLE ( 'NONE', #5099, 0.003937007874015724558 ) ;
#11629=ADVANCED_FACE ( 'NONE', ( #1930 ), #11490, .T. ) ;
#11630=VECTOR ( 'NONE', #15203, 39.37007874015748143 ) ;
#11631=EDGE_LOOP ( 'NONE', ( #11375, #4921, #9400, #4959 ) ) ;
#11632=AXIS2_PLACEMENT_3D ( 'NONE', #9086, #13865, #15115 ) ;
#11633=CYLINDRICAL_SURFACE ( 'NONE', #1064, 0.03937007874015751446 ) ;
#11634=VERTEX_POINT ( 'NONE', #4037 ) ;
#11635=CIRCLE ( 'NONE', #8130, 0.1614173228346456879 ) ;
#11636=ORIENTED_EDGE ( 'NONE', *, *, #8843, .T. ) ;
#11637=EDGE_CURVE ( 'NONE', #3832, #4717, #14598, .T. ) ;
#11638=VERTEX_POINT ( 'NONE', #9056 ) ;
#11642=AXIS2_PLACEMENT_3D ( 'NONE', #14519, #7233, #14284 ) ;
#11644=VECTOR ( 'NONE', #3036, 39.37007874015748143 ) ;
#11649=VERTEX_POINT ( 'NONE', #3186 ) ;
#11652=ORIENTED_EDGE ( 'NONE', *, *, #5861, .F. ) ;
#11653=CIRCLE ( 'NONE', #9900, 0.003937007874015750579 ) ;
#11654=CIRCLE ( 'NONE', #13654, 0.007874015748031501158 ) ;
#11656=EDGE_CURVE ( 'NONE', #9755, #2740, #10595, .T. ) ;
#11657=AXIS2_PLACEMENT_3D ( 'NONE', #6062, #3742, #14628 ) ;
#11658=CARTESIAN_POINT ( 'NONE',  ( 0.000000000000000000, -0.1023622047244094474, 0.000000000000000000 ) ) ;
#11661=DIRECTION ( 'NONE',  ( 0.5000000000000002220, 0.000000000000000000, -0.8660254037844384856 ) ) ;
#11665=DIRECTION ( 'NONE',  ( 0.4999999999999975575, 0.000000000000000000, 0.8660254037844399289 ) ) ;
#11668=AXIS2_PLACEMENT_3D ( 'NONE', #4189, #6369, #14840 ) ;
#11669=VERTEX_POINT ( 'NONE', #1843 ) ;
#11670=CARTESIAN_POINT ( 'NONE',  ( 0.1724006475077543565, -0.1023622047244094474, 0.1768186671464649640 ) ) ;
#11673=CIRCLE ( 'NONE', #14683, 0.003937007874015741038 ) ;
#11678=AXIS2_PLACEMENT_3D ( 'NONE', #9444, #810, #8186 ) ;
#11680=CIRCLE ( 'NONE', #4425, 0.003937007874015724558 ) ;
#11681=CARTESIAN_POINT ( 'NONE',  ( -0.4591888763630547210, -0.4921259842519685179, 0.3787644491703232585 ) ) ;
#11682=ADVANCED_FACE ( 'NONE', ( #13584 ), #6287, .T. ) ;
#11687=ORIENTED_EDGE ( 'NONE', *, *, #13553, .T. ) ;
#11688=DIRECTION ( 'NONE',  ( 0.8660254037844399289, 0.000000000000000000, 0.4999999999999975575 ) ) ;
#11690=TOROIDAL_SURFACE ( 'NONE', #2423, 0.04330708661417328326, 0.003937007874015747977 ) ;
#11692=FACE_OUTER_BOUND ( 'NONE', #2110, .T. ) ;
#11697=AXIS2_PLACEMENT_3D ( 'NONE', #3241, #2933, #3162 ) ;
#11698=VERTEX_POINT ( 'NONE', #7723 ) ;
#11699=EDGE_LOOP ( 'NONE', ( #13694, #3967, #2433, #15253 ) ) ;
#11700=DIRECTION ( 'NONE',  ( 0.4999999999999975575, 0.000000000000000000, 0.8660254037844399289 ) ) ;
#11701=CARTESIAN_POINT ( 'NONE',  ( 0.4749369078591172411, -0.09842519685039370636, 0.3514880584999470203 ) ) ;
#11702=AXIS2_PLACEMENT_3D ( 'NONE', #6740, #4632, #3466 ) ;
#11709=EDGE_CURVE ( 'NONE', #8494, #6177, #370, .T. ) ;
#11713=FACE_OUTER_BOUND ( 'NONE', #9307, .T. ) ;
#11714=DIRECTION ( 'NONE',  ( 3.942553354492736135E-16, 0.000000000000000000, -1.000000000000000000 ) ) ;
#11715=DIRECTION ( 'NONE',  ( 0.000000000000000000, -1.000000000000000000, 0.000000000000000000 ) ) ;
#11719=AXIS2_PLACEMENT_3D ( 'NONE', #14944, #7874, #14850 ) ;
#11721=CARTESIAN_POINT ( 'NONE',  ( -0.04921259842519618705, -0.4921259842519685179, 0.08523872084492388479 ) ) ;
#11723=AXIS2_PLACEMENT_3D ( 'NONE', #2504, #6090, #3610 ) ;
#11724=ORIENTED_EDGE ( 'NONE', *, *, #7416, .T. ) ;
#11725=ORIENTED_EDGE ( 'NONE', *, *, #10759, .F. ) ;
#11727=CARTESIAN_POINT ( 'NONE',  ( 0.1618514667033794374, -0.4921259842519685179, 0.2083147301385909200 ) ) ;
#11731=CARTESIAN_POINT ( 'NONE',  ( -0.05905511811012607165, -0.09842519685039370636, -2.134256245046224357E-17 ) ) ;
#11734=DIRECTION ( 'NONE',  ( 0.000000000000000000, 0.000000000000000000, -1.000000000000000000 ) ) ;
#11735=CYLINDRICAL_SURFACE ( 'NONE', #4147, 0.003937007874015741038 ) ;
#11738=CIRCLE ( 'NONE', #5960, 0.003937007874015758385 ) ;
#11740=CYLINDRICAL_SURFACE ( 'NONE', #3836, 0.003937007874015724558 ) ;
#11741=DIRECTION ( 'NONE',  ( -1.060575238724906792E-16, 1.000000000000000000, 6.123233995736767268E-17 ) ) ;
#11742=EDGE_LOOP ( 'NONE', ( #14434, #2381, #2309, #13601 ) ) ;
#11744=ORIENTED_EDGE ( 'NONE', *, *, #6946, .T. ) ;
#11745=EDGE_LOOP ( 'NONE', ( #5878, #7542, #15131, #7252 ) ) ;
#11751=CYLINDRICAL_SURFACE ( 'NONE', #3819, 0.003937007874015743640 ) ;
#11754=DIRECTION ( 'NONE',  ( -1.000000000000000000, -0.000000000000000000, -3.476578583725179813E-16 ) ) ;
#11756=CARTESIAN_POINT ( 'NONE',  ( -0.06692913385815731087, -0.2952755905511811330, -0.3757906139821208247 ) ) ;
#11760=ADVANCED_FACE ( 'NONE', ( #9135 ), #2001, .T. ) ;
#11762=DIRECTION ( 'NONE',  ( 1.060575238724906792E-16, 1.000000000000000000, -6.123233995736764803E-17 ) ) ;
#11763=DIRECTION ( 'NONE',  ( 0.000000000000000000, 0.000000000000000000, -1.000000000000000000 ) ) ;
#11768=VERTEX_POINT ( 'NONE', #2950 ) ;
#11770=CARTESIAN_POINT ( 'NONE',  ( 0.1023622047244639455, -0.1023622047244094474, -0.5870514566507987197 ) ) ;
#11772=ORIENTED_EDGE ( 'NONE', *, *, #5756, .F. ) ;
#11774=ORIENTED_EDGE ( 'NONE', *, *, #3386, .T. ) ;
#11775=ADVANCED_FACE ( 'NONE', ( #6603 ), #10338, .F. ) ;
#11776=ORIENTED_EDGE ( 'NONE', *, *, #1117, .F. ) ;
#11780=DIRECTION ( 'NONE',  ( 1.000000000000000000, 0.000000000000000000, 0.000000000000000000 ) ) ;
#11781=CARTESIAN_POINT ( 'NONE',  ( 0.1638199706403873079, -0.4881889763779528324, 0.2127791970528254417 ) ) ;
#11782=DIRECTION ( 'NONE',  ( 1.000000000000000000, 0.000000000000000000, 1.445602896647339903E-16 ) ) ;
#11784=CARTESIAN_POINT ( 'NONE',  ( -0.05905511811012598145, -0.09842519685039370636, -0.2377126739438355507 ) ) ;
#11786=ORIENTED_EDGE ( 'NONE', *, *, #2044, .T. ) ;
#11789=DIRECTION ( 'NONE',  ( 0.000000000000000000, 0.000000000000000000, 1.000000000000000000 ) ) ;
#11791=LINE ( 'NONE', #15310, #12692 ) ;
#11794=ORIENTED_EDGE ( 'NONE', *, *, #8166, .T. ) ;
#11795=DIRECTION ( 'NONE',  ( 1.971276677246368068E-16, 0.000000000000000000, -1.000000000000000000 ) ) ;
#11800=DIRECTION ( 'NONE',  ( -0.4999999999999798495, 0.000000000000000000, 0.8660254037844502539 ) ) ;
#11802=CARTESIAN_POINT ( 'NONE',  ( 0.2373612774290684013, -0.4881889763779528324, 0.06430355563125962626 ) ) ;
#11803=FACE_OUTER_BOUND ( 'NONE', #10420, .T. ) ;
#11805=ORIENTED_EDGE ( 'NONE', *, *, #15091, .T. ) ;
#11808=ORIENTED_EDGE ( 'NONE', *, *, #3019, .F. ) ;
#11809=ADVANCED_FACE ( 'NONE', ( #910 ), #14295, .F. ) ;
#11813=DIRECTION ( 'NONE',  ( 1.000000000000000000, 0.000000000000000000, 3.973232667114495301E-16 ) ) ;
#11814=CYLINDRICAL_SURFACE ( 'NONE', #446, 0.003937007874015758385 ) ;
#11815=CARTESIAN_POINT ( 'NONE',  ( 0.4788739157331329821, -0.09448818897637796532, 0.3446689608323530440 ) ) ;
#11816=DIRECTION ( 'NONE',  ( 0.8660254037844390407, 0.000000000000000000, -0.4999999999999995004 ) ) ;
#11818=ORIENTED_EDGE ( 'NONE', *, *, #14391, .F. ) ;
#11820=CARTESIAN_POINT ( 'NONE',  ( -0.4606299212598437554, -0.4881889763779528324, 0.3841425019411281450 ) ) ;
#11825=EDGE_CURVE ( 'NONE', #4883, #10896, #4836, .T. ) ;
#11828=EDGE_CURVE ( 'NONE', #13463, #8212, #4585, .T. ) ;
#11829=CARTESIAN_POINT ( 'NONE',  ( 0.1023622047244638761, -0.2952755905511811330, -0.3757906139821208247 ) ) ;
#11831=CARTESIAN_POINT ( 'NONE',  ( -0.1023622047242992716, -0.4881889763779528324, -0.2472069366677729363 ) ) ;
#11836=FACE_OUTER_BOUND ( 'NONE', #6006, .T. ) ;
#11838=VERTEX_POINT ( 'NONE', #9527 ) ;
#11840=ORIENTED_EDGE ( 'NONE', *, *, #12383, .T. ) ;
#11844=ORIENTED_EDGE ( 'NONE', *, *, #8508, .T. ) ;
#11845=ORIENTED_EDGE ( 'NONE', *, *, #1773, .T. ) ;
#11847=DIRECTION ( 'NONE',  ( 0.000000000000000000, 1.000000000000000000, -0.000000000000000000 ) ) ;
#11848=CARTESIAN_POINT ( 'NONE',  ( -0.09842519685028335019, -0.2952755905511811330, -0.4190977005962941981 ) ) ;
#11849=DIRECTION ( 'NONE',  ( 0.8660254037844385966, 0.000000000000000000, 0.5000000000000000000 ) ) ;
#11850=DIRECTION ( 'NONE',  ( 1.000000000000000000, 0.000000000000000000, 0.000000000000000000 ) ) ;
#11853=AXIS2_PLACEMENT_3D ( 'NONE', #11658, #12755, #2010 ) ;
#11859=AXIS2_PLACEMENT_3D ( 'NONE', #4165, #8961, #4238 ) ;
#11860=EDGE_CURVE ( 'NONE', #9228, #675, #3332, .T. ) ;
#11861=TOROIDAL_SURFACE ( 'NONE', #5581, 0.007874015748031495954, 0.003937007874015747977 ) ;
#11866=CARTESIAN_POINT ( 'NONE',  ( 0.5905511811023622659, -0.2952755905511811330, -0.4190977005962939206 ) ) ;
#11869=VECTOR ( 'NONE', #14229, 39.37007874015748143 ) ;
#11871=TOROIDAL_SURFACE ( 'NONE', #7847, 0.007874015748031495954, 0.003937007874015747977 ) ;
#11872=VERTEX_POINT ( 'NONE', #11964 ) ;
#11873=AXIS2_PLACEMENT_3D ( 'NONE', #9418, #3461, #1106 ) ;
#11874=FACE_OUTER_BOUND ( 'NONE', #7021, .T. ) ;
#11879=CYLINDRICAL_SURFACE ( 'NONE', #1167, 0.003937007874015724558 ) ;
#11882=AXIS2_PLACEMENT_3D ( 'NONE', #13777, #3204, #840 ) ;
#11883=AXIS2_PLACEMENT_3D ( 'NONE', #6050, #2619, #10839 ) ;
#11889=ORIENTED_EDGE ( 'NONE', *, *, #8552, .F. ) ;
#11894=CIRCLE ( 'NONE', #4372, 0.003937007874015750579 ) ;
#11895=AXIS2_PLACEMENT_3D ( 'NONE', #3838, #15457, #2671 ) ;
#11896=LINE ( 'NONE', #3666, #10352 ) ;
#11899=ADVANCED_FACE ( 'NONE', ( #1226 ), #3867, .T. ) ;
#11903=EDGE_CURVE ( 'NONE', #15013, #12057, #6568, .T. ) ;
#11904=EDGE_LOOP ( 'NONE', ( #1711, #4374, #9580, #11652 ) ) ;
#11906=DIRECTION ( 'NONE',  ( -0.8660254037844405950, 3.174764303743843882E-15, 0.4999999999999967804 ) ) ;
#11907=DIRECTION ( 'NONE',  ( 0.4999999999999979461, 0.000000000000000000, 0.8660254037844398178 ) ) ;
#11908=CIRCLE ( 'NONE', #13149, 0.003937007874015741038 ) ;
#11910=AXIS2_PLACEMENT_3D ( 'NONE', #5104, #7467, #12259 ) ;
#11911=VERTEX_POINT ( 'NONE', #11146 ) ;
#11913=ORIENTED_EDGE ( 'NONE', *, *, #2199, .T. ) ;
#11915=ORIENTED_EDGE ( 'NONE', *, *, #4, .T. ) ;
#11920=VECTOR ( 'NONE', #9585, 39.37007874015748143 ) ;
#11928=ORIENTED_EDGE ( 'NONE', *, *, #5100, .F. ) ;
#11933=ADVANCED_FACE ( 'NONE', ( #1366 ), #13343, .T. ) ;
#11934=CIRCLE ( 'NONE', #2679, 0.003937007874015721089 ) ;
#11937=AXIS2_PLACEMENT_3D ( 'NONE', #11541, #10686, #10363 ) ;
#11947=CYLINDRICAL_SURFACE ( 'NONE', #2670, 0.003937007874015721089 ) ;
#11948=CARTESIAN_POINT ( 'NONE',  ( -0.2681506793016945611, -0.4921259842519685179, 0.03207310886158504931 ) ) ;
#11949=VECTOR ( 'NONE', #12935, 39.37007874015748143 ) ;
#11950=DIRECTION ( 'NONE',  ( 0.8660254037844389297, 0.000000000000000000, -0.4999999999999994449 ) ) ;
#11951=EDGE_CURVE ( 'NONE', #11465, #5753, #9763, .T. ) ;
#11952=DIRECTION ( 'NONE',  ( -0.000000000000000000, -1.000000000000000000, -0.000000000000000000 ) ) ;
#11955=EDGE_LOOP ( 'NONE', ( #8433, #2310, #743, #9241 ) ) ;
#11957=ORIENTED_EDGE ( 'NONE', *, *, #6563, .T. ) ;
#11958=AXIS2_PLACEMENT_3D ( 'NONE', #5714, #6900, #10509 ) ;
#11959=ORIENTED_EDGE ( 'NONE', *, *, #15146, .T. ) ;
#11962=CYLINDRICAL_SURFACE ( 'NONE', #10143, 0.003937007874015721089 ) ;
#11964=CARTESIAN_POINT ( 'NONE',  ( 0.4783464566929142014, -0.4881889763779528324, 0.3534565624369548908 ) ) ;
#11966=CYLINDRICAL_SURFACE ( 'NONE', #14616, 0.03937007874015759773 ) ;
#11968=DIRECTION ( 'NONE',  ( -1.000000000000000000, 0.000000000000000000, 0.000000000000000000 ) ) ;
#11970=CARTESIAN_POINT ( 'NONE',  ( 0.5894146648244296127, -0.09448818897637796532, 0.1610807828475372405 ) ) ;
#11975=AXIS2_PLACEMENT_3D ( 'NONE', #2226, #11715, #981 ) ;
#11976=ORIENTED_EDGE ( 'NONE', *, *, #9854, .F. ) ;
#11977=ORIENTED_EDGE ( 'NONE', *, *, #12527, .T. ) ;
#11978=ORIENTED_EDGE ( 'NONE', *, *, #8490, .T. ) ;
#11979=ORIENTED_EDGE ( 'NONE', *, *, #14195, .F. ) ;
#11981=CIRCLE ( 'NONE', #9727, 0.003937007874015758385 ) ;
#11983=CARTESIAN_POINT ( 'NONE',  ( 0.2681506793018588186, -0.4881889763779528324, 0.03207310886168001501 ) ) ;
#11988=CARTESIAN_POINT ( 'NONE',  ( -0.06299212598414161146, -0.4921259842519685179, -0.5909884645248154600 ) ) ;
#11990=CARTESIAN_POINT ( 'NONE',  ( -0.1724006475077544398, -0.1023622047244094474, 0.1768186671464649640 ) ) ;
#11991=DIRECTION ( 'NONE',  ( -3.614007241618347785E-16, 0.000000000000000000, 1.000000000000000000 ) ) ;
#11993=AXIS2_PLACEMENT_3D ( 'NONE', #7433, #11029, #7274 ) ;
#11994=VERTEX_POINT ( 'NONE', #14602 ) ;
#11995=ORIENTED_EDGE ( 'NONE', *, *, #3861, .T. ) ;
#11996=ORIENTED_EDGE ( 'NONE', *, *, #4787, .T. ) ;
#11997=EDGE_CURVE ( 'NONE', #9448, #12429, #618, .T. ) ;
#11999=EDGE_CURVE ( 'NONE', #13962, #4061, #7102, .T. ) ;
#12000=CARTESIAN_POINT ( 'NONE',  ( -0.06299212598414173636, -0.4881889763779528324, -0.2377126739438355507 ) ) ;
#12001=FACE_OUTER_BOUND ( 'NONE', #14436, .T. ) ;
#12003=CARTESIAN_POINT ( 'NONE',  ( 0.1872249459501148516, -0.09842519685039370636, -0.1080943729433118949 ) ) ;
#12004=EDGE_LOOP ( 'NONE', ( #5536, #12694, #14555 ) ) ;
#12005=FACE_OUTER_BOUND ( 'NONE', #3641, .T. ) ;
#12006=CARTESIAN_POINT ( 'NONE',  ( 0.5418660417173575272, -0.4921259842519685179, 0.2355633981508976349 ) ) ;
#12009=VERTEX_POINT ( 'NONE', #13271 ) ;
#12016=CARTESIAN_POINT ( 'NONE',  ( 0.000000000000000000, -0.09842519685039370636, 0.000000000000000000 ) ) ;
#12018=DIRECTION ( 'NONE',  ( 1.000000000000000000, 0.000000000000000000, 0.000000000000000000 ) ) ;
#12019=CARTESIAN_POINT ( 'NONE',  ( 0.000000000000000000, 2.165354330708661568, 0.1535433070866141780 ) ) ;
#12024=CARTESIAN_POINT ( 'NONE',  ( 0.4591888763630541104, -0.4881889763779528324, 0.3787644491703230365 ) ) ;
#12025=ORIENTED_EDGE ( 'NONE', *, *, #6368, .T. ) ;
#12030=FACE_BOUND ( 'NONE', #4045, .T. ) ;
#12035=DIRECTION ( 'NONE',  ( 0.8660254037844501429, 0.000000000000000000, 0.4999999999999798495 ) ) ;
#12037=CARTESIAN_POINT ( 'NONE',  ( 0.3117681530218320840, -0.2952755905511811330, 0.2981971199768684855 ) ) ;
#12039=EDGE_CURVE ( 'NONE', #1202, #11305, #1363, .T. ) ;
#12041=DIRECTION ( 'NONE',  ( -0.4999999999999967248, -4.336808689941996437E-15, -0.8660254037844405950 ) ) ;
#12042=EDGE_LOOP ( 'NONE', ( #8277, #1762, #14758, #6599 ) ) ;
#12044=VERTEX_POINT ( 'NONE', #4094 ) ;
#12047=EDGE_CURVE ( 'NONE', #4812, #13356, #1131, .T. ) ;
#12048=CARTESIAN_POINT ( 'NONE',  ( 0.1023622047244638067, -0.4881889763779528324, -0.2482618547481154347 ) ) ;
#12050=DIRECTION ( 'NONE',  ( -0.8660254037844385966, 0.000000000000000000, 0.5000000000000001110 ) ) ;
#12051=DIRECTION ( 'NONE',  ( -0.8660254037844381525, 0.000000000000000000, 0.5000000000000006661 ) ) ;
#12052=ADVANCED_FACE ( 'NONE', ( #4407 ), #2851, .T. ) ;
#12054=EDGE_CURVE ( 'NONE', #13558, #5085, #3239, .T. ) ;
#12055=DIRECTION ( 'NONE',  ( -1.000000000000000000, -0.000000000000000000, -3.614007241618347785E-16 ) ) ;
#12057=VERTEX_POINT ( 'NONE', #2931 ) ;
#12059=VERTEX_POINT ( 'NONE', #13888 ) ;
#12061=CARTESIAN_POINT ( 'NONE',  ( 0.02952755905511747145, -0.09842519685039370636, 0.05114323250695394785 ) ) ;
#12067=CYLINDRICAL_SURFACE ( 'NONE', #436, 0.003937007874015741038 ) ;
#12069=ORIENTED_EDGE ( 'NONE', *, *, #8063, .T. ) ;
#12070=ORIENTED_EDGE ( 'NONE', *, *, #12047, .T. ) ;
#12072=ORIENTED_EDGE ( 'NONE', *, *, #6655, .T. ) ;
#12073=DIRECTION ( 'NONE',  ( -0.5000000000000004441, -1.618519037356983674E-14, -0.8660254037844383745 ) ) ;
#12074=DIRECTION ( 'NONE',  ( 0.8660254037844383745, 0.000000000000000000, -0.5000000000000004441 ) ) ;
#12079=ORIENTED_EDGE ( 'NONE', *, *, #14812, .F. ) ;
#12080=EDGE_CURVE ( 'NONE', #3171, #11605, #857, .T. ) ;
#12081=DIRECTION ( 'NONE',  ( -1.000000000000000000, 0.000000000000000000, 0.000000000000000000 ) ) ;
#12082=DIRECTION ( 'NONE',  ( 0.000000000000000000, -1.000000000000000000, 0.000000000000000000 ) ) ;
#12083=CARTESIAN_POINT ( 'NONE',  ( -0.3944453183761345572, -0.2952755905511811330, 0.1549960689574421957 ) ) ;
#12085=CARTESIAN_POINT ( 'NONE',  ( -0.1618514667033795484, -0.09842519685039370636, 0.2161887458866224576 ) ) ;
#12087=TOROIDAL_SURFACE ( 'NONE', #12337, 0.04330708661417328326, 0.003937007874015747977 ) ;
#12094=LINE ( 'NONE', #275, #14914 ) ;
#12098=CARTESIAN_POINT ( 'NONE',  ( 0.5860051159906326523, -0.09842519685039370636, 0.1591122789105293422 ) ) ;
#12109=DIRECTION ( 'NONE',  ( 1.000000000000000000, 0.000000000000000000, 0.000000000000000000 ) ) ;
#12112=AXIS2_PLACEMENT_3D ( 'NONE', #4335, #13910, #14145 ) ;
#12115=EDGE_CURVE ( 'NONE', #8036, #1499, #6597, .T. ) ;
#12116=AXIS2_PLACEMENT_3D ( 'NONE', #439, #2938, #14770 ) ;
#12120=DIRECTION ( 'NONE',  ( 0.000000000000000000, 0.000000000000000000, 1.000000000000000000 ) ) ;
#12121=AXIS2_PLACEMENT_3D ( 'NONE', #5526, #5611, #9235 ) ;
#12123=AXIS2_PLACEMENT_3D ( 'NONE', #3173, #5805, #8261 ) ;
#12124=AXIS2_PLACEMENT_3D ( 'NONE', #4840, #13006, #2267 ) ;
#12125=PLANE ( 'NONE',  #13657 ) ;
#12126=AXIS2_PLACEMENT_3D ( 'NONE', #15360, #15447, #12936 ) ;
#12131=CARTESIAN_POINT ( 'NONE',  ( 0.06767366483286080259, -0.2952755905511811330, 0.7209811753676967916 ) ) ;
#12132=LINE ( 'NONE', #9710, #13084 ) ;
#12141=CIRCLE ( 'NONE', #2358, 0.003937007874015724558 ) ;
#12150=DIRECTION ( 'NONE',  ( 1.000000000000000000, -8.673617379884049672E-15, 0.000000000000000000 ) ) ;
#12153=CIRCLE ( 'NONE', #8894, 0.003937007874015737569 ) ;
#12154=ORIENTED_EDGE ( 'NONE', *, *, #15399, .T. ) ;
#12155=DIRECTION ( 'NONE',  ( 0.5000000000000037748, -0.000000000000000000, 0.8660254037844365982 ) ) ;
#12157=CARTESIAN_POINT ( 'NONE',  ( 0.09842519685044820443, -0.4921259842519685179, -0.5870514566507987197 ) ) ;
#12159=EDGE_LOOP ( 'NONE', ( #6201, #679, #15177, #4735 ) ) ;
#12161=VERTEX_POINT ( 'NONE', #12729 ) ;
#12164=CARTESIAN_POINT ( 'NONE',  ( 0.000000000000000000, -0.09842519685039370636, 0.2161887458866224576 ) ) ;
#12168=CYLINDRICAL_SURFACE ( 'NONE', #627, 0.003937007874015749712 ) ;
#12170=PLANE ( 'NONE',  #13431 ) ;
#12171=CARTESIAN_POINT ( 'NONE',  ( 0.1574803149606299191, -0.003937007874015747977, -0.5909884645248143498 ) ) ;
#12175=DIRECTION ( 'NONE',  ( 0.8660254037844365982, -0.000000000000000000, 0.5000000000000035527 ) ) ;
#12177=AXIS2_PLACEMENT_3D ( 'NONE', #3730, #13275, #8657 ) ;
#12179=EDGE_LOOP ( 'NONE', ( #13943, #2246, #14954, #7654 ) ) ;
#12182=EDGE_CURVE ( 'NONE', #315, #7883, #1864, .T. ) ;
#12187=DIRECTION ( 'NONE',  ( 0.000000000000000000, 1.000000000000000000, -0.000000000000000000 ) ) ;
#12188=CARTESIAN_POINT ( 'NONE',  ( -0.5418660417173573052, -0.4881889763779528324, 0.2355633981508970520 ) ) ;
#12190=VECTOR ( 'NONE', #11362, 39.37007874015748143 ) ;
#12195=DIRECTION ( 'NONE',  ( 0.4999999999999998335, 0.000000000000000000, 0.8660254037844388186 ) ) ;
#12201=VERTEX_POINT ( 'NONE', #2286 ) ;
#12204=ADVANCED_FACE ( 'NONE', ( #13023 ), #1608, .T. ) ;
#12207=DIRECTION ( 'NONE',  ( 0.000000000000000000, 0.000000000000000000, 1.000000000000000000 ) ) ;
#12209=CARTESIAN_POINT ( 'NONE',  ( 0.5576140732134206024, -0.09842519685039370636, 0.2082870074805215910 ) ) ;
#12211=DIRECTION ( 'NONE',  ( 0.000000000000000000, 1.000000000000000000, 0.000000000000000000 ) ) ;
#12219=VERTEX_POINT ( 'NONE', #10444 ) ;
#12222=ORIENTED_EDGE ( 'NONE', *, *, #13057, .F. ) ;
#12223=ORIENTED_EDGE ( 'NONE', *, *, #6677, .F. ) ;
#12228=EDGE_CURVE ( 'NONE', #3506, #5345, #10359, .T. ) ;
#12235=ORIENTED_EDGE ( 'NONE', *, *, #13719, .T. ) ;
#12241=EDGE_CURVE ( 'NONE', #6593, #1223, #7356, .T. ) ;
#12244=CARTESIAN_POINT ( 'NONE',  ( 0.1804058482825207643, -0.4921259842519685179, -0.1041573650692960984 ) ) ;
#12247=DIRECTION ( 'NONE',  ( 0.000000000000000000, -1.000000000000000000, 0.000000000000000000 ) ) ;
#12252=CARTESIAN_POINT ( 'NONE',  ( 0.09948011493088554369, -0.4881889763779528324, -0.2443248468740996937 ) ) ;
#12253=DIRECTION ( 'NONE',  ( 0.8660254037844395958, 0.000000000000000000, -0.4999999999999982236 ) ) ;
#12255=VERTEX_POINT ( 'NONE', #4644 ) ;
#12258=DIRECTION ( 'NONE',  ( 0.5000000000000000000, 0.000000000000000000, 0.8660254037844388186 ) ) ;
#12259=DIRECTION ( 'NONE',  ( 1.445602896647339903E-16, 0.000000000000000000, -1.000000000000000000 ) ) ;
#12263=DIRECTION ( 'NONE',  ( -8.673617379884051249E-15, -1.000000000000000000, 0.000000000000000000 ) ) ;
#12264=DIRECTION ( 'NONE',  ( -0.000000000000000000, -1.000000000000000000, -0.000000000000000000 ) ) ;
#12266=DIRECTION ( 'NONE',  ( -0.8660254037844309360, 0.000000000000000000, -0.5000000000000134337 ) ) ;
#12267=CARTESIAN_POINT ( 'NONE',  ( -0.05905511811012585655, -0.09448818897637796532, -0.5909884645248143498 ) ) ;
#12268=ORIENTED_EDGE ( 'NONE', *, *, #14113, .T. ) ;
#12270=ORIENTED_EDGE ( 'NONE', *, *, #4793, .F. ) ;
#12277=DIRECTION ( 'NONE',  ( -0.8660254037844398178, 0.000000000000000000, 0.4999999999999979461 ) ) ;
#12280=SPHERICAL_SURFACE ( 'NONE', #1577, 0.003937007874015747977 ) ;
#12287=ADVANCED_FACE ( 'NONE', ( #6912 ), #5963, .T. ) ;
#12293=CARTESIAN_POINT ( 'NONE',  ( -0.3294846884549019750, -0.2952755905511811330, 0.2675111804726950648 ) ) ;
#12301=ORIENTED_EDGE ( 'NONE', *, *, #8663, .T. ) ;
#12302=ORIENTED_EDGE ( 'NONE', *, *, #8982, .F. ) ;
#12305=EDGE_LOOP ( 'NONE', ( #726, #1852, #8345 ) ) ;
#12309=DIRECTION ( 'NONE',  ( 0.5000000000000069944, -7.511572993685774449E-15, -0.8660254037844347108 ) ) ;
#12312=ORIENTED_EDGE ( 'NONE', *, *, #3284, .T. ) ;
#12313=DIRECTION ( 'NONE',  ( 0.5000000000000005551, 0.000000000000000000, -0.8660254037844384856 ) ) ;
#12320=VERTEX_POINT ( 'NONE', #1340 ) ;
#12322=EDGE_CURVE ( 'NONE', #6217, #15216, #2863, .T. ) ;
#12323=EDGE_CURVE ( 'NONE', #11649, #13020, #1381, .T. ) ;
#12329=CARTESIAN_POINT ( 'NONE',  ( 0.06692913385832206796, -0.4881889763779528324, 9.675294977568793108E-18 ) ) ;
#12335=AXIS2_PLACEMENT_3D ( 'NONE', #5514, #7646, #11249 ) ;
#12337=AXIS2_PLACEMENT_3D ( 'NONE', #4917, #3812, #7330 ) ;
#12341=DIRECTION ( 'NONE',  ( -0.8660254037844395958, 0.000000000000000000, 0.4999999999999982236 ) ) ;
#12344=VECTOR ( 'NONE', #11076, 39.37007874015748143 ) ;
#12346=CARTESIAN_POINT ( 'NONE',  ( 0.1062992125984795477, -0.1023622047244094474, -0.2482618547481154625 ) ) ;
#12347=AXIS2_PLACEMENT_3D ( 'NONE', #11287, #1299, #559 ) ;
#12351=ORIENTED_EDGE ( 'NONE', *, *, #3769, .T. ) ;
#12352=ORIENTED_EDGE ( 'NONE', *, *, #3561, .F. ) ;
#12353=VERTEX_POINT ( 'NONE', #8710 ) ;
#12355=ORIENTED_EDGE ( 'NONE', *, *, #14388, .T. ) ;
#12356=AXIS2_PLACEMENT_3D ( 'NONE', #5721, #3306, #15143 ) ;
#12359=AXIS2_PLACEMENT_3D ( 'NONE', #14766, #10999, #281 ) ;
#12360=TOROIDAL_SURFACE ( 'NONE', #11873, 0.04330708661417328326, 0.003937007874015747977 ) ;
#12361=DIRECTION ( 'NONE',  ( 0.000000000000000000, 1.000000000000000000, 0.000000000000000000 ) ) ;
#12368=DIRECTION ( 'NONE',  ( -1.000000000000000000, 0.000000000000000000, 0.000000000000000000 ) ) ;
#12373=ADVANCED_FACE ( 'NONE', ( #2515 ), #5357, .T. ) ;
#12375=AXIS2_PLACEMENT_3D ( 'NONE', #8761, #4214, #1548 ) ;
#12383=EDGE_CURVE ( 'NONE', #5753, #14387, #10636, .T. ) ;
#12384=AXIS2_PLACEMENT_3D ( 'NONE', #2051, #6821, #10447 ) ;
#12385=VECTOR ( 'NONE', #5656, 39.37007874015748143 ) ;
#12386=EDGE_CURVE ( 'NONE', #15216, #986, #11041, .T. ) ;
#12388=FACE_OUTER_BOUND ( 'NONE', #3605, .T. ) ;
#12390=CARTESIAN_POINT ( 'NONE',  ( -0.5418660417173573052, -0.4881889763779528324, 0.2355633981508970798 ) ) ;
#12391=AXIS2_PLACEMENT_3D ( 'NONE', #1869, #6629, #11427 ) ;
#12393=ORIENTED_EDGE ( 'NONE', *, *, #4733, .F. ) ;
#12400=DIRECTION ( 'NONE',  ( -0.000000000000000000, 1.000000000000000000, -0.000000000000000000 ) ) ;
#12401=AXIS2_PLACEMENT_3D ( 'NONE', #11520, #1029, #1893 ) ;
#12406=AXIS2_PLACEMENT_3D ( 'NONE', #1372, #1456, #14376 ) ;
#12411=CARTESIAN_POINT ( 'NONE',  ( 0.5860051159906326523, -0.09448818897637796532, 0.1591122789105293700 ) ) ;
#12415=CARTESIAN_POINT ( 'NONE',  ( 1.928577636452524610E-17, 0.003937007874015860734, 0.1574803149606299191 ) ) ;
#12416=CIRCLE ( 'NONE', #11668, 0.003937007874015750579 ) ;
#12417=CARTESIAN_POINT ( 'NONE',  ( -0.4307978335858689278, -0.09448818897637796532, 0.4279391777402706820 ) ) ;
#12418=ADVANCED_FACE ( 'NONE', ( #412 ), #8401, .F. ) ;
#12419=EDGE_CURVE ( 'NONE', #1083, #4570, #11635, .T. ) ;
#12421=AXIS2_PLACEMENT_3D ( 'NONE', #5256, #1756, #11298 ) ;
#12422=CARTESIAN_POINT ( 'NONE',  ( 0.1586168312385622392, -0.003937007874015747977, -0.5890199605878065903 ) ) ;
#12426=LINE ( 'NONE', #14705, #3372 ) ;
#12427=ORIENTED_EDGE ( 'NONE', *, *, #11656, .T. ) ;
#12428=AXIS2_PLACEMENT_3D ( 'NONE', #746, #5503, #13572 ) ;
#12429=VERTEX_POINT ( 'NONE', #6649 ) ;
#12433=DIRECTION ( 'NONE',  ( 0.4999999999999998335, -0.000000000000000000, 0.8660254037844388186 ) ) ;
#12438=CARTESIAN_POINT ( 'NONE',  ( -0.1023622047242991467, -0.1023622047244094474, -0.5909884645248154600 ) ) ;
#12440=VECTOR ( 'NONE', #3125, 39.37007874015748143 ) ;
#12443=VERTEX_POINT ( 'NONE', #11518 ) ;
#12446=ORIENTED_EDGE ( 'NONE', *, *, #12469, .T. ) ;
#12447=VECTOR ( 'NONE', #7344, 39.37007874015748854 ) ;
#12448=ORIENTED_EDGE ( 'NONE', *, *, #15091, .F. ) ;
#12451=DIRECTION ( 'NONE',  ( -1.000000000000000000, 0.000000000000000000, 0.000000000000000000 ) ) ;
#12452=DIRECTION ( 'NONE',  ( 0.000000000000000000, 0.000000000000000000, -1.000000000000000000 ) ) ;
#12453=CIRCLE ( 'NONE', #4191, 0.003937007874015724558 ) ;
#12454=LINE ( 'NONE', #1638, #14702 ) ;
#12455=DIRECTION ( 'NONE',  ( -0.000000000000000000, 1.000000000000000000, -0.000000000000000000 ) ) ;
#12457=AXIS2_PLACEMENT_3D ( 'NONE', #14331, #6798, #14262 ) ;
#12459=DIRECTION ( 'NONE',  ( 0.4999999999999998335, -0.000000000000000000, 0.8660254037844388186 ) ) ;
#12462=DIRECTION ( 'NONE',  ( 0.000000000000000000, -1.000000000000000000, 0.000000000000000000 ) ) ;
#12463=CARTESIAN_POINT ( 'NONE',  ( 0.4552518684890383138, -0.1023622047244094474, 0.3855835468379170128 ) ) ;
#12464=AXIS2_PLACEMENT_3D ( 'NONE', #8811, #12433, #3096 ) ;
#12466=ORIENTED_EDGE ( 'NONE', *, *, #4833, .T. ) ;
#12467=ORIENTED_EDGE ( 'NONE', *, *, #1889, .T. ) ;
#12468=AXIS2_PLACEMENT_3D ( 'NONE', #9419, #14192, #5635 ) ;
#12469=EDGE_CURVE ( 'NONE', #6177, #11006, #7367, .T. ) ;
#12472=CIRCLE ( 'NONE', #7210, 0.03937007874015751446 ) ;
#12474=CARTESIAN_POINT ( 'NONE',  ( -0.3780663654712353994, -0.2952755905511811330, 0.1046250900831904723 ) ) ;
#12479=DIRECTION ( 'NONE',  ( 0.4999999999999998335, 0.000000000000000000, 0.8660254037844388186 ) ) ;
#12480=CARTESIAN_POINT ( 'NONE',  ( 0.09842519685044813504, -0.2952755905511811330, -0.3757906139821208247 ) ) ;
#12483=EDGE_CURVE ( 'NONE', #3171, #10010, #9388, .T. ) ;
#12486=EDGE_LOOP ( 'NONE', ( #8983, #5679, #6596, #6122 ) ) ;
#12488=EDGE_CURVE ( 'NONE', #11529, #11032, #372, .T. ) ;
#12492=DIRECTION ( 'NONE',  ( 0.4999999999999979461, 0.000000000000000000, 0.8660254037844398178 ) ) ;
#12498=DIRECTION ( 'NONE',  ( 0.000000000000000000, -1.000000000000000000, 0.000000000000000000 ) ) ;
#12499=ADVANCED_FACE ( 'NONE', ( #2986 ), #12886, .F. ) ;
#12501=VERTEX_POINT ( 'NONE', #12474 ) ;
#12502=ADVANCED_FACE ( 'NONE', ( #2812 ), #4628, .T. ) ;
#12506=ORIENTED_EDGE ( 'NONE', *, *, #12488, .T. ) ;
#12511=ADVANCED_FACE ( 'NONE', ( #553 ), #3118, .T. ) ;
#12513=CARTESIAN_POINT ( 'NONE',  ( 0.4305093106511115875, -0.2952755905511811330, 0.1712715594937237185 ) ) ;
#12516=DIRECTION ( 'NONE',  ( 0.8660254037844387076, 0.000000000000000000, 0.5000000000000001110 ) ) ;
#12517=CARTESIAN_POINT ( 'NONE',  ( 0.06351958502452510757, -0.4921259842519685179, -0.2357441700067326174 ) ) ;
#12527=EDGE_CURVE ( 'NONE', #13891, #8036, #1621, .T. ) ;
#12529=SPHERICAL_SURFACE ( 'NONE', #14362, 0.003937007874015747977 ) ;
#12532=CYLINDRICAL_SURFACE ( 'NONE', #5162, 0.003937007874015758385 ) ;
#12537=EDGE_LOOP ( 'NONE', ( #1899, #1745, #15434, #2174 ) ) ;
#12538=ORIENTED_EDGE ( 'NONE', *, *, #2126, .T. ) ;
#12540=ORIENTED_EDGE ( 'NONE', *, *, #11312, .T. ) ;
#12541=FACE_OUTER_BOUND ( 'NONE', #12537, .T. ) ;
#12546=CARTESIAN_POINT ( 'NONE',  ( 0.4330708661417309036, -0.003937007874015747977, 0.4318761856142889766 ) ) ;
#12551=DIRECTION ( 'NONE',  ( 0.000000000000000000, 0.000000000000000000, 1.000000000000000000 ) ) ;
#12552=VERTEX_POINT ( 'NONE', #7588 ) ;
#12554=EDGE_LOOP ( 'NONE', ( #5415, #13308, #11530, #2463 ) ) ;
#12555=DIRECTION ( 'NONE',  ( 0.5000000000000069944, 0.000000000000000000, 0.8660254037844347108 ) ) ;
#12556=DIRECTION ( 'NONE',  ( -0.000000000000000000, -1.000000000000000000, 0.000000000000000000 ) ) ;
#12557=ADVANCED_FACE ( 'NONE', ( #12388 ), #12930, .F. ) ;
#12558=CYLINDRICAL_SURFACE ( 'NONE', #3609, 0.003937007874015749712 ) ;
#12559=DIRECTION ( 'NONE',  ( -3.614007241618347785E-16, 0.000000000000000000, 1.000000000000000000 ) ) ;
#12562=CARTESIAN_POINT ( 'NONE',  ( 0.06692913385832206796, -0.4881889763779528324, -0.2377126739437405434 ) ) ;
#12564=CYLINDRICAL_SURFACE ( 'NONE', #8668, 0.03937007874015759773 ) ;
#12565=DIRECTION ( 'NONE',  ( -0.000000000000000000, -1.000000000000000000, -0.000000000000000000 ) ) ;
#12566=CARTESIAN_POINT ( 'NONE',  ( 0.3766253205744449772, -0.2952755905511811330, 0.09924703731238518345 ) ) ;
#12568=CARTESIAN_POINT ( 'NONE',  ( -0.6923203342731879539, -0.2952755905511811330, -0.2821984354013215568 ) ) ;
#12569=ORIENTED_EDGE ( 'NONE', *, *, #8008, .F. ) ;
#12572=ORIENTED_EDGE ( 'NONE', *, *, #2426, .T. ) ;
#12573=EDGE_CURVE ( 'NONE', #10145, #2574, #7991, .T. ) ;
#12576=CARTESIAN_POINT ( 'NONE',  ( 0.000000000000000000, 0.000000000000000000, 0.000000000000000000 ) ) ;
#12584=EDGE_CURVE ( 'NONE', #10309, #12947, #8151, .T. ) ;
#12586=EDGE_LOOP ( 'NONE', ( #11636, #15027, #2212, #1119 ) ) ;
#12590=ORIENTED_EDGE ( 'NONE', *, *, #1238, .F. ) ;
#12592=DIRECTION ( 'NONE',  ( 0.000000000000000000, 0.000000000000000000, -1.000000000000000000 ) ) ;
#12593=DIRECTION ( 'NONE',  ( -0.4999999999999998335, 0.000000000000000000, -0.8660254037844388186 ) ) ;
#12597=CARTESIAN_POINT ( 'NONE',  ( 0.1552072824047652233, -0.003937007874015747977, -0.5870514566507987197 ) ) ;
#12599=CARTESIAN_POINT ( 'NONE',  ( -0.3492731901935981487, -0.2952755905511811330, 0.3198506632839545061 ) ) ;
#12600=SPHERICAL_SURFACE ( 'NONE', #12391, 0.003937007874015747977 ) ;
#12602=CARTESIAN_POINT ( 'NONE',  ( -0.1062992125983150127, -0.4921259842519685179, -0.2482618547482104143 ) ) ;
#12606=LINE ( 'NONE', #13853, #10437 ) ;
#12607=FACE_OUTER_BOUND ( 'NONE', #141, .T. ) ;
#12610=ORIENTED_EDGE ( 'NONE', *, *, #13802, .F. ) ;
#12616=VERTEX_POINT ( 'NONE', #3221 ) ;
#12618=DIRECTION ( 'NONE',  ( 0.4999999999999967804, 0.000000000000000000, -0.8660254037844405950 ) ) ;
#12620=DIRECTION ( 'NONE',  ( -0.8660254037844347108, 0.000000000000000000, -0.5000000000000069944 ) ) ;
#12621=AXIS2_PLACEMENT_3D ( 'NONE', #2393, #7249, #8503 ) ;
#12624=DIRECTION ( 'NONE',  ( 0.000000000000000000, -1.000000000000000000, 0.000000000000000000 ) ) ;
#12627=AXIS2_PLACEMENT_3D ( 'NONE', #9193, #5252, #10049 ) ;
#12628=DIRECTION ( 'NONE',  ( 0.000000000000000000, -1.734723475976806463E-14, -1.000000000000000000 ) ) ;
#12630=ORIENTED_EDGE ( 'NONE', *, *, #8396, .T. ) ;
#12631=DIRECTION ( 'NONE',  ( -0.8660254037844385966, 0.000000000000000000, 0.5000000000000001110 ) ) ;
#12634=TOROIDAL_SURFACE ( 'NONE', #6604, 0.007874015748031495954, 0.003937007874015747977 ) ;
#12636=AXIS2_PLACEMENT_3D ( 'NONE', #12329, #13504, #5190 ) ;
#12637=CIRCLE ( 'NONE', #9634, 0.003937007874015721089 ) ;
#12638=PLANE ( 'NONE',  #3416 ) ;
#12646=ORIENTED_EDGE ( 'NONE', *, *, #8535, .F. ) ;
#12648=CARTESIAN_POINT ( 'NONE',  ( 0.3314531923919106227, -0.2952755905511811330, 0.2641016316388982710 ) ) ;
#12649=LINE ( 'NONE', #1919, #9887 ) ;
#12656=EDGE_LOOP ( 'NONE', ( #8596, #12630 ) ) ;
#12658=ORIENTED_EDGE ( 'NONE', *, *, #2044, .F. ) ;
#12660=VECTOR ( 'NONE', #4123, 39.37007874015748143 ) ;
#12663=DIRECTION ( 'NONE',  ( -0.5000000000000004441, 0.000000000000000000, 0.8660254037844383745 ) ) ;
#12665=TOROIDAL_SURFACE ( 'NONE', #9919, 0.007874015748031495954, 0.003937007874015747977 ) ;
#12666=CARTESIAN_POINT ( 'NONE',  ( -0.5894146648244306119, -0.09448818897637796532, 0.1610807828475335490 ) ) ;
#12669=DIRECTION ( 'NONE',  ( 0.000000000000000000, 1.000000000000000000, 0.000000000000000000 ) ) ;
#12670=CARTESIAN_POINT ( 'NONE',  ( 0.1724006475077543565, -0.4881889763779528324, 0.1728816592724491952 ) ) ;
#12672=AXIS2_PLACEMENT_3D ( 'NONE', #1300, #2706, #14385 ) ;
#12676=ORIENTED_EDGE ( 'NONE', *, *, #14681, .T. ) ;
#12677=CIRCLE ( 'NONE', #12177, 0.007874015748031482076 ) ;
#12678=EDGE_CURVE ( 'NONE', #13903, #13305, #1324, .T. ) ;
#12680=EDGE_CURVE ( 'NONE', #3640, #2230, #4931, .T. ) ;
#12684=CARTESIAN_POINT ( 'NONE',  ( 0.2393297813660762996, -0.4881889763779528324, 0.06089400679746261730 ) ) ;
#12687=AXIS2_PLACEMENT_3D ( 'NONE', #15048, #4299, #11688 ) ;
#12688=DIRECTION ( 'NONE',  ( -0.5000000000000008882, 0.000000000000000000, 0.8660254037844381525 ) ) ;
#12689=VERTEX_POINT ( 'NONE', #12000 ) ;
#12692=VECTOR ( 'NONE', #4568, 39.37007874015748143 ) ;
#12694=ORIENTED_EDGE ( 'NONE', *, *, #12182, .T. ) ;
#12701=CARTESIAN_POINT ( 'NONE',  ( -0.3669897256266691499, -0.2952755905511811330, 0.2891647237797815850 ) ) ;
#12704=DIRECTION ( 'NONE',  ( 0.000000000000000000, -1.000000000000000000, 0.000000000000000000 ) ) ;
#12705=SHAPE_REPRESENTATION ( 'Spider', ( #11481 ), #5701 ) ;
#12709=AXIS2_PLACEMENT_3D ( 'NONE', #2167, #7291, #11734 ) ;
#12711=CARTESIAN_POINT ( 'NONE',  ( 0.06692913385832208184, -0.2952755905511811330, -0.4190977005962941426 ) ) ;
#12713=DIRECTION ( 'NONE',  ( -1.000000000000000000, -0.000000000000000000, 0.000000000000000000 ) ) ;
#12719=ORIENTED_EDGE ( 'NONE', *, *, #10576, .F. ) ;
#12724=ORIENTED_EDGE ( 'NONE', *, *, #4229, .F. ) ;
#12727=AXIS2_PLACEMENT_3D ( 'NONE', #8532, #2666, #2573 ) ;
#12729=CARTESIAN_POINT ( 'NONE',  ( -0.4572203724260467950, -0.4881889763779528324, 0.3821739980041202744 ) ) ;
#12731=DIRECTION ( 'NONE',  ( 3.942553354492736135E-16, 0.000000000000000000, -1.000000000000000000 ) ) ;
#12732=ORIENTED_EDGE ( 'NONE', *, *, #13418, .F. ) ;
#12737=CYLINDRICAL_SURFACE ( 'NONE', #14181, 0.003937007874015724558 ) ;
#12739=EDGE_LOOP ( 'NONE', ( #7952, #14085, #4777, #10492 ) ) ;
#12744=CARTESIAN_POINT ( 'NONE',  ( 0.000000000000000000, 0.003937007874015860734, 0.000000000000000000 ) ) ;
#12745=CARTESIAN_POINT ( 'NONE',  ( -0.05314960629921194196, -0.09842519685039370636, 0.09205781851251791659 ) ) ;
#12747=SPHERICAL_SURFACE ( 'NONE', #13906, 0.003937007874015747977 ) ;
#12748=CARTESIAN_POINT ( 'NONE',  ( 0.09842519685044820443, -0.4881889763779528324, -0.5870514566507987197 ) ) ;
#12752=ORIENTED_EDGE ( 'NONE', *, *, #13134, .T. ) ;
#12755=DIRECTION ( 'NONE',  ( 0.000000000000000000, -1.000000000000000000, 0.000000000000000000 ) ) ;
#12756=FACE_OUTER_BOUND ( 'NONE', #12767, .T. ) ;
#12757=FACE_OUTER_BOUND ( 'NONE', #12804, .T. ) ;
#12758=DIRECTION ( 'NONE',  ( 0.4999999999999966693, 0.000000000000000000, -0.8660254037844405950 ) ) ;
#12759=CARTESIAN_POINT ( 'NONE',  ( 0.1463103599445507719, -0.09842519685039370636, -0.08447232569921737932 ) ) ;
#12760=CARTESIAN_POINT ( 'NONE',  ( 0.1552072824047652233, -0.003937007874015747977, -0.5909884645248143498 ) ) ;
#12764=FACE_OUTER_BOUND ( 'NONE', #10221, .T. ) ;
#12767=EDGE_LOOP ( 'NONE', ( #3300, #4062, #7948, #964 ) ) ;
#12768=EDGE_LOOP ( 'NONE', ( #1713, #2509, #868, #12831 ) ) ;
#12773=DIRECTION ( 'NONE',  ( -0.8660254037844395958, 0.000000000000000000, -0.4999999999999982236 ) ) ;
#12778=DIRECTION ( 'NONE',  ( 0.4999999999999966693, 0.000000000000000000, 0.8660254037844405950 ) ) ;
#12780=ORIENTED_EDGE ( 'NONE', *, *, #10185, .F. ) ;
#12782=CARTESIAN_POINT ( 'NONE',  ( 0.1552072824047652788, -0.003937007874015747977, -0.5870514566507987197 ) ) ;
#12790=LINE ( 'NONE', #973, #15362 ) ;
#12793=DIRECTION ( 'NONE',  ( -0.8660254037844383745, 0.000000000000000000, -0.5000000000000004441 ) ) ;
#12796=CARTESIAN_POINT ( 'NONE',  ( 0.1734555655881918346, -0.1023622047244094474, 0.1728816592724491952 ) ) ;
#12797=CARTESIAN_POINT ( 'NONE',  ( 0.1062992125984794506, -0.09842519685039370636, 4.223515039848272764E-17 ) ) ;
#12800=EDGE_CURVE ( 'NONE', #13296, #12353, #10388, .T. ) ;
#12801=ORIENTED_EDGE ( 'NONE', *, *, #12323, .T. ) ;
#12803=LINE ( 'NONE', #5422, #11180 ) ;
#12804=EDGE_LOOP ( 'NONE', ( #2752, #8263, #6969, #11021 ) ) ;
#12805=ORIENTED_EDGE ( 'NONE', *, *, #4353, .F. ) ;
#12806=ADVANCED_FACE ( 'NONE', ( #15032 ), #6399, .T. ) ;
#12809=DIRECTION ( 'NONE',  ( 0.000000000000000000, -1.000000000000000000, 0.000000000000000000 ) ) ;
#12811=CARTESIAN_POINT ( 'NONE',  ( -0.4307978335858689278, -0.09448818897637796532, 0.4279391777402706265 ) ) ;
#12814=DIRECTION ( 'NONE',  ( 0.8660254037844383745, 0.000000000000000000, -0.5000000000000004441 ) ) ;
#12815=ORIENTED_EDGE ( 'NONE', *, *, #6269, .T. ) ;
#12817=VERTEX_POINT ( 'NONE', #4137 ) ;
#12819=VERTEX_POINT ( 'NONE', #1640 ) ;
#12820=DIRECTION ( 'NONE',  ( -3.942553354492736135E-16, 0.000000000000000000, 1.000000000000000000 ) ) ;
#12821=CARTESIAN_POINT ( 'NONE',  ( -0.2359202325321149429, -0.1023622047244094474, 0.06286251073437545966 ) ) ;
#12824=CARTESIAN_POINT ( 'NONE',  ( -0.5649606299212329708, -0.09448818897637796532, 0.2034364137499347913 ) ) ;
#12825=VECTOR ( 'NONE', #12050, 39.37007874015748143 ) ;
#12831=ORIENTED_EDGE ( 'NONE', *, *, #10743, .F. ) ;
#12839=AXIS2_PLACEMENT_3D ( 'NONE', #9645, #83, #3758 ) ;
#12840=ADVANCED_FACE ( 'NONE', ( #11267 ), #540, .T. ) ;
#12841=DIRECTION ( 'NONE',  ( -1.000000000000000000, 0.000000000000000000, 0.000000000000000000 ) ) ;
#12843=CARTESIAN_POINT ( 'NONE',  ( 0.5084014747882494856, -0.4881889763779528324, 0.2935257283254013583 ) ) ;
#12847=CARTESIAN_POINT ( 'NONE',  ( 0.1743691514447621993, -0.4881889763779528324, 0.1734091183126679481 ) ) ;
#12849=AXIS2_PLACEMENT_3D ( 'NONE', #11145, #506, #13743 ) ;
#12853=AXIS2_PLACEMENT_3D ( 'NONE', #3655, #12109, #7694 ) ;
#12855=TOROIDAL_SURFACE ( 'NONE', #11087, 0.007874015748031495954, 0.003937007874015747977 ) ;
#12856=EDGE_LOOP ( 'NONE', ( #7675, #12467, #5403 ) ) ;
#12862=CARTESIAN_POINT ( 'NONE',  ( -0.1574803149606299191, -0.09448818897637796532, -0.5870514566507987197 ) ) ;
#12865=EDGE_CURVE ( 'NONE', #777, #9061, #149, .T. ) ;
#12866=LINE ( 'NONE', #6669, #11350 ) ;
#12868=CIRCLE ( 'NONE', #11096, 0.007874015748031499423 ) ;
#12870=PLANE ( 'NONE',  #11446 ) ;
#12875=CARTESIAN_POINT ( 'NONE',  ( 0.09842519685044820443, -0.4921259842519685179, -0.5909884645248143498 ) ) ;
#12877=CARTESIAN_POINT ( 'NONE',  ( 0.02952755905509091630, -0.09842519685039370636, -0.05114323250690790829 ) ) ;
#12880=AXIS2_PLACEMENT_3D ( 'NONE', #7662, #13703, #9864 ) ;
#12881=CIRCLE ( 'NONE', #11883, 0.003937007874015724558 ) ;
#12882=TOROIDAL_SURFACE ( 'NONE', #2624, 0.04330708661417328326, 0.003937007874015747977 ) ;
#12884=LINE ( 'NONE', #14222, #8310 ) ;
#12886=TOROIDAL_SURFACE ( 'NONE', #6610, 0.007874015748031495954, 0.003937007874015747977 ) ;
#12890=CARTESIAN_POINT ( 'NONE',  ( -0.3706061991976995484, -0.003937007874015747977, -0.2139695888701363957 ) ) ;
#12891=CARTESIAN_POINT ( 'NONE',  ( 0.5084014747882494856, -0.09842519685039370636, 0.2935257283254013583 ) ) ;
#12893=ADVANCED_FACE ( 'NONE', ( #13778 ), #12600, .T. ) ;
#12906=ORIENTED_EDGE ( 'NONE', *, *, #13234, .F. ) ;
#12907=AXIS2_PLACEMENT_3D ( 'NONE', #2324, #3353, #11907 ) ;
#12908=VECTOR ( 'NONE', #14828, 39.37007874015748143 ) ;
#12910=CIRCLE ( 'NONE', #7642, 0.003937007874015721089 ) ;
#12911=FACE_OUTER_BOUND ( 'NONE', #14759, .T. ) ;
#12914=DIRECTION ( 'NONE',  ( 0.8660254037844385966, -0.000000000000000000, -0.5000000000000001110 ) ) ;
#12918=ORIENTED_EDGE ( 'NONE', *, *, #747, .F. ) ;
#12919=CARTESIAN_POINT ( 'NONE',  ( 0.5905511811023622659, -0.2952755905511811330, -0.4584677793364514420 ) ) ;
#12920=ADVANCED_FACE ( 'NONE', ( #10249 ), #11395, .T. ) ;
#12921=CARTESIAN_POINT ( 'NONE',  ( 0.000000000000000000, 0.003937007874015860734, -0.1574803149606299191 ) ) ;
#12922=TOROIDAL_SURFACE ( 'NONE', #6146, 0.007874015748031495954, 0.003937007874015747977 ) ;
#12924=ORIENTED_EDGE ( 'NONE', *, *, #8690, .T. ) ;
#12925=ORIENTED_EDGE ( 'NONE', *, *, #2460, .F. ) ;
#12927=CIRCLE ( 'NONE', #14433, 0.003937007874015724558 ) ;
#12928=CARTESIAN_POINT ( 'NONE',  ( -0.4307978335858689833, 0.000000000000000000, 0.4279391777402706265 ) ) ;
#12929=FACE_OUTER_BOUND ( 'NONE', #12004, .T. ) ;
#12930=SPHERICAL_SURFACE ( 'NONE', #3878, 0.003937007874015747977 ) ;
#12931=LINE ( 'NONE', #5776, #4932 ) ;
#12935=DIRECTION ( 'NONE',  ( 1.445602896647339903E-16, 0.000000000000000000, -1.000000000000000000 ) ) ;
#12936=DIRECTION ( 'NONE',  ( 0.000000000000000000, 0.000000000000000000, -1.000000000000000000 ) ) ;
#12937=CIRCLE ( 'NONE', #14947, 0.003937007874015758385 ) ;
#12938=FACE_BOUND ( 'NONE', #2176, .T. ) ;
#12940=EDGE_LOOP ( 'NONE', ( #13922, #7069, #3459, #927 ) ) ;
#12944=EDGE_CURVE ( 'NONE', #5535, #12443, #7631, .T. ) ;
#12946=CIRCLE ( 'NONE', #9955, 0.003937007874015758385 ) ;
#12947=VERTEX_POINT ( 'NONE', #12824 ) ;
#12948=ORIENTED_EDGE ( 'NONE', *, *, #5458, .F. ) ;
#12949=CARTESIAN_POINT ( 'NONE',  ( -0.5084014747882513729, -0.4881889763779528324, 0.2935257283253980831 ) ) ;
#12950=CYLINDRICAL_SURFACE ( 'NONE', #6133, 0.003937007874015724558 ) ;
#12956=PLANE ( 'NONE',  #1138 ) ;
#12958=FACE_OUTER_BOUND ( 'NONE', #6653, .T. ) ;
#12962=CYLINDRICAL_SURFACE ( 'NONE', #10188, 0.003937007874015759253 ) ;
#12967=CARTESIAN_POINT ( 'NONE',  ( 0.1724006475077543565, -0.4921259842519685179, 0.1768186671464649640 ) ) ;
#12972=CARTESIAN_POINT ( 'NONE',  ( 0.3623183339751714360, -0.2952755905511811330, 0.1319014807535661138 ) ) ;
#12979=FACE_OUTER_BOUND ( 'NONE', #10720, .T. ) ;
#12981=CIRCLE ( 'NONE', #14981, 0.003937007874015749712 ) ;
#12982=EDGE_CURVE ( 'NONE', #6020, #6007, #10146, .T. ) ;
#12984=LENGTH_MEASURE_WITH_UNIT ( LENGTH_MEASURE( 0.02539999999999999897 ), #55 );
#12985=ORIENTED_EDGE ( 'NONE', *, *, #11437, .F. ) ;
#12989=ORIENTED_EDGE ( 'NONE', *, *, #7024, .F. ) ;
#12991=CARTESIAN_POINT ( 'NONE',  ( 0.09842519685044814892, -0.2952755905511811330, -0.4190977005962941426 ) ) ;
#12994=FACE_OUTER_BOUND ( 'NONE', #5469, .T. ) ;
#12996=ORIENTED_EDGE ( 'NONE', *, *, #12039, .F. ) ;
#12998=DIRECTION ( 'NONE',  ( -0.000000000000000000, -0.000000000000000000, 1.000000000000000000 ) ) ;
#13001=ADVANCED_FACE ( 'NONE', ( #8042 ), #9303, .T. ) ;
#13004=DIRECTION ( 'NONE',  ( 0.8660254037844385966, 0.000000000000000000, -0.5000000000000000000 ) ) ;
#13006=DIRECTION ( 'NONE',  ( -1.000000000000000000, -0.000000000000000000, -3.973232667114495301E-16 ) ) ;
#13008=FACE_OUTER_BOUND ( 'NONE', #11271, .T. ) ;
#13013=CARTESIAN_POINT ( 'NONE',  ( 0.2652685895082805834, -0.4881889763779528324, 0.03495519865525829883 ) ) ;
#13014=DIRECTION ( 'NONE',  ( 1.000000000000000000, 0.000000000000000000, 0.000000000000000000 ) ) ;
#13018=EDGE_LOOP ( 'NONE', ( #8099, #10530, #42, #2414 ) ) ;
#13019=EDGE_LOOP ( 'NONE', ( #7005, #13965, #5014, #5264, #14411, #11915 ) ) ;
#13020=VERTEX_POINT ( 'NONE', #8133 ) ;
#13023=FACE_OUTER_BOUND ( 'NONE', #14142, .T. ) ;
#13025=FACE_OUTER_BOUND ( 'NONE', #5142, .T. ) ;
#13028=CARTESIAN_POINT ( 'NONE',  ( 0.3492731901935992034, -0.2952755905511811330, 0.3198506632839551167 ) ) ;
#13029=DIRECTION ( 'NONE',  ( -4.336808689942014285E-16, 0.000000000000000000, 1.000000000000000000 ) ) ;
#13031=CARTESIAN_POINT ( 'NONE',  ( 0.5860051159906327634, -0.003937007874015747977, 0.1591122789105294533 ) ) ;
#13033=FACE_OUTER_BOUND ( 'NONE', #6179, .T. ) ;
#13034=ORIENTED_EDGE ( 'NONE', *, *, #2258, .T. ) ;
#13036=EDGE_CURVE ( 'NONE', #12161, #3451, #11572, .T. ) ;
#13037=ORIENTED_EDGE ( 'NONE', *, *, #4302, .F. ) ;
#13038=CARTESIAN_POINT ( 'NONE',  ( -0.5860051159906336515, -0.003937007874015747977, 0.1591122789105256508 ) ) ;
#13051=ORIENTED_EDGE ( 'NONE', *, *, #14016, .F. ) ;
#13052=ORIENTED_EDGE ( 'NONE', *, *, #8024, .F. ) ;
#13053=ADVANCED_FACE ( 'NONE', ( #1080 ), #6712, .T. ) ;
#13055=ADVANCED_FACE ( 'NONE', ( #14313 ), #5043, .T. ) ;
#13057=EDGE_CURVE ( 'NONE', #14663, #2421, #10717, .T. ) ;
#13059=DIRECTION ( 'NONE',  ( 0.000000000000000000, 1.000000000000000000, 0.000000000000000000 ) ) ;
#13062=DIRECTION ( 'NONE',  ( 0.000000000000000000, 0.000000000000000000, 1.000000000000000000 ) ) ;
#13063=DIRECTION ( 'NONE',  ( -3.973232667114494807E-16, 0.000000000000000000, 1.000000000000000000 ) ) ;
#13078=DIRECTION ( 'NONE',  ( 0.5000000000000002220, 0.000000000000000000, -0.8660254037844384856 ) ) ;
#13084=VECTOR ( 'NONE', #10790, 39.37007874015748143 ) ;
#13085=ORIENTED_EDGE ( 'NONE', *, *, #3831, .T. ) ;
#13086=AXIS2_PLACEMENT_3D ( 'NONE', #6306, #392, #9956 ) ;
#13087=ORIENTED_EDGE ( 'NONE', *, *, #10612, .F. ) ;
#13088=CARTESIAN_POINT ( 'NONE',  ( 0.1618514667033794374, -0.1023622047244094474, 0.2122517380126066888 ) ) ;
#13090=FACE_OUTER_BOUND ( 'NONE', #15221, .T. ) ;
#13094=TOROIDAL_SURFACE ( 'NONE', #6316, 0.007874015748031495954, 0.003937007874015747977 ) ;
#13095=DIRECTION ( 'NONE',  ( 0.8660254037844387076, 0.000000000000000000, -0.4999999999999999445 ) ) ;
#13106=AXIS2_PLACEMENT_3D ( 'NONE', #10613, #11487, #753 ) ;
#13107=ORIENTED_EDGE ( 'NONE', *, *, #14776, .T. ) ;
#13108=AXIS2_PLACEMENT_3D ( 'NONE', #6206, #8332, #14294 ) ;
#13109=ORIENTED_EDGE ( 'NONE', *, *, #6447, .T. ) ;
#13110=AXIS2_PLACEMENT_3D ( 'NONE', #6954, #2303, #2388 ) ;
#13114=AXIS2_PLACEMENT_3D ( 'NONE', #1519, #14765, #6271 ) ;
#13119=CARTESIAN_POINT ( 'NONE',  ( -0.1618514667033796040, -0.4881889763779528324, 0.2122517380126066888 ) ) ;
#13120=DIRECTION ( 'NONE',  ( 0.000000000000000000, 1.000000000000000000, 0.000000000000000000 ) ) ;
#13122=VECTOR ( 'NONE', #14006, 39.37007874015748143 ) ;
#13124=AXIS2_PLACEMENT_3D ( 'NONE', #14090, #718, #949 ) ;
#13128=ADVANCED_FACE ( 'NONE', ( #1245 ), #14918, .T. ) ;
#13131=VERTEX_POINT ( 'NONE', #3576 ) ;
#13132=VERTEX_POINT ( 'NONE', #7260 ) ;
#13134=EDGE_CURVE ( 'NONE', #10775, #11599, #4896, .T. ) ;
#13135=CIRCLE ( 'NONE', #4371, 0.04330708661417331101 ) ;
#13136=CIRCLE ( 'NONE', #2374, 0.04330708661417331101 ) ;
#13141=DIRECTION ( 'NONE',  ( 0.4999999999999979461, 0.000000000000000000, 0.8660254037844398178 ) ) ;
#13144=VERTEX_POINT ( 'NONE', #7325 ) ;
#13146=DIRECTION ( 'NONE',  ( -0.4999999999999966693, 0.000000000000000000, -0.8660254037844405950 ) ) ;
#13147=CARTESIAN_POINT ( 'NONE',  ( 0.4307978335858664853, -0.003937007874015747977, 0.4318761856142889766 ) ) ;
#13148=ADVANCED_FACE ( 'NONE', ( #3808 ), #152, .T. ) ;
#13149=AXIS2_PLACEMENT_3D ( 'NONE', #6785, #844, #10410 ) ;
#13150=AXIS2_PLACEMENT_3D ( 'NONE', #13491, #849, #8866 ) ;
#13152=EDGE_CURVE ( 'NONE', #7115, #7217, #6892, .T. ) ;
#13155=EDGE_LOOP ( 'NONE', ( #5806, #13804, #3785 ) ) ;
#13157=ADVANCED_FACE ( 'NONE', ( #2409 ), #12125, .T. ) ;
#13158=ORIENTED_EDGE ( 'NONE', *, *, #2538, .F. ) ;
#13160=AXIS2_PLACEMENT_3D ( 'NONE', #1847, #12669, #10238 ) ;
#13171=EDGE_CURVE ( 'NONE', #8390, #12616, #7189, .T. ) ;
#13173=DIRECTION ( 'NONE',  ( 0.000000000000000000, 0.000000000000000000, 1.000000000000000000 ) ) ;
#13179=VERTEX_POINT ( 'NONE', #1474 ) ;
#13180=AXIS2_PLACEMENT_3D ( 'NONE', #14907, #2991, #10201 ) ;
#13181=DIRECTION ( 'NONE',  ( -0.000000000000000000, -1.000000000000000000, -0.000000000000000000 ) ) ;
#13185=CARTESIAN_POINT ( 'NONE',  ( -0.1618514667033796040, -0.4921259842519685179, 0.2161887458866224576 ) ) ;
#13186=FACE_OUTER_BOUND ( 'NONE', #15289, .T. ) ;
#13189=ORIENTED_EDGE ( 'NONE', *, *, #9028, .T. ) ;
#13191=CARTESIAN_POINT ( 'NONE',  ( -0.2613315816341005848, -0.4921259842519685179, 0.03601011673560078341 ) ) ;
#13193=CARTESIAN_POINT ( 'NONE',  ( -0.4141303577462134844, -0.2952755905511811330, 0.1209005806194722171 ) ) ;
#13195=CIRCLE ( 'NONE', #14943, 0.003937007874015761855 ) ;
#13197=ORIENTED_EDGE ( 'NONE', *, *, #4166, .T. ) ;
#13200=ORIENTED_EDGE ( 'NONE', *, *, #14318, .F. ) ;
#13201=VECTOR ( 'NONE', #13705, 39.37007874015748143 ) ;
#13203=DIRECTION ( 'NONE',  ( -1.000000000000000000, -0.000000000000000000, -3.476578583725179813E-16 ) ) ;
#13205=EDGE_CURVE ( 'NONE', #11006, #6292, #8907, .T. ) ;
#13206=DIRECTION ( 'NONE',  ( 0.000000000000000000, 0.000000000000000000, -1.000000000000000000 ) ) ;
#13207=DIRECTION ( 'NONE',  ( -0.4999999999999966693, 0.000000000000000000, 0.8660254037844405950 ) ) ;
#13209=VECTOR ( 'NONE', #8951, 39.37007874015748143 ) ;
#13210=DIRECTION ( 'NONE',  ( 0.000000000000000000, 0.000000000000000000, 1.000000000000000000 ) ) ;
#13212=CIRCLE ( 'NONE', #11719, 0.003937007874015741038 ) ;
#13213=DIRECTION ( 'NONE',  ( -0.000000000000000000, 1.000000000000000000, 0.000000000000000000 ) ) ;
#13218=CIRCLE ( 'NONE', #10466, 0.1574803149606299191 ) ;
#13219=DIRECTION ( 'NONE',  ( 0.000000000000000000, 0.000000000000000000, -1.000000000000000000 ) ) ;
#13220=DIRECTION ( 'NONE',  ( 0.8660254037844405950, 0.000000000000000000, 0.4999999999999967804 ) ) ;
#13221=AXIS2_PLACEMENT_3D ( 'NONE', #10339, #5002, #1423 ) ;
#13222=DIRECTION ( 'NONE',  ( 1.000000000000000000, 0.000000000000000000, 0.000000000000000000 ) ) ;
#13223=DIRECTION ( 'NONE',  ( -0.000000000000000000, -1.000000000000000000, -0.000000000000000000 ) ) ;
#13225=FACE_OUTER_BOUND ( 'NONE', #5451, .T. ) ;
#13227=DIRECTION ( 'NONE',  ( 1.000000000000000000, -1.734723475976802677E-14, 0.000000000000000000 ) ) ;
#13228=DIRECTION ( 'NONE',  ( 0.4999999999999979461, -0.000000000000000000, 0.8660254037844398178 ) ) ;
#13229=AXIS2_PLACEMENT_3D ( 'NONE', #246, #313, #12150 ) ;
#13230=ORIENTED_EDGE ( 'NONE', *, *, #4353, .T. ) ;
#13231=EDGE_LOOP ( 'NONE', ( #3748, #8841, #3984, #6255 ) ) ;
#13234=EDGE_CURVE ( 'NONE', #10253, #13441, #2151, .T. ) ;
#13235=EDGE_CURVE ( 'NONE', #7381, #14387, #13993, .T. ) ;
#13236=CYLINDRICAL_SURFACE ( 'NONE', #13366, 0.003937007874015749712 ) ;
#13239=FACE_OUTER_BOUND ( 'NONE', #4881, .T. ) ;
#13242=DIRECTION ( 'NONE',  ( -3.973232667114495301E-16, 0.000000000000000000, 1.000000000000000000 ) ) ;
#13243=EDGE_CURVE ( 'NONE', #14035, #5216, #3654, .T. ) ;
#13246=ORIENTED_EDGE ( 'NONE', *, *, #9611, .F. ) ;
#13247=ORIENTED_EDGE ( 'NONE', *, *, #9538, .F. ) ;
#13248=ORIENTED_EDGE ( 'NONE', *, *, #10757, .T. ) ;
#13249=ADVANCED_FACE ( 'NONE', ( #7118 ), #11879, .T. ) ;
#13251=FACE_OUTER_BOUND ( 'NONE', #9736, .T. ) ;
#13260=EDGE_CURVE ( 'NONE', #8290, #12501, #9151, .T. ) ;
#13261=ADVANCED_FACE ( 'NONE', ( #5815 ), #11735, .F. ) ;
#13267=ORIENTED_EDGE ( 'NONE', *, *, #1089, .T. ) ;
#13268=ORIENTED_EDGE ( 'NONE', *, *, #11997, .F. ) ;
#13270=DIRECTION ( 'NONE',  ( 0.000000000000000000, -0.000000000000000000, 1.000000000000000000 ) ) ;
#13271=CARTESIAN_POINT ( 'NONE',  ( -0.4342073824196659437, -0.09448818897637796532, 0.4299076816772785525 ) ) ;
#13273=FACE_OUTER_BOUND ( 'NONE', #1248, .T. ) ;
#13274=DIRECTION ( 'NONE',  ( 0.8660254037844383745, 0.000000000000000000, -0.5000000000000004441 ) ) ;
#13275=DIRECTION ( 'NONE',  ( 0.000000000000000000, -1.000000000000000000, 0.000000000000000000 ) ) ;
#13276=EDGE_CURVE ( 'NONE', #9540, #253, #10468, .T. ) ;
#13277=CARTESIAN_POINT ( 'NONE',  ( 0.05905511811029064834, -0.09448818897637796532, -0.5909884645248143498 ) ) ;
#13279=DIRECTION ( 'NONE',  ( 0.000000000000000000, 0.000000000000000000, 1.000000000000000000 ) ) ;
#13280=ORIENTED_EDGE ( 'NONE', *, *, #8982, .T. ) ;
#13281=ADVANCED_FACE ( 'NONE', ( #3560 ), #12665, .F. ) ;
#13282=ORIENTED_EDGE ( 'NONE', *, *, #2672, .F. ) ;
#13283=VERTEX_POINT ( 'NONE', #7013 ) ;
#13287=FACE_OUTER_BOUND ( 'NONE', #12179, .T. ) ;
#13288=DIRECTION ( 'NONE',  ( 0.5000000000000035527, 0.000000000000000000, -0.8660254037844365982 ) ) ;
#13289=CARTESIAN_POINT ( 'NONE',  ( 0.4307978335858664853, -0.09448818897637796532, 0.4318761856142889766 ) ) ;
#13291=CARTESIAN_POINT ( 'NONE',  ( 0.000000000000000000, 2.161417322834645827, 0.000000000000000000 ) ) ;
#13292=DIRECTION ( 'NONE',  ( -1.000000000000000000, -0.000000000000000000, -3.476578583725179813E-16 ) ) ;
#13296=VERTEX_POINT ( 'NONE', #4505 ) ;
#13305=VERTEX_POINT ( 'NONE', #13119 ) ;
#13308=ORIENTED_EDGE ( 'NONE', *, *, #13260, .T. ) ;
#13310=EDGE_LOOP ( 'NONE', ( #14524, #12302, #9252, #2669 ) ) ;
#13311=EDGE_CURVE ( 'NONE', #11994, #10116, #12910, .T. ) ;
#13317=CARTESIAN_POINT ( 'NONE',  ( 0.06692913385832209572, -0.1023622047244094474, -0.2377126739437405434 ) ) ;
#13321=DIRECTION ( 'NONE',  ( 0.5000000000000245359, -0.000000000000000000, 0.8660254037844243857 ) ) ;
#13324=DIRECTION ( 'NONE',  ( -0.5000000000000001110, 0.000000000000000000, 0.8660254037844387076 ) ) ;
#13325=DIRECTION ( 'NONE',  ( -0.8660254037844405950, 0.000000000000000000, 0.4999999999999966693 ) ) ;
#13329=DIRECTION ( 'NONE',  ( -1.000000000000000000, 0.000000000000000000, 0.000000000000000000 ) ) ;
#13332=ORIENTED_EDGE ( 'NONE', *, *, #7495, .F. ) ;
#13333=ORIENTED_EDGE ( 'NONE', *, *, #2258, .F. ) ;
#13334=ORIENTED_EDGE ( 'NONE', *, *, #9016, .T. ) ;
#13337=CARTESIAN_POINT ( 'NONE',  ( -0.5860051159906336515, -0.003937007874015747977, 0.1591122789105256785 ) ) ;
#13343=SPHERICAL_SURFACE ( 'NONE', #14843, 0.003937007874015747977 ) ;
#13349=CARTESIAN_POINT ( 'NONE',  ( 0.06692913385832209572, -0.09842519685039370636, -0.2377126739437405434 ) ) ;
#13351=DIRECTION ( 'NONE',  ( -0.8660254037844405950, 0.000000000000000000, -0.4999999999999966693 ) ) ;
#13354=AXIS2_PLACEMENT_3D ( 'NONE', #6911, #5559, #5494 ) ;
#13355=EDGE_CURVE ( 'NONE', #14974, #4713, #15157, .T. ) ;
#13356=VERTEX_POINT ( 'NONE', #2474 ) ;
#13357=AXIS2_PLACEMENT_3D ( 'NONE', #10701, #10835, #995 ) ;
#13358=VECTOR ( 'NONE', #12565, 39.37007874015748143 ) ;
#13363=CIRCLE ( 'NONE', #4849, 0.003937007874015724558 ) ;
#13365=CARTESIAN_POINT ( 'NONE',  ( 0.2919796512831356883, -0.2952755905511811330, 0.2458576371656085724 ) ) ;
#13366=AXIS2_PLACEMENT_3D ( 'NONE', #6973, #4703, #11763 ) ;
#13367=ADVANCED_FACE ( 'NONE', ( #10924 ), #1296, .T. ) ;
#13369=AXIS2_PLACEMENT_3D ( 'NONE', #6549, #711, #7980 ) ;
#13372=ORIENTED_EDGE ( 'NONE', *, *, #1148, .T. ) ;
#13374=FACE_OUTER_BOUND ( 'NONE', #1303, .T. ) ;
#13377=VERTEX_POINT ( 'NONE', #11064 ) ;
#13378=CIRCLE ( 'NONE', #865, 0.007874015748031499423 ) ;
#13380=VECTOR ( 'NONE', #15305, 39.37007874015748143 ) ;
#13385=AXIS2_PLACEMENT_3D ( 'NONE', #5305, #5540, #1802 ) ;
#13388=FACE_OUTER_BOUND ( 'NONE', #11158, .T. ) ;
#13395=CIRCLE ( 'NONE', #14395, 0.04330708661417331101 ) ;
#13401=ORIENTED_EDGE ( 'NONE', *, *, #1352, .F. ) ;
#13403=CIRCLE ( 'NONE', #10151, 0.04330708661417331101 ) ;
#13405=LINE ( 'NONE', #11514, #6346 ) ;
#13409=DIRECTION ( 'NONE',  ( -0.000000000000000000, 1.000000000000000000, -0.000000000000000000 ) ) ;
#13412=EDGE_LOOP ( 'NONE', ( #3015, #5975, #4476, #2827, #9944, #5990, #9795, #7909, #7266, #9278, #10165, #958, #13480, #14642, #7020, #14392 ) ) ;
#13414=CARTESIAN_POINT ( 'NONE',  ( -0.06692913385815735250, -0.4921259842519685179, -0.5870514566507987197 ) ) ;
#13415=CARTESIAN_POINT ( 'NONE',  ( -0.06299212598414173636, -0.4921259842519685179, -0.2366577558633980449 ) ) ;
#13417=DIRECTION ( 'NONE',  ( 0.000000000000000000, 1.000000000000000000, 0.000000000000000000 ) ) ;
#13418=EDGE_CURVE ( 'NONE', #13771, #4031, #2650, .T. ) ;
#13422=ORIENTED_EDGE ( 'NONE', *, *, #4833, .F. ) ;
#13423=ORIENTED_EDGE ( 'NONE', *, *, #7677, .T. ) ;
#13426=CARTESIAN_POINT ( 'NONE',  ( -0.06692913385815747740, -0.4881889763779528324, -0.2377126739438355507 ) ) ;
#13430=DIRECTION ( 'NONE',  ( 0.4999999999999999445, 0.000000000000000000, 0.8660254037844387076 ) ) ;
#13431=AXIS2_PLACEMENT_3D ( 'NONE', #1437, #9813, #14581 ) ;
#13436=CIRCLE ( 'NONE', #11697, 0.003937007874015758385 ) ;
#13441=VERTEX_POINT ( 'NONE', #10838 ) ;
#13442=ORIENTED_EDGE ( 'NONE', *, *, #988, .T. ) ;
#13461=CIRCLE ( 'NONE', #6691, 0.003937007874015724558 ) ;
#13462=ORIENTED_EDGE ( 'NONE', *, *, #13276, .T. ) ;
#13463=VERTEX_POINT ( 'NONE', #9828 ) ;
#13467=CYLINDRICAL_SURFACE ( 'NONE', #8917, 0.003937007874015721089 ) ;
#13471=SPHERICAL_SURFACE ( 'NONE', #13229, 0.003937007874015747977 ) ;
#13477=EDGE_CURVE ( 'NONE', #2079, #2454, #12677, .T. ) ;
#13480=ORIENTED_EDGE ( 'NONE', *, *, #2648, .T. ) ;
#13482=EDGE_CURVE ( 'NONE', #1905, #7883, #14608, .T. ) ;
#13484=CARTESIAN_POINT ( 'NONE',  ( -0.5860051159906336515, -0.09448818897637796532, 0.1591122789105256785 ) ) ;
#13487=DIRECTION ( 'NONE',  ( -1.000000000000000000, -0.000000000000000000, -1.445602896647339903E-16 ) ) ;
#13491=CARTESIAN_POINT ( 'NONE',  ( -0.05905511811012585655, -0.1023622047244094474, -0.5870514566507987197 ) ) ;
#13498=DIRECTION ( 'NONE',  ( 1.000000000000000000, 0.000000000000000000, 0.000000000000000000 ) ) ;
#13501=DIRECTION ( 'NONE',  ( -0.000000000000000000, -0.000000000000000000, 1.000000000000000000 ) ) ;
#13504=DIRECTION ( 'NONE',  ( 1.445602896647339903E-16, 0.000000000000000000, -1.000000000000000000 ) ) ;
#13507=VERTEX_POINT ( 'NONE', #7396 ) ;
#13509=VERTEX_POINT ( 'NONE', #1523 ) ;
#13511=ORIENTED_EDGE ( 'NONE', *, *, #11828, .F. ) ;
#13515=DIRECTION ( 'NONE',  ( -1.000000000000000000, 0.000000000000000000, 0.000000000000000000 ) ) ;
#13526=ORIENTED_EDGE ( 'NONE', *, *, #4674, .T. ) ;
#13528=ORIENTED_EDGE ( 'NONE', *, *, #6509, .T. ) ;
#13529=VERTEX_POINT ( 'NONE', #11153 ) ;
#13531=EDGE_CURVE ( 'NONE', #8021, #9271, #1822, .T. ) ;
#13532=EDGE_CURVE ( 'NONE', #12009, #10253, #1178, .T. ) ;
#13533=DIRECTION ( 'NONE',  ( -1.000000000000000000, 0.000000000000000000, 0.000000000000000000 ) ) ;
#13542=ORIENTED_EDGE ( 'NONE', *, *, #10893, .F. ) ;
#13543=ORIENTED_EDGE ( 'NONE', *, *, #1233, .F. ) ;
#13545=ADVANCED_FACE ( 'NONE', ( #1685 ), #12564, .F. ) ;
#13546=ADVANCED_FACE ( 'NONE', ( #6676 ), #2905, .T. ) ;
#13549=DIRECTION ( 'NONE',  ( 0.4999999999999966693, 0.000000000000000000, 0.8660254037844405950 ) ) ;
#13553=EDGE_CURVE ( 'NONE', #12443, #5050, #913, .T. ) ;
#13557=CARTESIAN_POINT ( 'NONE',  ( -0.1062992125983150127, -0.4921259842519685179, -0.2482618547482104143 ) ) ;
#13558=VERTEX_POINT ( 'NONE', #9041 ) ;
#13559=VERTEX_POINT ( 'NONE', #4097 ) ;
#13562=CARTESIAN_POINT ( 'NONE',  ( 0.3137366569588399545, -0.2952755905511811330, 0.2947875711430715251 ) ) ;
#13567=DIRECTION ( 'NONE',  ( 1.000000000000000000, 0.000000000000000000, 0.000000000000000000 ) ) ;
#13568=DIRECTION ( 'NONE',  ( 0.8660254037844368202, 0.000000000000000000, -0.5000000000000032196 ) ) ;
#13572=DIRECTION ( 'NONE',  ( 0.8660254037844347108, 0.000000000000000000, -0.5000000000000069944 ) ) ;
#13573=ORIENTED_EDGE ( 'NONE', *, *, #4679, .F. ) ;
#13577=VECTOR ( 'NONE', #8813, 39.37007874015748143 ) ;
#13579=TOROIDAL_SURFACE ( 'NONE', #14081, 0.04330708661417328326, 0.003937007874015747977 ) ;
#13583=LINE ( 'NONE', #7644, #9716 ) ;
#13584=FACE_OUTER_BOUND ( 'NONE', #12856, .T. ) ;
#13587=AXIS2_PLACEMENT_3D ( 'NONE', #12188, #6127, #4964 ) ;
#13588=DIRECTION ( 'NONE',  ( 1.000000000000000000, 0.000000000000000000, 3.973232667114495301E-16 ) ) ;
#13589=EDGE_CURVE ( 'NONE', #12219, #6685, #14425, .T. ) ;
#13595=ORIENTED_EDGE ( 'NONE', *, *, #8343, .T. ) ;
#13596=EDGE_CURVE ( 'NONE', #14774, #9212, #3916, .T. ) ;
#13601=ORIENTED_EDGE ( 'NONE', *, *, #6336, .T. ) ;
#13602=VECTOR ( 'NONE', #14465, 39.37007874015748143 ) ;
#13603=CIRCLE ( 'NONE', #114, 0.003937007874015750579 ) ;
#13605=VECTOR ( 'NONE', #7070, 39.37007874015748143 ) ;
#13606=AXIS2_PLACEMENT_3D ( 'NONE', #9594, #14374, #7012 ) ;
#13607=CYLINDRICAL_SURFACE ( 'NONE', #5561, 0.003937007874015758385 ) ;
#13611=FACE_OUTER_BOUND ( 'NONE', #8923, .T. ) ;
#13612=VECTOR ( 'NONE', #10800, 39.37007874015748143 ) ;
#13623=DIRECTION ( 'NONE',  ( -0.5000000000000069944, -8.673617379884209021E-15, 0.8660254037844347108 ) ) ;
#13625=CIRCLE ( 'NONE', #6103, 0.003937007874015762722 ) ;
#13628=ORIENTED_EDGE ( 'NONE', *, *, #8682, .F. ) ;
#13629=TOROIDAL_SURFACE ( 'NONE', #12124, 0.04330708661417328326, 0.003937007874015747977 ) ;
#13630=EDGE_CURVE ( 'NONE', #9261, #5839, #15066, .T. ) ;
#13632=AXIS2_PLACEMENT_3D ( 'NONE', #6493, #6559, #13640 ) ;
#13634=EDGE_LOOP ( 'NONE', ( #448, #194, #1383, #13803 ) ) ;
#13637=AXIS2_PLACEMENT_3D ( 'NONE', #10611, #3322, #8265 ) ;
#13638=EDGE_CURVE ( 'NONE', #10586, #10807, #11673, .T. ) ;
#13640=DIRECTION ( 'NONE',  ( 0.5000000000000226485, 0.000000000000000000, -0.8660254037844253849 ) ) ;
#13641=CARTESIAN_POINT ( 'NONE',  ( 0.1724006475077543565, -0.4881889763779528324, 0.1768186671464649640 ) ) ;
#13643=AXIS2_PLACEMENT_3D ( 'NONE', #11815, #3205, #2015 ) ;
#13646=VERTEX_POINT ( 'NONE', #9441 ) ;
#13653=AXIS2_PLACEMENT_3D ( 'NONE', #11948, #5618, #11132 ) ;
#13654=AXIS2_PLACEMENT_3D ( 'NONE', #15295, #9190, #10589 ) ;
#13655=ORIENTED_EDGE ( 'NONE', *, *, #14574, .T. ) ;
#13656=EDGE_LOOP ( 'NONE', ( #10291, #6054, #12079, #11808 ) ) ;
#13657=AXIS2_PLACEMENT_3D ( 'NONE', #1394, #6153, #13288 ) ;
#13666=DIRECTION ( 'NONE',  ( 0.8660254037844385966, -0.000000000000000000, 0.5000000000000001110 ) ) ;
#13667=CIRCLE ( 'NONE', #12375, 0.003937007874015721089 ) ;
#13668=DIRECTION ( 'NONE',  ( -0.4999999999999928946, -0.000000000000000000, -0.8660254037844428154 ) ) ;
#13670=DIRECTION ( 'NONE',  ( 0.8660254037844385966, 0.000000000000000000, 0.5000000000000000000 ) ) ;
#13672=CARTESIAN_POINT ( 'NONE',  ( -0.4330708661417336236, -0.09448818897637796532, 0.4279391777402706265 ) ) ;
#13673=ADVANCED_FACE ( 'NONE', ( #15398 ), #4907, .T. ) ;
#13674=ORIENTED_EDGE ( 'NONE', *, *, #1570, .F. ) ;
#13676=EDGE_LOOP ( 'NONE', ( #2155, #1103, #8454, #14938 ) ) ;
#13680=EDGE_CURVE ( 'NONE', #713, #7744, #15432, .T. ) ;
#13681=CIRCLE ( 'NONE', #13180, 0.03937007874015751446 ) ;
#13692=LINE ( 'NONE', #9059, #2161 ) ;
#13694=ORIENTED_EDGE ( 'NONE', *, *, #14821, .T. ) ;
#13696=CIRCLE ( 'NONE', #4181, 0.003937007874015724558 ) ;
#13700=CIRCLE ( 'NONE', #2437, 0.003937007874015747977 ) ;
#13701=FACE_OUTER_BOUND ( 'NONE', #4127, .T. ) ;
#13702=CARTESIAN_POINT ( 'NONE',  ( 0.5398975377803496567, -0.4881889763779528324, 0.2389729469846946508 ) ) ;
#13703=DIRECTION ( 'NONE',  ( 0.000000000000000000, 1.000000000000000000, -0.000000000000000000 ) ) ;
#13705=DIRECTION ( 'NONE',  ( -0.000000000000000000, -1.000000000000000000, -0.000000000000000000 ) ) ;
#13707=DIRECTION ( 'NONE',  ( 0.000000000000000000, 0.000000000000000000, 1.000000000000000000 ) ) ;
#13711=ORIENTED_EDGE ( 'NONE', *, *, #13205, .F. ) ;
#13714=AXIS2_PLACEMENT_3D ( 'NONE', #9704, #14479, #11011 ) ;
#13716=ORIENTED_EDGE ( 'NONE', *, *, #12322, .F. ) ;
#13718=CIRCLE ( 'NONE', #12727, 0.003937007874015741038 ) ;
#13719=EDGE_CURVE ( 'NONE', #8551, #12353, #5887, .T. ) ;
#13724=ADVANCED_FACE ( 'NONE', ( #890 ), #12922, .T. ) ;
#13725=CARTESIAN_POINT ( 'NONE',  ( -0.5894146648244306119, -0.003937007874015747977, 0.1571437749735178357 ) ) ;
#13727=AXIS2_PLACEMENT_3D ( 'NONE', #1471, #8745, #12120 ) ;
#13728=CARTESIAN_POINT ( 'NONE',  ( -0.05905511811012585655, -0.09448818897637796532, -0.5870514566507987197 ) ) ;
#13730=ORIENTED_EDGE ( 'NONE', *, *, #6715, .T. ) ;
#13731=CARTESIAN_POINT ( 'NONE',  ( -0.4822834645669299425, -0.1023622047244094474, 0.3466374647693608591 ) ) ;
#13732=CARTESIAN_POINT ( 'NONE',  ( 0.06299212598430634080, -0.1023622047244094474, -0.2366577558633030653 ) ) ;
#13734=DIRECTION ( 'NONE',  ( -1.000000000000000000, 0.000000000000000000, 0.000000000000000000 ) ) ;
#13736=ORIENTED_EDGE ( 'NONE', *, *, #2467, .T. ) ;
#13741=LINE ( 'NONE', #4018, #2401 ) ;
#13742=ADVANCED_FACE ( 'NONE', ( #12958 ), #6997, .F. ) ;
#13743=DIRECTION ( 'NONE',  ( -0.5000000000000001110, 0.000000000000000000, 0.8660254037844384856 ) ) ;
#13744=DIRECTION ( 'NONE',  ( 0.4999999999999991118, -2.275781674304493770E-14, 0.8660254037844391517 ) ) ;
#13746=FACE_OUTER_BOUND ( 'NONE', #5037, .T. ) ;
#13747=DIRECTION ( 'NONE',  ( 4.336808689942014285E-16, 0.000000000000000000, -1.000000000000000000 ) ) ;
#13751=FACE_OUTER_BOUND ( 'NONE', #11141, .T. ) ;
#13754=DIRECTION ( 'NONE',  ( -3.476578583725179813E-16, -0.000000000000000000, 1.000000000000000000 ) ) ;
#13756=EDGE_LOOP ( 'NONE', ( #8642, #2142, #14686 ) ) ;
#13759=ADVANCED_FACE ( 'NONE', ( #11713 ), #808, .F. ) ;
#13761=CARTESIAN_POINT ( 'NONE',  ( -0.1804058482824386078, -0.4921259842519685179, -0.1041573650692488584 ) ) ;
#13769=ORIENTED_EDGE ( 'NONE', *, *, #7721, .F. ) ;
#13771=VERTEX_POINT ( 'NONE', #13028 ) ;
#13775=DIRECTION ( 'NONE',  ( -0.8660254037844501429, 0.000000000000000000, 0.4999999999999798495 ) ) ;
#13776=DIRECTION ( 'NONE',  ( 0.000000000000000000, -0.000000000000000000, 1.000000000000000000 ) ) ;
#13777=CARTESIAN_POINT ( 'NONE',  ( -0.1724006475077544398, -0.1023622047244094474, 0.1768186671464649640 ) ) ;
#13778=FACE_OUTER_BOUND ( 'NONE', #13756, .T. ) ;
#13779=CARTESIAN_POINT ( 'NONE',  ( 0.5905511811023622659, -0.2952755905511811330, -0.4190977005962939206 ) ) ;
#13782=EDGE_LOOP ( 'NONE', ( #5751, #14289, #6097, #6535 ) ) ;
#13786=ORIENTED_EDGE ( 'NONE', *, *, #11312, .F. ) ;
#13787=ORIENTED_EDGE ( 'NONE', *, *, #2702, .T. ) ;
#13788=ORIENTED_EDGE ( 'NONE', *, *, #11535, .T. ) ;
#13789=CARTESIAN_POINT ( 'NONE',  ( 0.000000000000000000, 2.161417322834645827, 0.1535433070866141780 ) ) ;
#13793=ORIENTED_EDGE ( 'NONE', *, *, #1397, .F. ) ;
#13795=CARTESIAN_POINT ( 'NONE',  ( -0.5576140732134202693, -0.4921259842519685179, 0.2082870074805209248 ) ) ;
#13800=CARTESIAN_POINT ( 'NONE',  ( -0.4516353949179805483, -0.2952755905511811330, 0.1425541239265588345 ) ) ;
#13801=ORIENTED_EDGE ( 'NONE', *, *, #3753, .T. ) ;
#13802=EDGE_CURVE ( 'NONE', #12552, #10256, #3779, .T. ) ;
#13803=ORIENTED_EDGE ( 'NONE', *, *, #1268, .T. ) ;
#13804=ORIENTED_EDGE ( 'NONE', *, *, #5770, .T. ) ;
#13811=DIRECTION ( 'NONE',  ( 4.336808689942006692E-15, 0.000000000000000000, -1.000000000000000000 ) ) ;
#13817=EDGE_LOOP ( 'NONE', ( #7701, #4797, #5661 ) ) ;
#13819=EDGE_CURVE ( 'NONE', #14414, #9446, #4670, .T. ) ;
#13820=ORIENTED_EDGE ( 'NONE', *, *, #4444, .F. ) ;
#13821=ORIENTED_EDGE ( 'NONE', *, *, #10282, .T. ) ;
#13822=DIRECTION ( 'NONE',  ( 0.4999999999999966693, 0.000000000000000000, 0.8660254037844405950 ) ) ;
#13826=DIRECTION ( 'NONE',  ( -0.5000000000000004441, -0.000000000000000000, 0.8660254037844382635 ) ) ;
#13828=ADVANCED_FACE ( 'NONE', ( #106 ), #11947, .T. ) ;
#13829=DIRECTION ( 'NONE',  ( 3.476578583725179813E-16, 0.000000000000000000, -1.000000000000000000 ) ) ;
#13830=CARTESIAN_POINT ( 'NONE',  ( 0.1724006475077543565, -0.1023622047244094474, 0.1728816592724491952 ) ) ;
#13834=EDGE_CURVE ( 'NONE', #2262, #13144, #6256, .T. ) ;
#13835=ORIENTED_EDGE ( 'NONE', *, *, #12483, .T. ) ;
#13836=AXIS2_PLACEMENT_3D ( 'NONE', #2703, #4024, #14609 ) ;
#13838=ORIENTED_EDGE ( 'NONE', *, *, #1397, .T. ) ;
#13840=ADVANCED_FACE ( 'NONE', ( #7294 ), #7455, .T. ) ;
#13842=DIRECTION ( 'NONE',  ( 0.000000000000000000, 0.000000000000000000, -1.000000000000000000 ) ) ;
#13843=AXIS2_PLACEMENT_3D ( 'NONE', #833, #4516, #14244 ) ;
#13844=AXIS2_PLACEMENT_3D ( 'NONE', #12744, #6765, #11553 ) ;
#13845=FACE_OUTER_BOUND ( 'NONE', #3018, .T. ) ;
#13846=CIRCLE ( 'NONE', #8087, 0.007874015748031499423 ) ;
#13848=DIRECTION ( 'NONE',  ( 0.000000000000000000, 0.000000000000000000, -1.000000000000000000 ) ) ;
#13853=CARTESIAN_POINT ( 'NONE',  ( -0.1629063847838169987, -0.1023622047244094474, 0.2122517380126066888 ) ) ;
#13855=VERTEX_POINT ( 'NONE', #3847 ) ;
#13856=VERTEX_POINT ( 'NONE', #9894 ) ;
#13859=CIRCLE ( 'NONE', #8864, 0.003937007874015746242 ) ;
#13861=ORIENTED_EDGE ( 'NONE', *, *, #9352, .F. ) ;
#13865=DIRECTION ( 'NONE',  ( 0.4999999999999995004, 0.000000000000000000, 0.8660254037844390407 ) ) ;
#13868=CIRCLE ( 'NONE', #10620, 0.003937007874015750579 ) ;
#13869=DIRECTION ( 'NONE',  ( -1.000000000000000000, 0.000000000000000000, 0.000000000000000000 ) ) ;
#13870=VECTOR ( 'NONE', #10619, 39.37007874015748143 ) ;
#13871=ORIENTED_EDGE ( 'NONE', *, *, #1236, .T. ) ;
#13872=DIRECTION ( 'NONE',  ( 0.8660254037844383745, 0.000000000000000000, -0.5000000000000004441 ) ) ;
#13880=ORIENTED_EDGE ( 'NONE', *, *, #13532, .T. ) ;
#13881=CIRCLE ( 'NONE', #6101, 0.04330708661417331101 ) ;
#13888=CARTESIAN_POINT ( 'NONE',  ( -0.4769054117961255002, -0.1023622047244094474, 0.3480785096661502265 ) ) ;
#13891=VERTEX_POINT ( 'NONE', #1280 ) ;
#13892=DIRECTION ( 'NONE',  ( -0.8660254037844383745, 0.000000000000000000, -0.5000000000000002220 ) ) ;
#13894=DIRECTION ( 'NONE',  ( 0.000000000000000000, 0.000000000000000000, 1.000000000000000000 ) ) ;
#13895=AXIS2_PLACEMENT_3D ( 'NONE', #10198, #6652, #10267 ) ;
#13898=DIRECTION ( 'NONE',  ( 0.000000000000000000, 0.000000000000000000, -1.000000000000000000 ) ) ;
#13901=ORIENTED_EDGE ( 'NONE', *, *, #59, .F. ) ;
#13903=VERTEX_POINT ( 'NONE', #8406 ) ;
#13905=ADVANCED_FACE ( 'NONE', ( #2590, #2455 ), #12170, .F. ) ;
#13906=AXIS2_PLACEMENT_3D ( 'NONE', #1677, #8880, #8725 ) ;
#13907=AXIS2_PLACEMENT_3D ( 'NONE', #6532, #691, #9222 ) ;
#13910=DIRECTION ( 'NONE',  ( 0.000000000000000000, 1.000000000000000000, 0.000000000000000000 ) ) ;
#13911=CARTESIAN_POINT ( 'NONE',  ( -0.06692913385815735250, -0.4921259842519685179, -0.5870514566507987197 ) ) ;
#13915=LINE ( 'NONE', #10467, #6950 ) ;
#13916=EDGE_CURVE ( 'NONE', #12552, #15201, #11680, .T. ) ;
#13922=ORIENTED_EDGE ( 'NONE', *, *, #3154, .F. ) ;
#13924=EDGE_LOOP ( 'NONE', ( #14726, #3709, #56, #5414 ) ) ;
#13927=EDGE_CURVE ( 'NONE', #11529, #556, #8680, .T. ) ;
#13930=DIRECTION ( 'NONE',  ( 0.000000000000000000, 1.000000000000000000, 0.000000000000000000 ) ) ;
#13936=CIRCLE ( 'NONE', #8184, 0.03937007874015751446 ) ;
#13939=CARTESIAN_POINT ( 'NONE',  ( 0.06351958502452506594, -0.1023622047244094474, -0.2357441700067326729 ) ) ;
#13941=DIRECTION ( 'NONE',  ( 1.000000000000000000, 0.000000000000000000, 1.445602896647339903E-16 ) ) ;
#13943=ORIENTED_EDGE ( 'NONE', *, *, #9254, .T. ) ;
#13948=CIRCLE ( 'NONE', #6934, 0.003937007874015737569 ) ;
#13949=CARTESIAN_POINT ( 'NONE',  ( -0.06351958502436047538, -0.1023622047244094474, -0.2357441700068276802 ) ) ;
#13952=DIRECTION ( 'NONE',  ( -5.204170427930408030E-14, 0.000000000000000000, -1.000000000000000000 ) ) ;
#13954=DIRECTION ( 'NONE',  ( -1.000000000000000000, -0.000000000000000000, -1.445602896647339903E-16 ) ) ;
#13956=DIRECTION ( 'NONE',  ( 0.000000000000000000, 0.000000000000000000, -1.000000000000000000 ) ) ;
#13958=CIRCLE ( 'NONE', #8959, 0.003937007874015724558 ) ;
#13962=VERTEX_POINT ( 'NONE', #14755 ) ;
#13963=ADVANCED_FACE ( 'NONE', ( #11215 ), #1740, .F. ) ;
#13965=ORIENTED_EDGE ( 'NONE', *, *, #1053, .T. ) ;
#13970=DIRECTION ( 'NONE',  ( -1.000000000000000000, 0.000000000000000000, 0.000000000000000000 ) ) ;
#13971=AXIS2_PLACEMENT_3D ( 'NONE', #4818, #6150, #13515 ) ;
#13975=FACE_OUTER_BOUND ( 'NONE', #14457, .T. ) ;
#13977=ORIENTED_EDGE ( 'NONE', *, *, #10836, .T. ) ;
#13978=DIRECTION ( 'NONE',  ( -0.5000000000000001110, 0.000000000000000000, 0.8660254037844385966 ) ) ;
#13979=LINE ( 'NONE', #14051, #10847 ) ;
#13984=VERTEX_POINT ( 'NONE', #5404 ) ;
#13985=VECTOR ( 'NONE', #9702, 39.37007874015748143 ) ;
#13986=VERTEX_POINT ( 'NONE', #5310 ) ;
#13988=ORIENTED_EDGE ( 'NONE', *, *, #8047, .F. ) ;
#13989=ORIENTED_EDGE ( 'NONE', *, *, #14448, .T. ) ;
#13992=CARTESIAN_POINT ( 'NONE',  ( 0.5610236220472175628, -0.4881889763779528324, 0.2102555114175294892 ) ) ;
#13993=LINE ( 'NONE', #1156, #9663 ) ;
#13995=EDGE_CURVE ( 'NONE', #6393, #11911, #10038, .T. ) ;
#14005=DIRECTION ( 'NONE',  ( -4.336808689942014285E-16, 0.000000000000000000, 1.000000000000000000 ) ) ;
#14006=DIRECTION ( 'NONE',  ( -1.000000000000000000, -0.000000000000000000, -0.000000000000000000 ) ) ;
#14010=CARTESIAN_POINT ( 'NONE',  ( -0.06299212598414161146, -0.2952755905511811330, -0.3757906139821208247 ) ) ;
#14012=ORIENTED_EDGE ( 'NONE', *, *, #9597, .F. ) ;
#14014=ADVANCED_FACE ( 'NONE', ( #5239 ), #2913, .F. ) ;
#14015=CARTESIAN_POINT ( 'NONE',  ( -0.5610236220472173407, -0.4881889763779528324, 0.2102555114175287954 ) ) ;
#14016=EDGE_CURVE ( 'NONE', #7217, #7115, #13681, .T. ) ;
#14017=ORIENTED_EDGE ( 'NONE', *, *, #6388, .F. ) ;
#14026=DIRECTION ( 'NONE',  ( 1.000000000000000000, 1.734723475976817507E-14, 0.000000000000000000 ) ) ;
#14029=DIRECTION ( 'NONE',  ( -0.000000000000000000, -1.000000000000000000, -0.000000000000000000 ) ) ;
#14032=DIRECTION ( 'NONE',  ( 0.4999999999999992228, 0.000000000000000000, 0.8660254037844391517 ) ) ;
#14034=CARTESIAN_POINT ( 'NONE',  ( -0.4307978335858689278, -0.003937007874015747977, 0.4279391777402706265 ) ) ;
#14035=VERTEX_POINT ( 'NONE', #2753 ) ;
#14037=ADVANCED_FACE ( 'NONE', ( #2205 ), #15281, .T. ) ;
#14047=DIRECTION ( 'NONE',  ( -0.000000000000000000, -1.000000000000000000, -0.000000000000000000 ) ) ;
#14048=CARTESIAN_POINT ( 'NONE',  ( -0.5398975377803494347, -0.4921259842519685179, 0.2389729469846940679 ) ) ;
#14051=CARTESIAN_POINT ( 'NONE',  ( -0.2373612774289040883, -0.4921259842519685179, 0.06430355563116459117 ) ) ;
#14052=DIRECTION ( 'NONE',  ( 1.000000000000000000, 0.000000000000000000, 3.476578583725179813E-16 ) ) ;
#14054=DIRECTION ( 'NONE',  ( 0.5000000000000004441, 0.000000000000000000, -0.8660254037844383745 ) ) ;
#14055=ORIENTED_EDGE ( 'NONE', *, *, #14094, .T. ) ;
#14057=DIRECTION ( 'NONE',  ( -1.000000000000000000, -0.000000000000000000, -0.000000000000000000 ) ) ;
#14060=ORIENTED_EDGE ( 'NONE', *, *, #39, .F. ) ;
#14062=EDGE_CURVE ( 'NONE', #4029, #10145, #6661, .T. ) ;
#14068=EDGE_LOOP ( 'NONE', ( #4004, #13332, #14361, #12724 ) ) ;
#14069=ORIENTED_EDGE ( 'NONE', *, *, #5752, .T. ) ;
#14073=FACE_OUTER_BOUND ( 'NONE', #15026, .T. ) ;
#14077=LINE ( 'NONE', #8134, #10580 ) ;
#14081=AXIS2_PLACEMENT_3D ( 'NONE', #8752, #12055, #11991 ) ;
#14082=EDGE_CURVE ( 'NONE', #3335, #5966, #7919, .T. ) ;
#14083=LINE ( 'NONE', #5929, #5835 ) ;
#14084=CARTESIAN_POINT ( 'NONE',  ( -0.5576140732134202693, -0.4921259842519685179, 0.2082870074805209526 ) ) ;
#14085=ORIENTED_EDGE ( 'NONE', *, *, #5754, .F. ) ;
#14088=CIRCLE ( 'NONE', #2576, 0.04330708661417331101 ) ;
#14089=AXIS2_PLACEMENT_3D ( 'NONE', #13911, #12809, #3181 ) ;
#14090=CARTESIAN_POINT ( 'NONE',  ( 0.4591888763630541104, -0.4921259842519685179, 0.3787644491703230365 ) ) ;
#14091=VECTOR ( 'NONE', #5547, 39.37007874015748143 ) ;
#14094=EDGE_CURVE ( 'NONE', #5898, #12947, #6402, .T. ) ;
#14095=CARTESIAN_POINT ( 'NONE',  ( -0.5899421238646493926, -0.003937007874015747977, 0.1591122789105256785 ) ) ;
#14097=DIRECTION ( 'NONE',  ( 1.000000000000000000, 0.000000000000000000, 0.000000000000000000 ) ) ;
#14100=DIRECTION ( 'NONE',  ( 0.4999999999999979461, 0.000000000000000000, 0.8660254037844398178 ) ) ;
#14103=AXIS2_PLACEMENT_3D ( 'NONE', #2714, #5126, #8808 ) ;
#14110=VECTOR ( 'NONE', #10431, 39.37007874015748143 ) ;
#14111=ORIENTED_EDGE ( 'NONE', *, *, #6760, .T. ) ;
#14112=EDGE_LOOP ( 'NONE', ( #13528, #14069, #3942, #10672 ) ) ;
#14113=EDGE_CURVE ( 'NONE', #7462, #13020, #10573, .T. ) ;
#14114=FACE_OUTER_BOUND ( 'NONE', #8492, .T. ) ;
#14115=DIRECTION ( 'NONE',  ( -0.8660254037844405950, -4.336808689942015369E-15, -0.4999999999999967804 ) ) ;
#14120=VECTOR ( 'NONE', #1189, 39.37007874015748143 ) ;
#14122=DIRECTION ( 'NONE',  ( 1.445602896647339903E-16, 0.000000000000000000, -1.000000000000000000 ) ) ;
#14124=LINE ( 'NONE', #7061, #455 ) ;
#14126=FACE_OUTER_BOUND ( 'NONE', #4941, .T. ) ;
#14129=EDGE_CURVE ( 'NONE', #7462, #13509, #5657, .T. ) ;
#14135=AXIS2_PLACEMENT_3D ( 'NONE', #1605, #2848, #1692 ) ;
#14137=ORIENTED_EDGE ( 'NONE', *, *, #9611, .T. ) ;
#14142=EDGE_LOOP ( 'NONE', ( #13087, #605, #583, #1938 ) ) ;
#14145=DIRECTION ( 'NONE',  ( 0.000000000000000000, 0.000000000000000000, 1.000000000000000000 ) ) ;
#14148=AXIS2_PLACEMENT_3D ( 'NONE', #15046, #10428, #15121 ) ;
#14149=VECTOR ( 'NONE', #12479, 39.37007874015748143 ) ;
#14150=LINE ( 'NONE', #12745, #5178 ) ;
#14152=EDGE_CURVE ( 'NONE', #12616, #2098, #7995, .T. ) ;
#14156=FACE_OUTER_BOUND ( 'NONE', #530, .T. ) ;
#14158=EDGE_LOOP ( 'NONE', ( #4221, #12069, #2490 ) ) ;
#14159=EDGE_CURVE ( 'NONE', #1302, #2464, #13936, .T. ) ;
#14160=ORIENTED_EDGE ( 'NONE', *, *, #3196, .T. ) ;
#14164=CIRCLE ( 'NONE', #1401, 0.003937007874015741038 ) ;
#14165=ORIENTED_EDGE ( 'NONE', *, *, #2616, .F. ) ;
#14170=DIRECTION ( 'NONE',  ( 0.5000000000000001110, 0.000000000000000000, -0.8660254037844385966 ) ) ;
#14171=AXIS2_PLACEMENT_3D ( 'NONE', #9466, #10624, #12814 ) ;
#14172=CARTESIAN_POINT ( 'NONE',  ( 0.4822834645669299980, -0.09448818897637796532, 0.3466374647693609146 ) ) ;
#14174=LINE ( 'NONE', #12919, #3443 ) ;
#14175=LINE ( 'NONE', #9309, #15380 ) ;
#14177=AXIS2_PLACEMENT_3D ( 'NONE', #10598, #5727, #15303 ) ;
#14178=ORIENTED_EDGE ( 'NONE', *, *, #11999, .F. ) ;
#14181=AXIS2_PLACEMENT_3D ( 'NONE', #13672, #514, #13898 ) ;
#14186=CARTESIAN_POINT ( 'NONE',  ( -0.4586614173228354407, -0.1023622047244094474, 0.3875520507749248833 ) ) ;
#14189=EDGE_LOOP ( 'NONE', ( #4419, #11398, #13268, #12918 ) ) ;
#14191=DIRECTION ( 'NONE',  ( 0.8660254037844385966, 0.000000000000000000, 0.5000000000000001110 ) ) ;
#14192=DIRECTION ( 'NONE',  ( 0.000000000000000000, 1.000000000000000000, 0.000000000000000000 ) ) ;
#14193=DIRECTION ( 'NONE',  ( -1.000000000000000000, -1.734723475976817507E-14, 0.000000000000000000 ) ) ;
#14195=EDGE_CURVE ( 'NONE', #3677, #4499, #11430, .T. ) ;
#14197=AXIS2_PLACEMENT_3D ( 'NONE', #6787, #5466, #8046 ) ;
#14200=CIRCLE ( 'NONE', #15204, 0.003937007874015724558 ) ;
#14201=ORIENTED_EDGE ( 'NONE', *, *, #1026, .T. ) ;
#14206=AXIS2_PLACEMENT_3D ( 'NONE', #9617, #13222, #4977 ) ;
#14208=CARTESIAN_POINT ( 'NONE',  ( -0.4307978335858689278, -0.09842519685039370636, 0.4279391777402706820 ) ) ;
#14215=LINE ( 'NONE', #8017, #3948 ) ;
#14216=ADVANCED_FACE ( 'NONE', ( #12005 ), #12067, .F. ) ;
#14220=ORIENTED_EDGE ( 'NONE', *, *, #12944, .T. ) ;
#14222=CARTESIAN_POINT ( 'NONE',  ( 0.5084014747882494856, -0.09842519685039370636, 0.2935257283254013583 ) ) ;
#14225=ORIENTED_EDGE ( 'NONE', *, *, #9450, .F. ) ;
#14226=EDGE_CURVE ( 'NONE', #3128, #6593, #1329, .T. ) ;
#14227=ORIENTED_EDGE ( 'NONE', *, *, #3698, .F. ) ;
#14228=DIRECTION ( 'NONE',  ( 1.000000000000000000, 0.000000000000000000, 1.445602896647339903E-16 ) ) ;
#14229=DIRECTION ( 'NONE',  ( 0.8660254037844385966, 0.000000000000000000, -0.4999999999999998890 ) ) ;
#14232=CARTESIAN_POINT ( 'NONE',  ( 0.000000000000000000, -0.4921259842519685179, 0.000000000000000000 ) ) ;
#14236=DIRECTION ( 'NONE',  ( 0.000000000000000000, 0.000000000000000000, 1.000000000000000000 ) ) ;
#14241=ORIENTED_EDGE ( 'NONE', *, *, #12680, .T. ) ;
#14242=ADVANCED_FACE ( 'NONE', ( #15446 ), #2570, .F. ) ;
#14244=DIRECTION ( 'NONE',  ( -1.000000000000000000, 0.000000000000000000, 0.000000000000000000 ) ) ;
#14250=ORIENTED_EDGE ( 'NONE', *, *, #6322, .F. ) ;
#14252=DIRECTION ( 'NONE',  ( -0.4999999999999981681, 0.000000000000000000, -0.8660254037844397068 ) ) ;
#14253=FACE_OUTER_BOUND ( 'NONE', #4697, .T. ) ;
#14262=DIRECTION ( 'NONE',  ( 0.000000000000000000, 0.000000000000000000, -1.000000000000000000 ) ) ;
#14263=SPHERICAL_SURFACE ( 'NONE', #10713, 0.003937007874015747977 ) ;
#14267=CARTESIAN_POINT ( 'NONE',  ( 0.000000000000000000, -0.4881889763779528324, 0.000000000000000000 ) ) ;
#14268=LINE ( 'NONE', #8304, #6696 ) ;
#14269=CARTESIAN_POINT ( 'NONE',  ( -0.5418660417173573052, -0.4881889763779528324, 0.2355633981508970520 ) ) ;
#14270=ORIENTED_EDGE ( 'NONE', *, *, #3763, .F. ) ;
#14271=ORIENTED_EDGE ( 'NONE', *, *, #13916, .T. ) ;
#14272=ORIENTED_EDGE ( 'NONE', *, *, #7374, .T. ) ;
#14273=DIRECTION ( 'NONE',  ( -1.000000000000000000, -0.000000000000000000, 8.673617379884087537E-15 ) ) ;
#14275=LINE ( 'NONE', #11534, #5892 ) ;
#14279=DIRECTION ( 'NONE',  ( 1.000000000000000000, -0.000000000000000000, 0.000000000000000000 ) ) ;
#14281=FACE_OUTER_BOUND ( 'NONE', #14068, .T. ) ;
#14284=DIRECTION ( 'NONE',  ( 0.000000000000000000, 0.000000000000000000, -1.000000000000000000 ) ) ;
#14285=CARTESIAN_POINT ( 'NONE',  ( 0.09842519685044820443, -0.1023622047244094474, -0.5909884645248143498 ) ) ;
#14287=DIRECTION ( 'NONE',  ( 0.8660254037844365982, -0.000000000000000000, 0.5000000000000035527 ) ) ;
#14289=ORIENTED_EDGE ( 'NONE', *, *, #9263, .T. ) ;
#14291=ORIENTED_EDGE ( 'NONE', *, *, #6835, .T. ) ;
#14292=ORIENTED_EDGE ( 'NONE', *, *, #8122, .T. ) ;
#14294=DIRECTION ( 'NONE',  ( 0.000000000000000000, 0.000000000000000000, 1.000000000000000000 ) ) ;
#14295=CYLINDRICAL_SURFACE ( 'NONE', #3593, 0.003937007874015750579 ) ;
#14296=ADVANCED_FACE ( 'NONE', ( #625 ), #6405, .T. ) ;
#14298=DIRECTION ( 'NONE',  ( 3.614007241618347785E-16, -0.000000000000000000, -1.000000000000000000 ) ) ;
#14300=DIRECTION ( 'NONE',  ( 0.000000000000000000, 0.000000000000000000, -1.000000000000000000 ) ) ;
#14301=DIRECTION ( 'NONE',  ( -0.8660254037844385966, -0.000000000000000000, -0.5000000000000000000 ) ) ;
#14302=CARTESIAN_POINT ( 'NONE',  ( 0.5595825771504284729, -0.4921259842519685179, 0.2048774586467246028 ) ) ;
#14306=ORIENTED_EDGE ( 'NONE', *, *, #7682, .T. ) ;
#14309=ORIENTED_EDGE ( 'NONE', *, *, #12944, .F. ) ;
#14313=FACE_OUTER_BOUND ( 'NONE', #5725, .T. ) ;
#14314=DIRECTION ( 'NONE',  ( -0.000000000000000000, 1.000000000000000000, -0.000000000000000000 ) ) ;
#14316=ORIENTED_EDGE ( 'NONE', *, *, #1858, .F. ) ;
#14317=DIRECTION ( 'NONE',  ( 0.000000000000000000, 0.000000000000000000, -1.000000000000000000 ) ) ;
#14318=EDGE_CURVE ( 'NONE', #9714, #6660, #6487, .T. ) ;
#14319=DIRECTION ( 'NONE',  ( 0.000000000000000000, 0.000000000000000000, -1.000000000000000000 ) ) ;
#14321=EDGE_CURVE ( 'NONE', #9228, #10534, #7191, .T. ) ;
#14323=ORIENTED_EDGE ( 'NONE', *, *, #15367, .F. ) ;
#14325=ORIENTED_EDGE ( 'NONE', *, *, #7896, .T. ) ;
#14331=CARTESIAN_POINT ( 'NONE',  ( -0.09842519685028333631, -0.2952755905511811330, -0.4624047872104675161 ) ) ;
#14337=EDGE_CURVE ( 'NONE', #12501, #8290, #8434, .T. ) ;
#14341=CIRCLE ( 'NONE', #4824, 0.003937007874015724558 ) ;
#14345=LINE ( 'NONE', #8394, #11378 ) ;
#14346=DIRECTION ( 'NONE',  ( 0.4999999999999922284, -0.000000000000000000, -0.8660254037844431485 ) ) ;
#14350=VECTOR ( 'NONE', #9365, 39.37007874015748143 ) ;
#14354=CIRCLE ( 'NONE', #7837, 0.003937007874015749712 ) ;
#14355=DIRECTION ( 'NONE',  ( -0.000000000000000000, 1.000000000000000000, -0.000000000000000000 ) ) ;
#14356=CIRCLE ( 'NONE', #4095, 0.003937007874015750579 ) ;
#14357=DIRECTION ( 'NONE',  ( -0.5000000000000004441, 0.000000000000000000, 0.8660254037844383745 ) ) ;
#14359=DIRECTION ( 'NONE',  ( -0.8660254037844428154, 0.000000000000000000, -0.4999999999999926725 ) ) ;
#14361=ORIENTED_EDGE ( 'NONE', *, *, #224, .F. ) ;
#14362=AXIS2_PLACEMENT_3D ( 'NONE', #12684, #11571, #10175 ) ;
#14365=ORIENTED_EDGE ( 'NONE', *, *, #14416, .F. ) ;
#14366=VECTOR ( 'NONE', #10109, 39.37007874015748854 ) ;
#14371=CARTESIAN_POINT ( 'NONE',  ( 0.03346456692913316738, -0.4921259842519685179, 0.05796233017454786168 ) ) ;
#14374=DIRECTION ( 'NONE',  ( 0.8660254037844400399, 0.000000000000000000, -0.4999999999999977240 ) ) ;
#14376=DIRECTION ( 'NONE',  ( 0.000000000000000000, 0.000000000000000000, 1.000000000000000000 ) ) ;
#14379=CIRCLE ( 'NONE', #10382, 0.003937007874015758385 ) ;
#14385=DIRECTION ( 'NONE',  ( 0.5000000000000001110, 0.000000000000000000, -0.8660254037844384856 ) ) ;
#14387=VERTEX_POINT ( 'NONE', #13939 ) ;
#14388=EDGE_CURVE ( 'NONE', #13891, #11599, #1874, .T. ) ;
#14389=ORIENTED_EDGE ( 'NONE', *, *, #6563, .F. ) ;
#14390=ORIENTED_EDGE ( 'NONE', *, *, #3561, .T. ) ;
#14391=EDGE_CURVE ( 'NONE', #14773, #15003, #6425, .T. ) ;
#14392=ORIENTED_EDGE ( 'NONE', *, *, #3092, .F. ) ;
#14394=TOROIDAL_SURFACE ( 'NONE', #5116, 0.007874015748031495954, 0.003937007874015747977 ) ;
#14395=AXIS2_PLACEMENT_3D ( 'NONE', #10957, #242, #13004 ) ;
#14397=DIRECTION ( 'NONE',  ( 0.000000000000000000, 0.000000000000000000, 1.000000000000000000 ) ) ;
#14401=DIRECTION ( 'NONE',  ( 0.000000000000000000, 0.000000000000000000, -1.000000000000000000 ) ) ;
#14402=CARTESIAN_POINT ( 'NONE',  ( 0.06299212598430634080, -0.4881889763779528324, -0.2377126739437405434 ) ) ;
#14403=CARTESIAN_POINT ( 'NONE',  ( 0.4788739157331329821, -0.09842519685039370636, 0.3446689608323530440 ) ) ;
#14404=ORIENTED_EDGE ( 'NONE', *, *, #15146, .F. ) ;
#14407=CARTESIAN_POINT ( 'NONE',  ( 1.928577636452524610E-17, -0.1023622047244094474, -0.1574803149606299191 ) ) ;
#14408=AXIS2_PLACEMENT_3D ( 'NONE', #6495, #645, #414 ) ;
#14409=VECTOR ( 'NONE', #15431, 39.37007874015748143 ) ;
#14410=CIRCLE ( 'NONE', #7395, 0.003937007874015750579 ) ;
#14411=ORIENTED_EDGE ( 'NONE', *, *, #13834, .T. ) ;
#14412=ORIENTED_EDGE ( 'NONE', *, *, #6166, .F. ) ;
#14413=EDGE_CURVE ( 'NONE', #105, #13903, #12606, .T. ) ;
#14414=VERTEX_POINT ( 'NONE', #4600 ) ;
#14416=EDGE_CURVE ( 'NONE', #9061, #3536, #5617, .T. ) ;
#14419=CIRCLE ( 'NONE', #9672, 0.03937007874015751446 ) ;
#14421=DIRECTION ( 'NONE',  ( 0.000000000000000000, -1.000000000000000000, 0.000000000000000000 ) ) ;
#14424=CARTESIAN_POINT ( 'NONE',  ( -0.09842519685028361387, -0.4881889763779528324, -3.421829314686310476E-17 ) ) ;
#14425=CIRCLE ( 'NONE', #14932, 0.003937007874015780069 ) ;
#14433=AXIS2_PLACEMENT_3D ( 'NONE', #2843, #8092, #11789 ) ;
#14434=ORIENTED_EDGE ( 'NONE', *, *, #2596, .F. ) ;
#14436=EDGE_LOOP ( 'NONE', ( #9784, #8993, #11818, #4274 ) ) ;
#14437=EDGE_CURVE ( 'NONE', #12443, #15072, #8137, .T. ) ;
#14438=CARTESIAN_POINT ( 'NONE',  ( -0.1743691514447623103, -0.4881889763779528324, 0.1734091183126679758 ) ) ;
#14445=DIRECTION ( 'NONE',  ( -0.000000000000000000, 0.000000000000000000, 1.000000000000000000 ) ) ;
#14448=EDGE_CURVE ( 'NONE', #2464, #14862, #14174, .T. ) ;
#14451=CARTESIAN_POINT ( 'NONE',  ( -0.2325106836983179548, -0.09842519685039370636, 0.06483101467138333018 ) ) ;
#14452=FACE_OUTER_BOUND ( 'NONE', #14580, .T. ) ;
#14456=VECTOR ( 'NONE', #5288, 39.37007874015748143 ) ;
#14457=EDGE_LOOP ( 'NONE', ( #15056, #488, #11088, #13462 ) ) ;
#14464=DIRECTION ( 'NONE',  ( 0.5000000000000037748, -0.000000000000000000, 0.8660254037844365982 ) ) ;
#14465=DIRECTION ( 'NONE',  ( 1.000000000000000000, -0.000000000000000000, 0.000000000000000000 ) ) ;
#14468=CARTESIAN_POINT ( 'NONE',  ( 0.5418660417173575272, -0.4881889763779528324, 0.2355633981508976627 ) ) ;
#14469=AXIS2_PLACEMENT_3D ( 'NONE', #7487, #3668, #2638 ) ;
#14470=DIRECTION ( 'NONE',  ( 0.4999999999999967804, 1.935995467731361712E-14, -0.8660254037844405950 ) ) ;
#14471=DIRECTION ( 'NONE',  ( -1.224646799147352961E-16, 0.000000000000000000, -1.000000000000000000 ) ) ;
#14476=LINE ( 'NONE', #6149, #835 ) ;
#14477=DIRECTION ( 'NONE',  ( 0.000000000000000000, 0.000000000000000000, -1.000000000000000000 ) ) ;
#14479=DIRECTION ( 'NONE',  ( -0.8660254037844385966, 0.000000000000000000, -0.5000000000000003331 ) ) ;
#14484=EDGE_CURVE ( 'NONE', #13509, #105, #2019, .T. ) ;
#14485=DIRECTION ( 'NONE',  ( 0.8660254037844365982, -0.000000000000000000, 0.5000000000000035527 ) ) ;
#14486=CARTESIAN_POINT ( 'NONE',  ( 0.5905511811023622659, -0.2952755905511811330, -0.4190977005962939206 ) ) ;
#14492=ORIENTED_EDGE ( 'NONE', *, *, #9169, .F. ) ;
#14497=CARTESIAN_POINT ( 'NONE',  ( -0.5894146648244306119, -0.09842519685039370636, 0.1571437749735178357 ) ) ;
#14498=FACE_OUTER_BOUND ( 'NONE', #6174, .T. ) ;
#14500=EDGE_CURVE ( 'NONE', #6393, #10256, #6412, .T. ) ;
#14502=DIRECTION ( 'NONE',  ( 3.476578583725179813E-16, 0.000000000000000000, -1.000000000000000000 ) ) ;
#14503=CARTESIAN_POINT ( 'NONE',  ( -0.3964138223131424277, -0.2952755905511811330, 0.1515865201236452631 ) ) ;
#14505=ADVANCED_FACE ( 'NONE', ( #15266 ), #5763, .T. ) ;
#14509=DIRECTION ( 'NONE',  ( -1.445602896647339903E-16, -0.000000000000000000, 1.000000000000000000 ) ) ;
#14513=CARTESIAN_POINT ( 'NONE',  ( 0.000000000000000000, 2.161417322834645827, -0.1574803149606299191 ) ) ;
#14516=ORIENTED_EDGE ( 'NONE', *, *, #9644, .T. ) ;
#14517=DIRECTION ( 'NONE',  ( -0.5000000000000008882, 0.000000000000000000, 0.8660254037844380415 ) ) ;
#14519=CARTESIAN_POINT ( 'NONE',  ( 0.4307978335858663188, -0.09448818897637796532, 0.4279391777402731800 ) ) ;
#14521=EDGE_CURVE ( 'NONE', #8551, #9061, #2934, .T. ) ;
#14522=LINE ( 'NONE', #8550, #9449 ) ;
#14523=EDGE_LOOP ( 'NONE', ( #10190, #15009, #2891 ) ) ;
#14524=ORIENTED_EDGE ( 'NONE', *, *, #1305, .F. ) ;
#14526=EDGE_LOOP ( 'NONE', ( #10913, #11794, #5393, #4261 ) ) ;
#14527=ADVANCED_FACE ( 'NONE', ( #710 ), #4287, .F. ) ;
#14534=CARTESIAN_POINT ( 'NONE',  ( 0.4121618538092042816, -0.2952755905511811330, 0.1243101294532687889 ) ) ;
#14538=ORIENTED_EDGE ( 'NONE', *, *, #1552, .T. ) ;
#14541=EDGE_CURVE ( 'NONE', #5934, #10775, #3517, .T. ) ;
#14545=DIRECTION ( 'NONE',  ( 0.000000000000000000, -1.000000000000000000, 0.000000000000000000 ) ) ;
#14546=CARTESIAN_POINT ( 'NONE',  ( -0.5649606299212329708, -0.1023622047244094474, 0.2034364137499347913 ) ) ;
#14552=ORIENTED_EDGE ( 'NONE', *, *, #7960, .T. ) ;
#14555=ORIENTED_EDGE ( 'NONE', *, *, #5872, .F. ) ;
#14558=DIRECTION ( 'NONE',  ( -0.5000000000000001110, 0.000000000000000000, 0.8660254037844385966 ) ) ;
#14560=DIRECTION ( 'NONE',  ( -0.000000000000000000, -1.000000000000000000, -0.000000000000000000 ) ) ;
#14562=CARTESIAN_POINT ( 'NONE',  ( -0.3689582295636769649, -0.2952755905511811885, 0.2857551749459845136 ) ) ;
#14565=ORIENTED_EDGE ( 'NONE', *, *, #7868, .T. ) ;
#14571=ORIENTED_EDGE ( 'NONE', *, *, #1743, .T. ) ;
#14572=EDGE_CURVE ( 'NONE', #8715, #10586, #4691, .T. ) ;
#14573=DIRECTION ( 'NONE',  ( -0.8660254037844383745, 0.000000000000000000, 0.5000000000000004441 ) ) ;
#14574=EDGE_CURVE ( 'NONE', #2963, #9161, #14708, .T. ) ;
#14580=EDGE_LOOP ( 'NONE', ( #6927, #1882, #8210, #9103 ) ) ;
#14581=DIRECTION ( 'NONE',  ( -0.8660254037844385966, 0.000000000000000000, 0.5000000000000001110 ) ) ;
#14585=CARTESIAN_POINT ( 'NONE',  ( 0.09842519685044817668, -0.2952755905511811330, -0.4624047872104674606 ) ) ;
#14586=AXIS2_PLACEMENT_3D ( 'NONE', #4508, #10544, #4583 ) ;
#14589=ORIENTED_EDGE ( 'NONE', *, *, #4098, .T. ) ;
#14594=VERTEX_POINT ( 'NONE', #2552 ) ;
#14596=CARTESIAN_POINT ( 'NONE',  ( 0.5576140732134206024, -0.4921259842519685179, 0.2082870074805215910 ) ) ;
#14598=CIRCLE ( 'NONE', #15095, 0.003937007874015724558 ) ;
#14599=AXIS2_PLACEMENT_3D ( 'NONE', #10041, #14470, #13351 ) ;
#14600=ADVANCED_FACE ( 'NONE', ( #4694 ), #15190, .F. ) ;
#14602=CARTESIAN_POINT ( 'NONE',  ( 0.5860051159906327634, 0.000000000000000000, 0.1591122789105294533 ) ) ;
#14605=EDGE_CURVE ( 'NONE', #12616, #5966, #12453, .T. ) ;
#14607=FACE_OUTER_BOUND ( 'NONE', #1194, .T. ) ;
#14608=LINE ( 'NONE', #2617, #7912 ) ;
#14609=DIRECTION ( 'NONE',  ( -3.973232667114494807E-16, 0.000000000000000000, 1.000000000000000000 ) ) ;
#14610=CARTESIAN_POINT ( 'NONE',  ( -0.1023622047242992716, -0.4921259842519685179, -0.2472069366677729363 ) ) ;
#14612=CARTESIAN_POINT ( 'NONE',  ( 0.5576140732134206024, -0.1023622047244094474, 0.2082870074805215910 ) ) ;
#14613=AXIS2_PLACEMENT_3D ( 'NONE', #7545, #5439, #10233 ) ;
#14615=ORIENTED_EDGE ( 'NONE', *, *, #1238, .T. ) ;
#14616=AXIS2_PLACEMENT_3D ( 'NONE', #4889, #14464, #6935 ) ;
#14619=ORIENTED_EDGE ( 'NONE', *, *, #6972, .T. ) ;
#14622=CARTESIAN_POINT ( 'NONE',  ( 0.4749369078591172411, -0.4881889763779528324, 0.3514880584999470203 ) ) ;
#14628=DIRECTION ( 'NONE',  ( 0.8660254037844385966, 0.000000000000000000, 0.5000000000000000000 ) ) ;
#14630=CARTESIAN_POINT ( 'NONE',  ( -0.1531294576120625917, -0.4921259842519685179, -0.08840933357318583874 ) ) ;
#14641=AXIS2_PLACEMENT_3D ( 'NONE', #9989, #6442, #3007 ) ;
#14642=ORIENTED_EDGE ( 'NONE', *, *, #14541, .T. ) ;
#14649=DIRECTION ( 'NONE',  ( -0.4999999999999817368, -0.000000000000000000, -0.8660254037844491437 ) ) ;
#14650=CARTESIAN_POINT ( 'NONE',  ( 0.09842519685044796851, -0.4881889763779528324, 3.910662073933746312E-17 ) ) ;
#14654=TOROIDAL_SURFACE ( 'NONE', #12907, 0.007874015748031495954, 0.003937007874015747977 ) ;
#14663=VERTEX_POINT ( 'NONE', #3811 ) ;
#14674=ORIENTED_EDGE ( 'NONE', *, *, #10484, .F. ) ;
#14677=DIRECTION ( 'NONE',  ( 0.4999999999999979461, 0.000000000000000000, 0.8660254037844398178 ) ) ;
#14680=PLANE ( 'NONE',  #15202 ) ;
#14681=EDGE_CURVE ( 'NONE', #10896, #4883, #10944, .T. ) ;
#14682=FACE_OUTER_BOUND ( 'NONE', #14867, .T. ) ;
#14683=AXIS2_PLACEMENT_3D ( 'NONE', #3166, #6357, #8086 ) ;
#14686=ORIENTED_EDGE ( 'NONE', *, *, #1501, .F. ) ;
#14688=CARTESIAN_POINT ( 'NONE',  ( 0.1724006475077543565, -0.4881889763779528324, 0.1768186671464649640 ) ) ;
#14689=CARTESIAN_POINT ( 'NONE',  ( 0.000000000000000000, -0.4881889763779528324, 0.1574803149606299191 ) ) ;
#14690=AXIS2_PLACEMENT_3D ( 'NONE', #12024, #10821, #8489 ) ;
#14692=DIRECTION ( 'NONE',  ( 0.000000000000000000, 0.000000000000000000, -1.000000000000000000 ) ) ;
#14697=DIRECTION ( 'NONE',  ( 0.8660254037844384856, 0.000000000000000000, 0.5000000000000003331 ) ) ;
#14700=FACE_OUTER_BOUND ( 'NONE', #13310, .T. ) ;
#14702=VECTOR ( 'NONE', #9154, 39.37007874015748143 ) ;
#14705=CARTESIAN_POINT ( 'NONE',  ( -0.06299212598414173636, -0.4881889763779528324, -0.2366577558633980449 ) ) ;
#14708=CIRCLE ( 'NONE', #7939, 0.007874015748031475137 ) ;
#14713=CIRCLE ( 'NONE', #3198, 0.003937007874015758385 ) ;
#14715=CARTESIAN_POINT ( 'NONE',  ( -0.4141303577462134844, -0.2952755905511811330, 0.1209005806194722171 ) ) ;
#14722=EDGE_CURVE ( 'NONE', #6576, #5898, #14215, .T. ) ;
#14726=ORIENTED_EDGE ( 'NONE', *, *, #1008, .T. ) ;
#14727=ORIENTED_EDGE ( 'NONE', *, *, #15076, .F. ) ;
#14731=CARTESIAN_POINT ( 'NONE',  ( 0.1023622047244638761, -0.2952755905511811330, -0.4190977005962941426 ) ) ;
#14733=DIRECTION ( 'NONE',  ( 0.000000000000000000, 0.000000000000000000, 1.000000000000000000 ) ) ;
#14735=CARTESIAN_POINT ( 'NONE',  ( -0.4749369078591176296, -0.4921259842519685179, 0.3514880584999472424 ) ) ;
#14737=CIRCLE ( 'NONE', #11993, 0.003937007874015724558 ) ;
#14745=ORIENTED_EDGE ( 'NONE', *, *, #1053, .F. ) ;
#14752=DIRECTION ( 'NONE',  ( 0.000000000000000000, 1.000000000000000000, -0.000000000000000000 ) ) ;
#14755=CARTESIAN_POINT ( 'NONE',  ( 0.3478321452968100580, -0.2952755905511811330, 0.3144726105131502858 ) ) ;
#14758=ORIENTED_EDGE ( 'NONE', *, *, #10367, .F. ) ;
#14759=EDGE_LOOP ( 'NONE', ( #1354, #5993, #13107, #10521 ) ) ;
#14761=CARTESIAN_POINT ( 'NONE',  ( 0.1531294576121448037, -0.4881889763779528324, -0.08840933357323313424 ) ) ;
#14762=DIRECTION ( 'NONE',  ( 0.000000000000000000, 0.000000000000000000, -1.000000000000000000 ) ) ;
#14763=EDGE_CURVE ( 'NONE', #2746, #8120, #6920, .T. ) ;
#14765=DIRECTION ( 'NONE',  ( -1.000000000000000000, 8.673617379884087537E-15, 0.000000000000000000 ) ) ;
#14766=CARTESIAN_POINT ( 'NONE',  ( -0.4822834645669303311, -0.1023622047244094474, 0.3466374647693611366 ) ) ;
#14767=LINE ( 'NONE', #8888, #2373 ) ;
#14768=DIRECTION ( 'NONE',  ( 0.000000000000000000, 2.602085213965215059E-14, 1.000000000000000000 ) ) ;
#14769=EDGE_CURVE ( 'NONE', #12161, #9377, #6180, .T. ) ;
#14770=DIRECTION ( 'NONE',  ( 3.476578583725179813E-16, 0.000000000000000000, -1.000000000000000000 ) ) ;
#14771=FACE_OUTER_BOUND ( 'NONE', #3493, .T. ) ;
#14772=CARTESIAN_POINT ( 'NONE',  ( 0.3689582295636777420, -0.2952755905511811330, 0.2857551749459849022 ) ) ;
#14773=VERTEX_POINT ( 'NONE', #14285 ) ;
#14774=VERTEX_POINT ( 'NONE', #8320 ) ;
#14775=VERTEX_POINT ( 'NONE', #7155 ) ;
#14776=EDGE_CURVE ( 'NONE', #8756, #1083, #701, .T. ) ;
#14781=EDGE_CURVE ( 'NONE', #13986, #11669, #2451, .T. ) ;
#14789=VERTEX_POINT ( 'NONE', #8549 ) ;
#14791=VERTEX_POINT ( 'NONE', #12085 ) ;
#14795=CYLINDRICAL_SURFACE ( 'NONE', #7627, 0.003937007874015721089 ) ;
#14796=CARTESIAN_POINT ( 'NONE',  ( -0.09842519685028340570, -0.4881889763779528324, -0.5909884645248143498 ) ) ;
#14799=ADVANCED_FACE ( 'NONE', ( #8411 ), #14680, .F. ) ;
#14803=ORIENTED_EDGE ( 'NONE', *, *, #1427, .F. ) ;
#14807=EDGE_CURVE ( 'NONE', #14775, #13507, #13958, .T. ) ;
#14809=VERTEX_POINT ( 'NONE', #14451 ) ;
#14810=DIRECTION ( 'NONE',  ( 1.000000000000000000, -0.000000000000000000, -0.000000000000000000 ) ) ;
#14812=EDGE_CURVE ( 'NONE', #2740, #9755, #11455, .T. ) ;
#14813=CARTESIAN_POINT ( 'NONE',  ( 0.2661821753648509481, -0.09842519685039372024, 0.03548265769547701703 ) ) ;
#14817=DIRECTION ( 'NONE',  ( -0.8660254037844394848, 0.000000000000000000, -0.4999999999999985567 ) ) ;
#14818=CARTESIAN_POINT ( 'NONE',  ( 0.1734555655881918346, -0.4921259842519685179, 0.1728816592724491952 ) ) ;
#14820=CARTESIAN_POINT ( 'NONE',  ( -0.2393297813659119866, -0.4881889763779528324, 0.06089400679736760302 ) ) ;
#14821=EDGE_CURVE ( 'NONE', #12320, #2868, #5436, .T. ) ;
#14824=ORIENTED_EDGE ( 'NONE', *, *, #15068, .T. ) ;
#14827=SPHERICAL_SURFACE ( 'NONE', #2655, 0.003937007874015747977 ) ;
#14828=DIRECTION ( 'NONE',  ( 0.5000000000000035527, 0.000000000000000000, -0.8660254037844365982 ) ) ;
#14830=CARTESIAN_POINT ( 'NONE',  ( -0.4788739157331333707, -0.09448818897637796532, 0.3446689608323532106 ) ) ;
#14832=LINE ( 'NONE', #7309, #15366 ) ;
#14837=CARTESIAN_POINT ( 'NONE',  ( 0.3589087851413743646, -0.2952755905511811330, 0.1299329768165582988 ) ) ;
#14839=VERTEX_POINT ( 'NONE', #10988 ) ;
#14840=DIRECTION ( 'NONE',  ( 0.4999999999999966693, 0.000000000000000000, 0.8660254037844405950 ) ) ;
#14841=AXIS2_PLACEMENT_3D ( 'NONE', #15222, #6812, #15294 ) ;
#14843=AXIS2_PLACEMENT_3D ( 'NONE', #12411, #13498, #14692 ) ;
#14846=AXIS2_PLACEMENT_3D ( 'NONE', #12293, #10881, #4996 ) ;
#14850=DIRECTION ( 'NONE',  ( 5.204170427930430750E-14, 1.000000000000000000, 0.000000000000000000 ) ) ;
#14852=DIRECTION ( 'NONE',  ( 0.000000000000000000, 1.000000000000000000, 0.000000000000000000 ) ) ;
#14862=VERTEX_POINT ( 'NONE', #5242 ) ;
#14867=EDGE_LOOP ( 'NONE', ( #4109, #7907, #9189, #3469 ) ) ;
#14871=TOROIDAL_SURFACE ( 'NONE', #13357, 0.04330708661417328326, 0.003937007874015747977 ) ;
#14873=AXIS2_PLACEMENT_3D ( 'NONE', #10968, #2572, #3828 ) ;
#14874=DIRECTION ( 'NONE',  ( 0.8660254037844383745, 0.000000000000000000, -0.5000000000000004441 ) ) ;
#14876=DIRECTION ( 'NONE',  ( -1.000000000000000000, -0.000000000000000000, 1.734723475976802677E-14 ) ) ;
#14885=EDGE_CURVE ( 'NONE', #6434, #4737, #7693, .T. ) ;
#14889=AXIS2_PLACEMENT_3D ( 'NONE', #14610, #353, #5114 ) ;
#14892=ORIENTED_EDGE ( 'NONE', *, *, #12483, .F. ) ;
#14894=VECTOR ( 'NONE', #15442, 39.37007874015748143 ) ;
#14899=AXIS2_PLACEMENT_3D ( 'NONE', #12083, #1281, #2594 ) ;
#14904=DIRECTION ( 'NONE',  ( -0.000000000000000000, 1.000000000000000000, -0.000000000000000000 ) ) ;
#14905=FACE_OUTER_BOUND ( 'NONE', #5301, .T. ) ;
#14907=CARTESIAN_POINT ( 'NONE',  ( 0.3294846884549027521, -0.2952755905511811330, 0.2675111804726952314 ) ) ;
#14910=DIRECTION ( 'NONE',  ( -0.8660254037844389297, 0.000000000000000000, 0.4999999999999996114 ) ) ;
#14912=CIRCLE ( 'NONE', #13160, 0.1535433070866141780 ) ;
#14914=VECTOR ( 'NONE', #13203, 39.37007874015748143 ) ;
#14917=ORIENTED_EDGE ( 'NONE', *, *, #1268, .F. ) ;
#14918=TOROIDAL_SURFACE ( 'NONE', #10660, 0.007874015748031495954, 0.003937007874015747977 ) ;
#14919=ORIENTED_EDGE ( 'NONE', *, *, #1610, .F. ) ;
#14921=ADVANCED_FACE ( 'NONE', ( #3061 ), #14988, .T. ) ;
#14923=CARTESIAN_POINT ( 'NONE',  ( 0.5860051159906326523, -0.09448818897637796532, 0.1591122789105293422 ) ) ;
#14925=CIRCLE ( 'NONE', #8164, 0.003937007874015737569 ) ;
#14929=FACE_OUTER_BOUND ( 'NONE', #9013, .T. ) ;
#14931=DIRECTION ( 'NONE',  ( -0.4999999999999979461, 0.000000000000000000, -0.8660254037844398178 ) ) ;
#14932=AXIS2_PLACEMENT_3D ( 'NONE', #15004, #13668, #2936 ) ;
#14934=ORIENTED_EDGE ( 'NONE', *, *, #11031, .T. ) ;
#14936=EDGE_LOOP ( 'NONE', ( #12805, #5622, #14516, #13871 ) ) ;
#14937=VECTOR ( 'NONE', #6448, 39.37007874015748143 ) ;
#14938=ORIENTED_EDGE ( 'NONE', *, *, #11335, .T. ) ;
#14939=VECTOR ( 'NONE', #10430, 39.37007874015748143 ) ;
#14940=FACE_OUTER_BOUND ( 'NONE', #2976, .T. ) ;
#14943=AXIS2_PLACEMENT_3D ( 'NONE', #6672, #805, #5560 ) ;
#14944=CARTESIAN_POINT ( 'NONE',  ( 0.4307978335858664853, -0.09448818897637796532, 0.4279391777402732910 ) ) ;
#14946=LINE ( 'NONE', #15019, #7582 ) ;
#14947=AXIS2_PLACEMENT_3D ( 'NONE', #9099, #7763, #12551 ) ;
#14948=CARTESIAN_POINT ( 'NONE',  ( 0.000000000000000000, -0.4921259842519685179, 0.000000000000000000 ) ) ;
#14951=VECTOR ( 'NONE', #6874, 39.37007874015748143 ) ;
#14953=EDGE_LOOP ( 'NONE', ( #7853, #15413, #15057, #2377 ) ) ;
#14954=ORIENTED_EDGE ( 'NONE', *, *, #14321, .F. ) ;
#14959=EDGE_CURVE ( 'NONE', #6434, #4728, #7451, .T. ) ;
#14960=FACE_OUTER_BOUND ( 'NONE', #9132, .T. ) ;
#14963=DIRECTION ( 'NONE',  ( 0.5000000000000004441, 0.000000000000000000, -0.8660254037844383745 ) ) ;
#14965=CARTESIAN_POINT ( 'NONE',  ( 0.05905511811029059283, -0.1023622047244094474, -0.2366577558633030653 ) ) ;
#14967=CARTESIAN_POINT ( 'NONE',  ( -0.4749369078591176296, -0.4881889763779528324, 0.3514880584999472424 ) ) ;
#14970=ADVANCED_FACE ( 'NONE', ( #498 ), #10040, .T. ) ;
#14971=CARTESIAN_POINT ( 'NONE',  ( 0.2681506793018588741, -0.09842519685039370636, 0.03207310886168006359 ) ) ;
#14974=VERTEX_POINT ( 'NONE', #4164 ) ;
#14975=AXIS2_PLACEMENT_3D ( 'NONE', #14503, #3921, #11035 ) ;
#14978=ADVANCED_FACE ( 'NONE', ( #5484 ), #10271, .F. ) ;
#14981=AXIS2_PLACEMENT_3D ( 'NONE', #11983, #1308, #63 ) ;
#14982=FACE_OUTER_BOUND ( 'NONE', #4276, .T. ) ;
#14983=DIRECTION ( 'NONE',  ( -0.000000000000000000, -1.000000000000000000, -0.000000000000000000 ) ) ;
#14985=DIRECTION ( 'NONE',  ( -0.8660254037844384856, 0.000000000000000000, -0.5000000000000003331 ) ) ;
#14988=SPHERICAL_SURFACE ( 'NONE', #5937, 0.003937007874015747977 ) ;
#14991=PLANE ( 'NONE',  #8193 ) ;
#14997=EDGE_CURVE ( 'NONE', #2079, #9714, #10715, .T. ) ;
#15002=LINE ( 'NONE', #6586, #7872 ) ;
#15003=VERTEX_POINT ( 'NONE', #11770 ) ;
#15004=CARTESIAN_POINT ( 'NONE',  ( -0.4552518684890389244, -0.09448818897637796532, 0.3855835468379172903 ) ) ;
#15005=ADVANCED_FACE ( 'NONE', ( #5783 ), #10575, .T. ) ;
#15006=DIRECTION ( 'NONE',  ( 0.000000000000000000, 0.000000000000000000, 1.000000000000000000 ) ) ;
#15007=DIRECTION ( 'NONE',  ( 0.4999999999999922284, -0.000000000000000000, -0.8660254037844431485 ) ) ;
#15009=ORIENTED_EDGE ( 'NONE', *, *, #9530, .T. ) ;
#15012=CYLINDRICAL_SURFACE ( 'NONE', #10130, 0.1574803149606299191 ) ;
#15013=VERTEX_POINT ( 'NONE', #3463 ) ;
#15014=ORIENTED_EDGE ( 'NONE', *, *, #11903, .F. ) ;
#15019=CARTESIAN_POINT ( 'NONE',  ( -0.1638199706403874467, -0.09842519685039372024, 0.2127791970528254695 ) ) ;
#15021=LINE ( 'NONE', #6531, #15340 ) ;
#15024=ADVANCED_FACE ( 'NONE', ( #12938, #6981 ), #11597, .F. ) ;
#15025=VERTEX_POINT ( 'NONE', #9181 ) ;
#15026=EDGE_LOOP ( 'NONE', ( #9657, #14201, #1714, #10868 ) ) ;
#15027=ORIENTED_EDGE ( 'NONE', *, *, #6655, .F. ) ;
#15028=FACE_OUTER_BOUND ( 'NONE', #7179, .T. ) ;
#15030=LINE ( 'NONE', #11332, #8953 ) ;
#15032=FACE_OUTER_BOUND ( 'NONE', #3857, .T. ) ;
#15034=DIRECTION ( 'NONE',  ( 0.000000000000000000, -1.000000000000000000, 0.000000000000000000 ) ) ;
#15038=DIRECTION ( 'NONE',  ( 0.000000000000000000, 0.000000000000000000, 1.000000000000000000 ) ) ;
#15040=ORIENTED_EDGE ( 'NONE', *, *, #3227, .F. ) ;
#15045=DIRECTION ( 'NONE',  ( 0.000000000000000000, 0.000000000000000000, -1.000000000000000000 ) ) ;
#15046=CARTESIAN_POINT ( 'NONE',  ( -0.5576140732134202693, -0.4881889763779528324, 0.2082870074805209248 ) ) ;
#15048=CARTESIAN_POINT ( 'NONE',  ( -0.06011003619056348030, -0.1023622047244094474, -0.2337756660698198097 ) ) ;
#15050=CARTESIAN_POINT ( 'NONE',  ( 0.06767366483286080259, -0.2952755905511811330, 0.7209811753676967916 ) ) ;
#15055=VERTEX_POINT ( 'NONE', #8240 ) ;
#15056=ORIENTED_EDGE ( 'NONE', *, *, #5315, .T. ) ;
#15057=ORIENTED_EDGE ( 'NONE', *, *, #4302, .T. ) ;
#15059=FACE_OUTER_BOUND ( 'NONE', #12940, .T. ) ;
#15066=LINE ( 'NONE', #4319, #9677 ) ;
#15068=EDGE_CURVE ( 'NONE', #14594, #6761, #6450, .T. ) ;
#15071=ADVANCED_FACE ( 'NONE', ( #11836 ), #7704, .T. ) ;
#15072=VERTEX_POINT ( 'NONE', #10433 ) ;
#15076=EDGE_CURVE ( 'NONE', #10200, #13856, #9970, .T. ) ;
#15084=VECTOR ( 'NONE', #3895, 39.37007874015748143 ) ;
#15086=AXIS2_PLACEMENT_3D ( 'NONE', #3029, #9144, #8817 ) ;
#15088=VECTOR ( 'NONE', #10177, 39.37007874015748143 ) ;
#15089=ORIENTED_EDGE ( 'NONE', *, *, #5458, .T. ) ;
#15091=EDGE_CURVE ( 'NONE', #7182, #13179, #14268, .T. ) ;
#15092=CARTESIAN_POINT ( 'NONE',  ( -0.2661821753646866906, -0.4881889763779528324, 0.03548265769538203052 ) ) ;
#15093=DIRECTION ( 'NONE',  ( 4.336808689942006692E-15, 0.000000000000000000, -1.000000000000000000 ) ) ;
#15095=AXIS2_PLACEMENT_3D ( 'NONE', #756, #10237, #4269 ) ;
#15096=ADVANCED_FACE ( 'NONE', ( #790 ), #1704, .T. ) ;
#15099=EDGE_CURVE ( 'NONE', #9161, #4029, #10215, .T. ) ;
#15102=DIRECTION ( 'NONE',  ( 0.000000000000000000, 0.000000000000000000, -1.000000000000000000 ) ) ;
#15106=CARTESIAN_POINT ( 'NONE',  ( 1.928577636452524610E-17, 2.161417322834645827, 0.1574803149606299191 ) ) ;
#15108=EDGE_LOOP ( 'NONE', ( #9314, #41, #807, #2727 ) ) ;
#15113=VECTOR ( 'NONE', #12559, 39.37007874015748143 ) ;
#15115=DIRECTION ( 'NONE',  ( 0.8660254037844389297, 0.000000000000000000, -0.4999999999999994449 ) ) ;
#15121=DIRECTION ( 'NONE',  ( 0.000000000000000000, 0.000000000000000000, -1.000000000000000000 ) ) ;
#15124=DIRECTION ( 'NONE',  ( -1.000000000000000000, 0.000000000000000000, 0.000000000000000000 ) ) ;
#15127=VECTOR ( 'NONE', #6011, 39.37007874015748143 ) ;
#15129=CARTESIAN_POINT ( 'NONE',  ( 0.5576140732134206024, -0.4881889763779528324, 0.2082870074805215910 ) ) ;
#15131=ORIENTED_EDGE ( 'NONE', *, *, #2238, .T. ) ;
#15134=CIRCLE ( 'NONE', #8874, 0.03937007874015751446 ) ;
#15138=TOROIDAL_SURFACE ( 'NONE', #7141, 0.007874015748031495954, 0.003937007874015747977 ) ;
#15140=DIRECTION ( 'NONE',  ( 0.000000000000000000, 0.000000000000000000, 1.000000000000000000 ) ) ;
#15143=DIRECTION ( 'NONE',  ( -0.8660254037844381525, 0.000000000000000000, 0.5000000000000006661 ) ) ;
#15146=EDGE_CURVE ( 'NONE', #2098, #3506, #9474, .T. ) ;
#15148=ORIENTED_EDGE ( 'NONE', *, *, #2530, .T. ) ;
#15149=DIRECTION ( 'NONE',  ( 0.8660254037844385966, 0.000000000000000000, 0.5000000000000000000 ) ) ;
#15150=CARTESIAN_POINT ( 'NONE',  ( -0.4462573421471757174, -0.2952755905511811330, 0.1439951688233481186 ) ) ;
#15151=AXIS2_PLACEMENT_3D ( 'NONE', #8284, #10719, #9478 ) ;
#15152=AXIS2_PLACEMENT_3D ( 'NONE', #4077, #6876, #9896 ) ;
#15155=CARTESIAN_POINT ( 'NONE',  ( -0.4342073824196659437, -0.09842519685039370636, 0.4299076816772786080 ) ) ;
#15156=VERTEX_POINT ( 'NONE', #8389 ) ;
#15157=CIRCLE ( 'NONE', #12406, 0.003937007874015758385 ) ;
#15158=EDGE_LOOP ( 'NONE', ( #1279, #10597, #9625, #3966 ) ) ;
#15159=DIRECTION ( 'NONE',  ( 0.000000000000000000, 0.000000000000000000, 1.000000000000000000 ) ) ;
#15161=ORIENTED_EDGE ( 'NONE', *, *, #8267, .F. ) ;
#15162=AXIS2_PLACEMENT_3D ( 'NONE', #1719, #14649, #13775 ) ;
#15175=ADVANCED_FACE ( 'NONE', ( #9734, #1198 ), #2438, .F. ) ;
#15177=ORIENTED_EDGE ( 'NONE', *, *, #4510, .T. ) ;
#15179=ORIENTED_EDGE ( 'NONE', *, *, #12527, .F. ) ;
#15180=AXIS2_PLACEMENT_3D ( 'NONE', #9178, #12713, #13956 ) ;
#15183=CYLINDRICAL_SURFACE ( 'NONE', #6102, 0.003937007874015724558 ) ;
#15185=EDGE_CURVE ( 'NONE', #12201, #4124, #8613, .T. ) ;
#15190=TOROIDAL_SURFACE ( 'NONE', #1947, 0.007874015748031495954, 0.003937007874015747977 ) ;
#15195=EDGE_CURVE ( 'NONE', #6593, #13559, #13718, .T. ) ;
#15196=ORIENTED_EDGE ( 'NONE', *, *, #4030, .F. ) ;
#15201=VERTEX_POINT ( 'NONE', #251 ) ;
#15202=AXIS2_PLACEMENT_3D ( 'NONE', #2685, #13417, #1351 ) ;
#15203=DIRECTION ( 'NONE',  ( -0.000000000000000000, -1.000000000000000000, -0.000000000000000000 ) ) ;
#15204=AXIS2_PLACEMENT_3D ( 'NONE', #2362, #9511, #6994 ) ;
#15207=PLANE ( 'NONE',  #11479 ) ;
#15209=DIRECTION ( 'NONE',  ( -0.000000000000000000, 0.000000000000000000, 1.000000000000000000 ) ) ;
#15210=ORIENTED_EDGE ( 'NONE', *, *, #14437, .F. ) ;
#15216=VERTEX_POINT ( 'NONE', #12157 ) ;
#15221=EDGE_LOOP ( 'NONE', ( #2123, #5431, #15400, #7718, #11928 ) ) ;
#15222=CARTESIAN_POINT ( 'NONE',  ( 0.2393297813660762718, -0.4881889763779528324, 0.06089400679746261036 ) ) ;
#15223=DIRECTION ( 'NONE',  ( 0.000000000000000000, -1.000000000000000000, 0.000000000000000000 ) ) ;
#15229=EDGE_LOOP ( 'NONE', ( #3174, #7235, #9858 ) ) ;
#15231=DIRECTION ( 'NONE',  ( 0.8660254037844405950, 0.000000000000000000, -0.4999999999999966693 ) ) ;
#15232=AXIS2_PLACEMENT_3D ( 'NONE', #8299, #6891, #1028 ) ;
#15233=DIRECTION ( 'NONE',  ( 0.8660254037844383745, -0.000000000000000000, 0.5000000000000002220 ) ) ;
#15242=FACE_OUTER_BOUND ( 'NONE', #14158, .T. ) ;
#15243=EDGE_CURVE ( 'NONE', #6007, #8, #11273, .T. ) ;
#15248=DIRECTION ( 'NONE',  ( 0.000000000000000000, -1.000000000000000000, 0.000000000000000000 ) ) ;
#15249=LINE ( 'NONE', #14302, #13870 ) ;
#15253=ORIENTED_EDGE ( 'NONE', *, *, #1233, .T. ) ;
#15258=DIRECTION ( 'NONE',  ( -3.075191616504334757E-15, 0.000000000000000000, 1.000000000000000000 ) ) ;
#15266=FACE_OUTER_BOUND ( 'NONE', #3216, .T. ) ;
#15267=CARTESIAN_POINT ( 'NONE',  ( -0.4339188594849095471, -0.2952755905511811330, 0.1732400634307318665 ) ) ;
#15268=DIRECTION ( 'NONE',  ( 0.000000000000000000, -1.000000000000000000, 0.000000000000000000 ) ) ;
#15272=ORIENTED_EDGE ( 'NONE', *, *, #8195, .T. ) ;
#15274=ORIENTED_EDGE ( 'NONE', *, *, #5770, .F. ) ;
#15278=DIRECTION ( 'NONE',  ( 5.642372883946976675E-29, -6.505213034913038437E-15, 1.000000000000000000 ) ) ;
#15279=DIRECTION ( 'NONE',  ( -0.5000000000000004441, -0.000000000000000000, 0.8660254037844382635 ) ) ;
#15280=ORIENTED_EDGE ( 'NONE', *, *, #9246, .T. ) ;
#15281=CYLINDRICAL_SURFACE ( 'NONE', #8935, 0.003937007874015721089 ) ;
#15285=DIRECTION ( 'NONE',  ( 0.000000000000000000, -1.000000000000000000, 0.000000000000000000 ) ) ;
#15287=DIRECTION ( 'NONE',  ( -0.8660254037844394848, 0.000000000000000000, 0.4999999999999985567 ) ) ;
#15288=VERTEX_POINT ( 'NONE', #7673 ) ;
#15289=EDGE_LOOP ( 'NONE', ( #1991, #13037, #14227, #7382 ) ) ;
#15290=ORIENTED_EDGE ( 'NONE', *, *, #5938, .T. ) ;
#15294=DIRECTION ( 'NONE',  ( 0.8660254037844395958, 0.000000000000000000, -0.4999999999999982236 ) ) ;
#15295=CARTESIAN_POINT ( 'NONE',  ( -0.4586614173228359959, -0.1023622047244094474, 0.3875520507749251053 ) ) ;
#15300=CARTESIAN_POINT ( 'NONE',  ( -0.1023622047242992161, -0.2952755905511811330, -0.4190977005962941981 ) ) ;
#15301=EDGE_CURVE ( 'NONE', #1810, #5085, #3706, .T. ) ;
#15302=ORIENTED_EDGE ( 'NONE', *, *, #10486, .F. ) ;
#15303=DIRECTION ( 'NONE',  ( -0.8660254037844428154, 0.000000000000000000, -0.4999999999999926725 ) ) ;
#15304=EDGE_CURVE ( 'NONE', #5535, #5050, #474, .T. ) ;
#15305=DIRECTION ( 'NONE',  ( 3.973232667114494807E-16, -0.000000000000000000, -1.000000000000000000 ) ) ;
#15306=CARTESIAN_POINT ( 'NONE',  ( -0.1804058482824385523, -0.4881889763779528324, -0.1041573650692488306 ) ) ;
#15310=CARTESIAN_POINT ( 'NONE',  ( -0.5433070866141463950, -0.4881889763779528324, 0.2409414509217019384 ) ) ;
#15313=ORIENTED_EDGE ( 'NONE', *, *, #6972, .F. ) ;
#15319=DIRECTION ( 'NONE',  ( -0.000000000000000000, 1.000000000000000000, -0.000000000000000000 ) ) ;
#15323=CARTESIAN_POINT ( 'NONE',  ( 0.4788739157331329821, -0.1023622047244094474, 0.3446689608323529885 ) ) ;
#15336=FACE_BOUND ( 'NONE', #10875, .T. ) ;
#15337=EDGE_CURVE ( 'NONE', #7829, #12817, #2465, .T. ) ;
#15339=DIRECTION ( 'NONE',  ( 0.000000000000000000, 0.000000000000000000, -1.000000000000000000 ) ) ;
#15340=VECTOR ( 'NONE', #11176, 39.37007874015748143 ) ;
#15342=CYLINDRICAL_SURFACE ( 'NONE', #159, 0.003937007874015758385 ) ;
#15346=ORIENTED_EDGE ( 'NONE', *, *, #14226, .T. ) ;
#15348=AXIS2_PLACEMENT_3D ( 'NONE', #6863, #10551, #3438 ) ;
#15350=CIRCLE ( 'NONE', #6078, 0.003937007874015758385 ) ;
#15353=SPHERICAL_SURFACE ( 'NONE', #7612, 0.003937007874015747977 ) ;
#15355=CARTESIAN_POINT ( 'NONE',  ( 0.2353927734920605308, -0.09842519685039370636, 0.06771310446505662828 ) ) ;
#15360=CARTESIAN_POINT ( 'NONE',  ( 0.000000000000000000, -0.003937007874015747977, -0.5870514566507987197 ) ) ;
#15362=VECTOR ( 'NONE', #2048, 39.37007874015748143 ) ;
#15363=DIRECTION ( 'NONE',  ( 0.4999999999999827915, -0.000000000000000000, -0.8660254037844488106 ) ) ;
#15366=VECTOR ( 'NONE', #1369, 39.37007874015748143 ) ;
#15367=EDGE_CURVE ( 'NONE', #13986, #13529, #12981, .T. ) ;
#15372=ORIENTED_EDGE ( 'NONE', *, *, #14722, .F. ) ;
#15377=AXIS2_PLACEMENT_3D ( 'NONE', #10496, #11587, #640 ) ;
#15380=VECTOR ( 'NONE', #14252, 39.37007874015748143 ) ;
#15383=DIRECTION ( 'NONE',  ( 1.000000000000000000, 0.000000000000000000, 3.476578583725179813E-16 ) ) ;
#15384=PRODUCT_DEFINITION_FORMATION_WITH_SPECIFIED_SOURCE ( 'ANY', '', #1908, .NOT_KNOWN. ) ;
#15389=EDGE_CURVE ( 'NONE', #7774, #13558, #2966, .T. ) ;
#15392=AXIS2_PLACEMENT_3D ( 'NONE', #9120, #6998, #10601 ) ;
#15398=FACE_OUTER_BOUND ( 'NONE', #2604, .T. ) ;
#15399=EDGE_CURVE ( 'NONE', #5085, #12689, #6060, .T. ) ;
#15400=ORIENTED_EDGE ( 'NONE', *, *, #3861, .F. ) ;
#15401=SPHERICAL_SURFACE ( 'NONE', #4878, 0.003937007874015747977 ) ;
#15403=DIRECTION ( 'NONE',  ( 0.4999999999999798495, 0.000000000000000000, -0.8660254037844501429 ) ) ;
#15405=VECTOR ( 'NONE', #4776, 39.37007874015748143 ) ;
#15407=CIRCLE ( 'NONE', #13150, 0.003937007874015749712 ) ;
#15408=DIRECTION ( 'NONE',  ( -1.224646799147352961E-16, 0.000000000000000000, -1.000000000000000000 ) ) ;
#15409=CARTESIAN_POINT ( 'NONE',  ( 0.1734555655881918346, -0.4881889763779528324, 0.1728816592724491952 ) ) ;
#15410=CYLINDRICAL_SURFACE ( 'NONE', #8367, 0.003937007874015724558 ) ;
#15413=ORIENTED_EDGE ( 'NONE', *, *, #8473, .T. ) ;
#15418=AXIS2_PLACEMENT_3D ( 'NONE', #10047, #10214, #6505 ) ;
#15419=EDGE_LOOP ( 'NONE', ( #3925, #7801 ) ) ;
#15422=CARTESIAN_POINT ( 'NONE',  ( 0.06011003619072806392, -0.09842519685039370636, -0.2337756660697248301 ) ) ;
#15426=CIRCLE ( 'NONE', #11678, 0.003937007874015721089 ) ;
#15431=DIRECTION ( 'NONE',  ( 0.5000000000000035527, -0.000000000000000000, -0.8660254037844365982 ) ) ;
#15432=CIRCLE ( 'NONE', #8921, 0.1574803149606299191 ) ;
#15434=ORIENTED_EDGE ( 'NONE', *, *, #3753, .F. ) ;
#15436=VECTOR ( 'NONE', #6999, 39.37007874015748143 ) ;
#15437=ADVANCED_FACE ( 'NONE', ( #2545 ), #9733, .T. ) ;
#15442=DIRECTION ( 'NONE',  ( -0.8660254037844385966, 0.000000000000000000, -0.5000000000000001110 ) ) ;
#15446=FACE_OUTER_BOUND ( 'NONE', #6021, .T. ) ;
#15447=DIRECTION ( 'NONE',  ( 1.000000000000000000, 0.000000000000000000, 0.000000000000000000 ) ) ;
#15448=CIRCLE ( 'NONE', #10704, 0.003937007874015758385 ) ;
#15449=DIRECTION ( 'NONE',  ( -0.8660254037844428154, 0.000000000000000000, -0.4999999999999926725 ) ) ;
#15450=DIRECTION ( 'NONE',  ( 0.000000000000000000, 1.000000000000000000, 0.000000000000000000 ) ) ;
#15453=ORIENTED_EDGE ( 'NONE', *, *, #7248, .F. ) ;
#15454=ORIENTED_EDGE ( 'NONE', *, *, #8508, .F. ) ;
#15456=EDGE_CURVE ( 'NONE', #7829, #13509, #6968, .T. ) ;
#15457=DIRECTION ( 'NONE',  ( -0.5000000000000035527, 0.000000000000000000, 0.8660254037844365982 ) ) ;
#15458=DIRECTION ( 'NONE',  ( 0.4999999999999979461, 0.000000000000000000, 0.8660254037844398178 ) ) ;
#15459=DIRECTION ( 'NONE',  ( -0.4999999999999966693, 0.000000000000000000, 0.8660254037844405950 ) ) ;
#15461=EDGE_CURVE ( 'NONE', #11838, #10253, #4910, .T. ) ;
#15513=COLOUR_RGB('Sky Blue',0.24,0.69,0.87);
#15514=FILL_AREA_STYLE_COLOUR('',#15513);
#15515=FILL_AREA_STYLE('',(#15514));
#15516=SURFACE_STYLE_FILL_AREA(#15515);
#15517=SURFACE_SIDE_STYLE('',(#15516));
#15518=SURFACE_STYLE_USAGE(.BOTH.,#15517);
#15519=PRESENTATION_STYLE_ASSIGNMENT((#15518));
ENDSEC;
END-ISO-10303-21;
